ISO-10303-21;
HEADER;
FILE_DESCRIPTION (('STEP AP214'),
    '1' );
FILE_NAME ('Handle Housing.step',
    '2026-10-06T09:00:30',
    ( '' ),
    ( '' ),
    'SwSTEP 2.0',
    'SolidWorks 2020',
    '' );
FILE_SCHEMA (( 'AUTOMOTIVE_DESIGN' ));
ENDSEC;

DATA;
#6=DIRECTION ( 'NONE',  ( -1.000000000000000000, 1.167320209990000089E-13, -2.253435535809999718E-12 ) ) ;
#8=ORIENTED_EDGE ( 'NONE', *, *, #13852, .T. ) ;
#15=ORIENTED_EDGE ( 'NONE', *, *, #21844, .F. ) ;
#41=ADVANCED_FACE ( 'NONE', ( #13225 ), #5997, .F. ) ;
#42=CARTESIAN_POINT ( 'NONE',  ( 17.19192930164915722, 9.890905752024515607, -1.400000000000002132 ) ) ;
#49=VERTEX_POINT ( 'NONE', #5842 ) ;
#58=DIRECTION ( 'NONE',  ( 1.000000000000000000, 0.000000000000000000, 0.000000000000000000 ) ) ;
#68=VERTEX_POINT ( 'NONE', #12776 ) ;
#78=CARTESIAN_POINT ( 'NONE',  ( 11.39453140432736511, 21.69999999994131912, -70.10000000020002631 ) ) ;
#79=DIRECTION ( 'NONE',  ( -1.000000000000000000, 0.000000000000000000, -2.253435535809999718E-12 ) ) ;
#110=CARTESIAN_POINT ( 'NONE',  ( -10.99999999969999998, 20.99999999999999645, -58.51619611000000276 ) ) ;
#113=CARTESIAN_POINT ( 'NONE',  ( -9.000000000000000000, -130.0000000000000000, -44.10000000000000142 ) ) ;
#122=CARTESIAN_POINT ( 'NONE',  ( 8.999999999800001760, 21.69999999998272244, -51.75615994398976483 ) ) ;
#145=VERTEX_POINT ( 'NONE', #2379 ) ;
#150=AXIS2_PLACEMENT_3D ( 'NONE', #9380, #9854, #2162 ) ;
#152=DIRECTION ( 'NONE',  ( 0.000000000000000000, 1.000000000000000000, 0.000000000000000000 ) ) ;
#156=DIRECTION ( 'NONE',  ( 1.000000000000000000, -0.000000000000000000, -2.257150022439999944E-12 ) ) ;
#158=CARTESIAN_POINT ( 'NONE',  ( 8.999999999770000869, 20.92262005359999577, -43.64010329495499718 ) ) ;
#159=B_SPLINE_CURVE_WITH_KNOTS ( 'NONE', 3,
 ( #30867, #2535, #9297, #23951 ),
 .UNSPECIFIED., .F., .F.,
 ( 4, 4 ),
 ( 0.000000000000000000, 1.000000000000000000 ),
 .UNSPECIFIED. ) ;
#181=CARTESIAN_POINT ( 'NONE',  ( -10.69999999996051798, -35.47467438098505710, -24.90706660654935689 ) ) ;
#185=DIRECTION ( 'NONE',  ( 0.000000000000000000, -2.257145581549999994E-12, -1.000000000000000000 ) ) ;
#187=LINE ( 'NONE', #21734, #27735 ) ;
#193=CIRCLE ( 'NONE', #5696, 0.9999999999999991118 ) ;
#194=CARTESIAN_POINT ( 'NONE',  ( 9.999999999959999997, -24.87868334570000073, -26.27868334529999927 ) ) ;
#196=ORIENTED_EDGE ( 'NONE', *, *, #30807, .F. ) ;
#197=PLANE ( 'NONE',  #19813 ) ;
#230=CARTESIAN_POINT ( 'NONE',  ( -10.69999999930000101, -30.00000000000000000, -28.40000000000000213 ) ) ;
#232=EDGE_CURVE ( 'NONE', #14788, #6922, #2831, .T. ) ;
#234=DIRECTION ( 'NONE',  ( -1.000000000000000000, 0.000000000000000000, 0.000000000000000000 ) ) ;
#238=EDGE_LOOP ( 'NONE', ( #5235, #17859 ) ) ;
#247=ORIENTED_EDGE ( 'NONE', *, *, #6735, .T. ) ;
#249=ORIENTED_EDGE ( 'NONE', *, *, #27861, .T. ) ;
#260=VECTOR ( 'NONE', #12799, 1000.000000000000000 ) ;
#274=LINE ( 'NONE', #1578, #23781 ) ;
#288=B_SPLINE_CURVE_WITH_KNOTS ( 'NONE', 3,
 ( #27666, #1871, #22960, #8785, #25480, #25320 ),
 .UNSPECIFIED., .F., .F.,
 ( 4, 2, 4 ),
 ( 0.000000000000000000, 0.5000000000000000000, 1.000000000000000000 ),
 .UNSPECIFIED. ) ;
#294=ORIENTED_EDGE ( 'NONE', *, *, #26070, .F. ) ;
#316=CARTESIAN_POINT ( 'NONE',  ( -10.69999999999999929, -120.5233595621999996, -31.26042064940000387 ) ) ;
#318=CARTESIAN_POINT ( 'NONE',  ( 10.99289321870000080, -2.500000000000002220, -1.692893218799999877 ) ) ;
#320=CARTESIAN_POINT ( 'NONE',  ( 8.999999999770000869, 20.38323484520000051, -43.42699808786800020 ) ) ;
#323=ADVANCED_FACE ( 'NONE', ( #27664 ), #10999, .T. ) ;
#328=EDGE_LOOP ( 'NONE', ( #29249, #19391, #9540, #3873 ) ) ;
#329=EDGE_LOOP ( 'NONE', ( #30586, #15478, #7122, #23473 ) ) ;
#343=FACE_OUTER_BOUND ( 'NONE', #7511, .T. ) ;
#344=ORIENTED_EDGE ( 'NONE', *, *, #5154, .T. ) ;
#357=LINE ( 'NONE', #17016, #5202 ) ;
#374=ORIENTED_EDGE ( 'NONE', *, *, #19213, .T. ) ;
#375=PLANE ( 'NONE',  #27480 ) ;
#378=CARTESIAN_POINT ( 'NONE',  ( 10.69999999996367102, -29.15111427914373721, -26.30567555911243360 ) ) ;
#388=LINE ( 'NONE', #26960, #26358 ) ;
#391=CARTESIAN_POINT ( 'NONE',  ( -10.69999999999999929, -25.99080750769999781, -31.25597987799999444 ) ) ;
#393=DIRECTION ( 'NONE',  ( -1.000000000000000000, 0.000000000000000000, 0.000000000000000000 ) ) ;
#401=VECTOR ( 'NONE', #6112, 1000.000000000000000 ) ;
#409=VERTEX_POINT ( 'NONE', #30514 ) ;
#411=CARTESIAN_POINT ( 'NONE',  ( 17.16657240420000008, -9.000000000000001776, -0.8000000000000020428 ) ) ;
#414=CARTESIAN_POINT ( 'NONE',  ( 17.16657240490000191, 11.00000000029999825, -0.6999999999999992895 ) ) ;
#418=VECTOR ( 'NONE', #18881, 1000.000000000000000 ) ;
#423=ORIENTED_EDGE ( 'NONE', *, *, #232, .T. ) ;
#441=ORIENTED_EDGE ( 'NONE', *, *, #29887, .F. ) ;
#451=CARTESIAN_POINT ( 'NONE',  ( 18.13191322229999969, 10.47263190749999495, -1.399999999599998990 ) ) ;
#452=ORIENTED_EDGE ( 'NONE', *, *, #845, .F. ) ;
#468=CARTESIAN_POINT ( 'NONE',  ( 12.63351996701598878, 21.70000000000023377, -55.99837678453474865 ) ) ;
#478=CARTESIAN_POINT ( 'NONE',  ( 8.999999999770000869, 21.34659487689999935, -44.03581336912210276 ) ) ;
#482=CARTESIAN_POINT ( 'NONE',  ( -10.00000000039044856, -37.77593666279831552, -25.96758248505484801 ) ) ;
#494=AXIS2_PLACEMENT_3D ( 'NONE', #24933, #10926, #20518 ) ;
#499=CYLINDRICAL_SURFACE ( 'NONE', #6959, 3.000000000000003997 ) ;
#503=EDGE_CURVE ( 'NONE', #26528, #20466, #26706, .T. ) ;
#516=AXIS2_PLACEMENT_3D ( 'NONE', #27552, #8502, #8343 ) ;
#517=ORIENTED_EDGE ( 'NONE', *, *, #14756, .F. ) ;
#520=DIRECTION ( 'NONE',  ( 1.000000000000000000, -0.000000000000000000, -2.257150022439999944E-12 ) ) ;
#522=ORIENTED_EDGE ( 'NONE', *, *, #12199, .T. ) ;
#537=CARTESIAN_POINT ( 'NONE',  ( 10.69999999989999928, -25.00000000000000000, -7.274962170899998526 ) ) ;
#549=CYLINDRICAL_SURFACE ( 'NONE', #29045, 20.00000000000000355 ) ;
#563=CARTESIAN_POINT ( 'NONE',  ( -10.99289321870000080, 19.99999999999999645, -1.692893218799999877 ) ) ;
#587=LINE ( 'NONE', #26687, #5223 ) ;
#588=DIRECTION ( 'NONE',  ( 0.000000000000000000, 0.000000000000000000, 1.000000000000000000 ) ) ;
#594=CARTESIAN_POINT ( 'NONE',  ( 11.59065746419999954, -24.20066399999999973, -1.404983722799999057 ) ) ;
#598=EDGE_CURVE ( 'NONE', #11580, #19721, #22614, .T. ) ;
#599=ORIENTED_EDGE ( 'NONE', *, *, #18165, .T. ) ;
#600=DIRECTION ( 'NONE',  ( -4.656612873080000265E-10, 2.255973186040000320E-12, 1.000000000000000000 ) ) ;
#613=ADVANCED_FACE ( 'NONE', ( #29527 ), #24814, .T. ) ;
#618=FACE_OUTER_BOUND ( 'NONE', #29092, .T. ) ;
#628=CARTESIAN_POINT ( 'NONE',  ( 8.999999999770000869, 20.56980753179999510, -43.48101130890499633 ) ) ;
#629=ORIENTED_EDGE ( 'NONE', *, *, #30807, .T. ) ;
#633=EDGE_CURVE ( 'NONE', #28095, #17368, #24462, .T. ) ;
#635=CARTESIAN_POINT ( 'NONE',  ( 9.999999999971985076, -26.60730091853679369, -31.40000000000158664 ) ) ;
#638=ORIENTED_EDGE ( 'NONE', *, *, #24063, .F. ) ;
#641=ORIENTED_EDGE ( 'NONE', *, *, #7365, .F. ) ;
#642=DIRECTION ( 'NONE',  ( -1.181300906760215537E-13, 0.9986295347541825906, 0.05233595625040957794 ) ) ;
#643=EDGE_CURVE ( 'NONE', #22250, #22666, #3841, .T. ) ;
#644=LINE ( 'NONE', #10231, #6918 ) ;
#650=DIRECTION ( 'NONE',  ( 0.000000000000000000, -1.000000000000000000, 2.257145581549999994E-12 ) ) ;
#659=CARTESIAN_POINT ( 'NONE',  ( 9.999999999969999109, -24.00000000000000000, -28.40000000000000213 ) ) ;
#663=DIRECTION ( 'NONE',  ( 4.901511854548699870E-24, -1.000000000000000000, 2.257145581550420047E-12 ) ) ;
#669=VERTEX_POINT ( 'NONE', #6546 ) ;
#676=ADVANCED_FACE ( 'NONE', ( #8584 ), #13788, .T. ) ;
#689=CARTESIAN_POINT ( 'NONE',  ( 16.20123158609999692, -8.472631907500000281, -1.399999999599998990 ) ) ;
#697=CARTESIAN_POINT ( 'NONE',  ( 8.999999999770000869, 20.70710678120000381, -44.39289321881399530 ) ) ;
#701=ORIENTED_EDGE ( 'NONE', *, *, #14521, .F. ) ;
#721=CARTESIAN_POINT ( 'NONE',  ( -15.88645657644312337, 11.57790908595850965, -1.400000000000001910 ) ) ;
#723=CARTESIAN_POINT ( 'NONE',  ( 13.99999999979999821, 21.69999999929999390, -58.51619795559999915 ) ) ;
#727=ADVANCED_FACE ( 'NONE', ( #13470 ), #28257, .F. ) ;
#728=DIRECTION ( 'NONE',  ( 0.000000000000000000, -2.256683728769999802E-12, -1.000000000000000000 ) ) ;
#745=CARTESIAN_POINT ( 'NONE',  ( 13.99999999979999821, 21.34999999960000139, -58.51619795559999915 ) ) ;
#753=ORIENTED_EDGE ( 'NONE', *, *, #18876, .T. ) ;
#760=CARTESIAN_POINT ( 'NONE',  ( 26.57440914490000239, -3.469982507400000582, -0.6999999999999992895 ) ) ;
#781=EDGE_LOOP ( 'NONE', ( #13468, #9312, #24772, #16453 ) ) ;
#791=CARTESIAN_POINT ( 'NONE',  ( -10.58956532309999865, -24.61949706369999902, -1.102843534499998945 ) ) ;
#806=CARTESIAN_POINT ( 'NONE',  ( 10.69999999999999929, -27.00000000000000000, -28.40000000000000213 ) ) ;
#810=DIRECTION ( 'NONE',  ( 0.000000000000000000, 1.000000000000000000, 0.000000000000000000 ) ) ;
#815=EDGE_CURVE ( 'NONE', #10804, #9494, #21654, .T. ) ;
#817=CARTESIAN_POINT ( 'NONE',  ( 9.000000000000000000, 20.99999999990000887, -67.10000000019999788 ) ) ;
#828=B_SPLINE_CURVE_WITH_KNOTS ( 'NONE', 3,
 ( #13806, #6715, #27644, #25299, #3733, #13332 ),
 .UNSPECIFIED., .F., .F.,
 ( 4, 2, 4 ),
 ( 0.000000000000000000, 0.5000000000000000000, 1.000000000000000000 ),
 .UNSPECIFIED. ) ;
#841=FACE_OUTER_BOUND ( 'NONE', #10613, .T. ) ;
#845=EDGE_CURVE ( 'NONE', #4569, #29453, #19752, .T. ) ;
#848=CARTESIAN_POINT ( 'NONE',  ( -11.66358246699999945, -24.14124255240000139, -1.399999999999998579 ) ) ;
#860=EDGE_LOOP ( 'NONE', ( #6960, #16558, #28447, #28985 ) ) ;
#866=AXIS2_PLACEMENT_3D ( 'NONE', #19748, #7622, #5419 ) ;
#868=CARTESIAN_POINT ( 'NONE',  ( 12.12499559729999810, 20.99999999999999645, -55.73512174120000395 ) ) ;
#870=DIRECTION ( 'NONE',  ( 0.000000000000000000, 1.000000000000000000, 0.000000000000000000 ) ) ;
#888=CARTESIAN_POINT ( 'NONE',  ( -10.69999999999999929, -27.00000000000000000, -31.39999999999999858 ) ) ;
#895=CARTESIAN_POINT ( 'NONE',  ( 10.58956533789999988, -24.61949705740000027, -1.102843518299999381 ) ) ;
#913=AXIS2_PLACEMENT_3D ( 'NONE', #1973, #13609, #2285 ) ;
#915=CARTESIAN_POINT ( 'NONE',  ( 10.69999999999999929, -27.00000000000000000, -28.40000000000000213 ) ) ;
#918=CARTESIAN_POINT ( 'NONE',  ( 10.69999999999999929, -82.23832021929999314, -29.25398675779999991 ) ) ;
#920=CARTESIAN_POINT ( 'NONE',  ( 12.55799324160000019, 21.70000000000000284, -55.95247857500000066 ) ) ;
#926=CARTESIAN_POINT ( 'NONE',  ( -16.17969668575259590, 11.89630849621310738, -1.400000000000001910 ) ) ;
#928=CARTESIAN_POINT ( 'NONE',  ( -10.69999999999829932, -27.75984822496048920, -25.47305230109693142 ) ) ;
#929=DIRECTION ( 'NONE',  ( 1.000000000000000000, 0.000000000000000000, 0.000000000000000000 ) ) ;
#935=CARTESIAN_POINT ( 'NONE',  ( -10.32522729140000095, -25.00000000000000000, -1.399999999999998579 ) ) ;
#938=EDGE_LOOP ( 'NONE', ( #7881, #1510, #28414, #15809 ) ) ;
#939=EDGE_CURVE ( 'NONE', #11197, #5944, #10463, .T. ) ;
#953=CARTESIAN_POINT ( 'NONE',  ( 2.910738317039999947E-11, 21.69999999990000106, -70.09999999999999432 ) ) ;
#955=CARTESIAN_POINT ( 'NONE',  ( 11.69999999989999928, -2.500000000000002220, -2.399999999999999467 ) ) ;
#963=DIRECTION ( 'NONE',  ( 0.000000000000000000, 2.257145581549999994E-12, 1.000000000000000000 ) ) ;
#993=CARTESIAN_POINT ( 'NONE',  ( 10.69999999999999929, -24.97510463969999961, -26.18619911029999869 ) ) ;
#997=CARTESIAN_POINT ( 'NONE',  ( 10.69999999996385576, -38.97238336744932496, -26.38768795973993520 ) ) ;
#1006=DIRECTION ( 'NONE',  ( 0.000000000000000000, -1.000000000000000000, 2.257145581549999994E-12 ) ) ;
#1015=CARTESIAN_POINT ( 'NONE',  ( -10.46447140189999914, 20.99999999999999645, -54.63552859760000047 ) ) ;
#1019=CARTESIAN_POINT ( 'NONE',  ( -10.69999999999979856, -29.23060343762547220, -26.39054106483859741 ) ) ;
#1028=LINE ( 'NONE', #10770, #14022 ) ;
#1040=CARTESIAN_POINT ( 'NONE',  ( 12.77819780750000156, 21.69999999929999390, -56.09999999999999432 ) ) ;
#1043=CARTESIAN_POINT ( 'NONE',  ( 11.57608395239999943, -24.17108566339999953, -0.7028182531999965788 ) ) ;
#1045=CARTESIAN_POINT ( 'NONE',  ( -14.76964124820000102, 19.99999999999999645, -0.6999999999999992895 ) ) ;
#1055=EDGE_LOOP ( 'NONE', ( #16172, #12715, #18535, #3982 ) ) ;
#1062=ORIENTED_EDGE ( 'NONE', *, *, #30828, .F. ) ;
#1064=CARTESIAN_POINT ( 'NONE',  ( -9.000000000000000000, 21.69999999990000106, -67.10000000019999788 ) ) ;
#1071=FACE_OUTER_BOUND ( 'NONE', #24230, .T. ) ;
#1084=EDGE_LOOP ( 'NONE', ( #29264, #25787, #11237, #9561 ) ) ;
#1091=FACE_OUTER_BOUND ( 'NONE', #5069, .T. ) ;
#1093=CARTESIAN_POINT ( 'NONE',  ( -13.99999999969999820, 20.99999999999999645, -51.10000000000000142 ) ) ;
#1106=AXIS2_PLACEMENT_3D ( 'NONE', #23921, #152, #26722 ) ;
#1109=CARTESIAN_POINT ( 'NONE',  ( 10.35000000029999967, -25.00000000000000000, -7.274962170099999348 ) ) ;
#1127=FACE_OUTER_BOUND ( 'NONE', #4296, .T. ) ;
#1128=DIRECTION ( 'NONE',  ( 0.000000000000000000, 0.000000000000000000, -1.000000000000000000 ) ) ;
#1133=CARTESIAN_POINT ( 'NONE',  ( 9.000000000000000000, -55.00000000000001421, -42.39999999999999858 ) ) ;
#1138=CARTESIAN_POINT ( 'NONE',  ( 10.69999999999999929, -24.95051888409999918, -26.20881396380000083 ) ) ;
#1150=EDGE_CURVE ( 'NONE', #26133, #24435, #22901, .T. ) ;
#1155=ORIENTED_EDGE ( 'NONE', *, *, #4608, .T. ) ;
#1166=CARTESIAN_POINT ( 'NONE',  ( -10.69999999930000101, -24.87867965640000278, -30.52132034359999935 ) ) ;
#1178=CARTESIAN_POINT ( 'NONE',  ( 13.88844815065594496, 21.69999999930212198, -57.58022008509880862 ) ) ;
#1185=CARTESIAN_POINT ( 'NONE',  ( 10.32522729140000095, -24.73114799960000099, -1.399999999999998579 ) ) ;
#1188=FACE_OUTER_BOUND ( 'NONE', #30134, .T. ) ;
#1191=CARTESIAN_POINT ( 'NONE',  ( -10.00000000024713742, -28.51085694111269575, -31.02135916506436430 ) ) ;
#1194=VECTOR ( 'NONE', #8324, 1000.000000000000000 ) ;
#1195=AXIS2_PLACEMENT_3D ( 'NONE', #14636, #5486, #19510 ) ;
#1202=CARTESIAN_POINT ( 'NONE',  ( -10.97092057897609862, -24.67424207454737939, -1.714865362423650508 ) ) ;
#1209=AXIS2_PLACEMENT_3D ( 'NONE', #16925, #19297, #12205 ) ;
#1215=AXIS2_PLACEMENT_3D ( 'NONE', #2118, #1815, #4167 ) ;
#1216=CYLINDRICAL_SURFACE ( 'NONE', #11313, 3.000000000000005329 ) ;
#1218=CYLINDRICAL_SURFACE ( 'NONE', #22576, 3.000000000000003997 ) ;
#1221=LINE ( 'NONE', #1064, #2721 ) ;
#1224=FACE_OUTER_BOUND ( 'NONE', #25517, .T. ) ;
#1229=LINE ( 'NONE', #17884, #20251 ) ;
#1236=VECTOR ( 'NONE', #16768, 1000.000000000000000 ) ;
#1238=ORIENTED_EDGE ( 'NONE', *, *, #21745, .T. ) ;
#1242=DIRECTION ( 'NONE',  ( 0.000000000000000000, 0.000000000000000000, 1.000000000000000000 ) ) ;
#1244=VERTEX_POINT ( 'NONE', #12847 ) ;
#1271=ADVANCED_FACE ( 'NONE', ( #28635 ), #11802, .F. ) ;
#1272=AXIS2_PLACEMENT_3D ( 'NONE', #3031, #29928, #8200 ) ;
#1286=ORIENTED_EDGE ( 'NONE', *, *, #8341, .T. ) ;
#1297=EDGE_CURVE ( 'NONE', #23190, #14788, #7235, .T. ) ;
#1300=DIRECTION ( 'NONE',  ( -1.000000000000000000, 0.000000000000000000, 0.000000000000000000 ) ) ;
#1305=CARTESIAN_POINT ( 'NONE',  ( 10.69999999995387086, -31.36650361035140477, -21.96235324005989753 ) ) ;
#1309=EDGE_LOOP ( 'NONE', ( #18962, #2062, #1393, #5608, #28099, #12108, #20122, #17059, #7243, #25749, #28852, #21248 ) ) ;
#1314=ORIENTED_EDGE ( 'NONE', *, *, #4200, .F. ) ;
#1319=VERTEX_POINT ( 'NONE', #21878 ) ;
#1320=ORIENTED_EDGE ( 'NONE', *, *, #24982, .T. ) ;
#1323=DIRECTION ( 'NONE',  ( 0.000000000000000000, 0.000000000000000000, -1.000000000000000000 ) ) ;
#1329=CARTESIAN_POINT ( 'NONE',  ( -10.00000000057842087, -23.99999999999979394, -28.79269908169899495 ) ) ;
#1345=CARTESIAN_POINT ( 'NONE',  ( -11.62710820939999934, -24.17108566160000294, -1.401657795899999392 ) ) ;
#1346=DIRECTION ( 'NONE',  ( -9.868649108069999529E-17, -2.257145581549999994E-12, -1.000000000000000000 ) ) ;
#1348=EDGE_CURVE ( 'NONE', #7041, #9481, #16146, .T. ) ;
#1366=VERTEX_POINT ( 'NONE', #18174 ) ;
#1371=CARTESIAN_POINT ( 'NONE',  ( 18.26261577949329151, 11.17152825599126054, -1.400000000000001910 ) ) ;
#1373=FACE_OUTER_BOUND ( 'NONE', #9906, .T. ) ;
#1388=EDGE_CURVE ( 'NONE', #28481, #19078, #8148, .T. ) ;
#1393=ORIENTED_EDGE ( 'NONE', *, *, #31039, .F. ) ;
#1398=EDGE_LOOP ( 'NONE', ( #8843, #21305, #25039, #18047 ) ) ;
#1407=FACE_OUTER_BOUND ( 'NONE', #15137, .T. ) ;
#1415=FACE_OUTER_BOUND ( 'NONE', #27203, .T. ) ;
#1420=CARTESIAN_POINT ( 'NONE',  ( -8.999999999699999975, 21.34999999950001026, -70.09999999999999432 ) ) ;
#1421=CARTESIAN_POINT ( 'NONE',  ( 10.46446609389999871, 20.99999999999999645, -54.63553390589999736 ) ) ;
#1423=DIRECTION ( 'NONE',  ( -1.000000000000000000, 0.000000000000000000, 0.000000000000000000 ) ) ;
#1425=FACE_OUTER_BOUND ( 'NONE', #16091, .T. ) ;
#1427=VECTOR ( 'NONE', #9255, 1000.000000000000000 ) ;
#1428=ORIENTED_EDGE ( 'NONE', *, *, #28444, .T. ) ;
#1439=EDGE_LOOP ( 'NONE', ( #11897, #21831, #3160, #7996 ) ) ;
#1444=EDGE_LOOP ( 'NONE', ( #2096, #20345, #12000, #15130 ) ) ;
#1447=DIRECTION ( 'NONE',  ( 0.8775825618903718706, -0.4794255386042047262, 0.000000000000000000 ) ) ;
#1449=EDGE_CURVE ( 'NONE', #11197, #15367, #17700, .T. ) ;
#1470=VERTEX_POINT ( 'NONE', #25114 ) ;
#1476=CARTESIAN_POINT ( 'NONE',  ( 10.00000000020000002, -25.00000000000000000, -2.400000000399998612 ) ) ;
#1479=ORIENTED_EDGE ( 'NONE', *, *, #30200, .F. ) ;
#1483=ORIENTED_EDGE ( 'NONE', *, *, #9638, .T. ) ;
#1487=CARTESIAN_POINT ( 'NONE',  ( 9.999999999979998222, -127.2537437101000108, -34.36317024011000143 ) ) ;
#1489=LINE ( 'NONE', #4922, #26302 ) ;
#1495=VECTOR ( 'NONE', #9365, 1000.000000000000000 ) ;
#1500=ORIENTED_EDGE ( 'NONE', *, *, #28250, .F. ) ;
#1501=CARTESIAN_POINT ( 'NONE',  ( -10.69999999996760742, -30.00000000000001421, -28.04899130767095983 ) ) ;
#1503=CARTESIAN_POINT ( 'NONE',  ( -2.299991308520000465E-10, 21.69999999990000106, -70.09999999999999432 ) ) ;
#1508=CARTESIAN_POINT ( 'NONE',  ( -11.63809019400000011, -24.14124255240000139, -0.6999999999999992895 ) ) ;
#1510=ORIENTED_EDGE ( 'NONE', *, *, #2441, .T. ) ;
#1516=EDGE_CURVE ( 'NONE', #28644, #30907, #1985, .T. ) ;
#1524=EDGE_LOOP ( 'NONE', ( #22834, #29814, #9317, #26166 ) ) ;
#1527=CARTESIAN_POINT ( 'NONE',  ( -11.32877539260000077, -24.28840542069999842, -0.7339858089999984347 ) ) ;
#1534=FACE_OUTER_BOUND ( 'NONE', #20098, .T. ) ;
#1559=ORIENTED_EDGE ( 'NONE', *, *, #28153, .F. ) ;
#1578=CARTESIAN_POINT ( 'NONE',  ( -12.77820031409999935, 20.99999999999999645, -56.09999999999999432 ) ) ;
#1592=CARTESIAN_POINT ( 'NONE',  ( 9.999999999958726349, -35.47767383584782408, -24.90806880973072879 ) ) ;
#1595=ORIENTED_EDGE ( 'NONE', *, *, #1972, .F. ) ;
#1604=LINE ( 'NONE', #20794, #16956 ) ;
#1607=VERTEX_POINT ( 'NONE', #10712 ) ;
#1611=CARTESIAN_POINT ( 'NONE',  ( 10.89131017139999891, -24.73114799890000270, -1.811764705899998606 ) ) ;
#1624=EDGE_LOOP ( 'NONE', ( #12461, #24851, #2719, #20904 ) ) ;
#1629=EDGE_CURVE ( 'NONE', #3949, #4546, #9480, .T. ) ;
#1645=VECTOR ( 'NONE', #4875, 1000.000000000000000 ) ;
#1654=CARTESIAN_POINT ( 'NONE',  ( 20.84977244261583706, 16.87341063695685150, -1.399999999999998357 ) ) ;
#1655=DIRECTION ( 'NONE',  ( 2.257102469710000208E-12, 0.000000000000000000, 1.000000000000000000 ) ) ;
#1656=CARTESIAN_POINT ( 'NONE',  ( -9.000000000000000000, 19.99999999999999645, -44.10000000000000142 ) ) ;
#1658=CARTESIAN_POINT ( 'NONE',  ( -13.46485713443429511, 20.99999999997146105, -56.74255209446624093 ) ) ;
#1671=AXIS2_PLACEMENT_3D ( 'NONE', #6906, #26120, #28627 ) ;
#1679=EDGE_CURVE ( 'NONE', #23122, #20967, #8493, .T. ) ;
#1681=CARTESIAN_POINT ( 'NONE',  ( 9.760738032020000787, 19.99999999999999645, -43.05080462335000391 ) ) ;
#1685=CARTESIAN_POINT ( 'NONE',  ( -9.999999999959999997, -29.06671945329999929, -26.22544931050000017 ) ) ;
#1690=EDGE_CURVE ( 'NONE', #12603, #12725, #19535, .T. ) ;
#1700=CARTESIAN_POINT ( 'NONE',  ( 0.000000000000000000, 21.70000000000000284, -44.10000000017312516 ) ) ;
#1704=CIRCLE ( 'NONE', #21365, 4.175165894169885483 ) ;
#1712=AXIS2_PLACEMENT_3D ( 'NONE', #10527, #1242, #20425 ) ;
#1737=VECTOR ( 'NONE', #728, 1000.000000000000000 ) ;
#1750=VERTEX_POINT ( 'NONE', #23623 ) ;
#1755=CYLINDRICAL_SURFACE ( 'NONE', #5919, 1.000000000000000666 ) ;
#1762=CARTESIAN_POINT ( 'NONE',  ( -9.999999999959999997, -29.06671945329999929, -26.22544931050000017 ) ) ;
#1765=CARTESIAN_POINT ( 'NONE',  ( 18.89227650605998932, -19.04064001868236389, -1.399999999999998801 ) ) ;
#1781=ORIENTED_EDGE ( 'NONE', *, *, #21395, .F. ) ;
#1784=ORIENTED_EDGE ( 'NONE', *, *, #11351, .T. ) ;
#1796=EDGE_LOOP ( 'NONE', ( #5260, #1320, #4571, #30312 ) ) ;
#1805=DIRECTION ( 'NONE',  ( 0.000000000000000000, -1.000000000000000000, 0.000000000000000000 ) ) ;
#1811=CARTESIAN_POINT ( 'NONE',  ( -13.67718144140000014, 21.70000000000000284, -57.16242377749999548 ) ) ;
#1815=DIRECTION ( 'NONE',  ( 1.000000000000000000, -6.668066630619518976E-24, -2.257150022442225012E-12 ) ) ;
#1818=CARTESIAN_POINT ( 'NONE',  ( 11.19633374170000018, -24.50869455149999965, -1.530575659700002200 ) ) ;
#1829=CARTESIAN_POINT ( 'NONE',  ( -10.00000000008316370, -24.60099947280619404, -26.55635984007588490 ) ) ;
#1836=DIRECTION ( 'NONE',  ( 2.612942924549014782E-24, -1.000000000000000000, 2.257145581549775024E-12 ) ) ;
#1837=DIRECTION ( 'NONE',  ( 1.000000000000000000, -6.668066630619518976E-24, -2.257150022442225012E-12 ) ) ;
#1845=DIRECTION ( 'NONE',  ( 1.000000000000000000, 0.000000000000000000, -2.257150022439999944E-12 ) ) ;
#1848=DIRECTION ( 'NONE',  ( 1.000000000000000000, -3.757855673434259506E-24, -2.257150022441365115E-12 ) ) ;
#1853=CARTESIAN_POINT ( 'NONE',  ( 10.46446609389999871, 20.99999999999999645, -54.63553390589999736 ) ) ;
#1859=EDGE_LOOP ( 'NONE', ( #31058, #20185, #25944, #5885 ) ) ;
#1866=DIRECTION ( 'NONE',  ( 1.000000000000000000, 3.757855673434259506E-24, -2.257150022441365115E-12 ) ) ;
#1871=CARTESIAN_POINT ( 'NONE',  ( -9.800032898256745284, -130.0000000000000000, -43.01413704553658590 ) ) ;
#1879=ORIENTED_EDGE ( 'NONE', *, *, #15322, .T. ) ;
#1896=VECTOR ( 'NONE', #8931, 1000.000000000000000 ) ;
#1916=CYLINDRICAL_SURFACE ( 'NONE', #2394, 1.700000000000000178 ) ;
#1932=CARTESIAN_POINT ( 'NONE',  ( -9.999999999949999108, -30.49286765380000119, -21.04171673159999756 ) ) ;
#1933=EDGE_LOOP ( 'NONE', ( #30266, #6187, #28949, #10531 ) ) ;
#1949=VECTOR ( 'NONE', #7026, 1000.000000000000000 ) ;
#1957=ADVANCED_FACE ( 'NONE', ( #29792 ), #8224, .F. ) ;
#1965=EDGE_CURVE ( 'NONE', #23901, #1607, #22719, .T. ) ;
#1969=CARTESIAN_POINT ( 'NONE',  ( -9.499999999560001740, 21.70000000000000284, -64.10000000000000853 ) ) ;
#1971=LINE ( 'NONE', #14815, #3096 ) ;
#1972=EDGE_CURVE ( 'NONE', #12725, #15866, #29634, .T. ) ;
#1973=CARTESIAN_POINT ( 'NONE',  ( -9.000000000000000000, 19.99999999999999645, -42.39999999999999858 ) ) ;
#1985=LINE ( 'NONE', #14834, #7163 ) ;
#1989=FACE_BOUND ( 'NONE', #6422, .T. ) ;
#1995=ORIENTED_EDGE ( 'NONE', *, *, #12701, .T. ) ;
#1998=CARTESIAN_POINT ( 'NONE',  ( 9.707106781189999367, 19.99999999999999645, -43.10710678118599759 ) ) ;
#2002=CARTESIAN_POINT ( 'NONE',  ( -10.00000000070000183, -29.30501631370000482, -26.47986984990000181 ) ) ;
#2020=ADVANCED_FACE ( 'NONE', ( #22883 ), #3838, .T. ) ;
#2021=EDGE_CURVE ( 'NONE', #6914, #5828, #23517, .T. ) ;
#2022=CARTESIAN_POINT ( 'NONE',  ( 10.69999999999999929, -24.87867965640000278, -30.52132034359999935 ) ) ;
#2026=ORIENTED_EDGE ( 'NONE', *, *, #3615, .T. ) ;
#2029=ORIENTED_EDGE ( 'NONE', *, *, #10803, .T. ) ;
#2040=CARTESIAN_POINT ( 'NONE',  ( 10.69999999989999928, -2.500000000000002220, -2.399999999999999467 ) ) ;
#2051=CARTESIAN_POINT ( 'NONE',  ( 2.910560681360000016E-11, 19.99999999999999645, -45.10000000000000142 ) ) ;
#2059=ORIENTED_EDGE ( 'NONE', *, *, #8464, .F. ) ;
#2062=ORIENTED_EDGE ( 'NONE', *, *, #2738, .T. ) ;
#2071=CARTESIAN_POINT ( 'NONE',  ( 10.69999999999999929, -27.00000000000000000, -28.40000000000000213 ) ) ;
#2080=DIRECTION ( 'NONE',  ( 0.000000000000000000, -2.257145581549999994E-12, -1.000000000000000000 ) ) ;
#2082=CARTESIAN_POINT ( 'NONE',  ( 26.57440914490000239, -3.469982507400000582, -0.6999999995999997005 ) ) ;
#2083=EDGE_CURVE ( 'NONE', #24262, #22250, #20514, .T. ) ;
#2096=ORIENTED_EDGE ( 'NONE', *, *, #11030, .F. ) ;
#2101=EDGE_CURVE ( 'NONE', #26977, #14341, #7433, .T. ) ;
#2108=VECTOR ( 'NONE', #7734, 1000.000000000000000 ) ;
#2116=ORIENTED_EDGE ( 'NONE', *, *, #25280, .F. ) ;
#2117=DIRECTION ( 'NONE',  ( 0.000000000000000000, 1.000000000000000000, 0.000000000000000000 ) ) ;
#2118=CARTESIAN_POINT ( 'NONE',  ( -10.69999999999999929, -27.00000000000000000, -28.40000000000000213 ) ) ;
#2121=FACE_BOUND ( 'NONE', #7009, .T. ) ;
#2125=ORIENTED_EDGE ( 'NONE', *, *, #4176, .F. ) ;
#2137=EDGE_LOOP ( 'NONE', ( #29446, #13219, #24655, #9479 ) ) ;
#2149=DIRECTION ( 'NONE',  ( 0.8923938138917432150, -1.018860921557045171E-12, -0.4512574441798702374 ) ) ;
#2154=CARTESIAN_POINT ( 'NONE',  ( -10.69999999930000101, -25.00000000000000000, -26.16393202249999916 ) ) ;
#2162=DIRECTION ( 'NONE',  ( -0.8775825618903718706, 0.4794255386042047262, 0.000000000000000000 ) ) ;
#2163=CARTESIAN_POINT ( 'NONE',  ( 13.99999999979999821, 20.99999999999999645, -58.51619795559999915 ) ) ;
#2177=ORIENTED_EDGE ( 'NONE', *, *, #9621, .F. ) ;
#2199=CARTESIAN_POINT ( 'NONE',  ( -10.22459498839999981, -25.00000000000000000, -1.538346542999995181 ) ) ;
#2210=ORIENTED_EDGE ( 'NONE', *, *, #18493, .F. ) ;
#2212=CARTESIAN_POINT ( 'NONE',  ( -10.08101130870000084, 19.99999999999999645, -1.830192468500003944 ) ) ;
#2215=EDGE_LOOP ( 'NONE', ( #12039, #1879, #19313, #18321, #26558, #13314 ) ) ;
#2218=ORIENTED_EDGE ( 'NONE', *, *, #25626, .T. ) ;
#2220=ORIENTED_EDGE ( 'NONE', *, *, #29973, .F. ) ;
#2239=DIRECTION ( 'NONE',  ( -0.000000000000000000, 1.000000000000000000, -2.255973188440000244E-12 ) ) ;
#2241=DIRECTION ( 'NONE',  ( 0.000000000000000000, -1.000000000000000000, 0.000000000000000000 ) ) ;
#2247=CARTESIAN_POINT ( 'NONE',  ( -26.57440607989999748, -3.469982107200002108, -1.399999999999998579 ) ) ;
#2255=VECTOR ( 'NONE', #24072, 1000.000000000000000 ) ;
#2268=EDGE_LOOP ( 'NONE', ( #3914, #1479, #3538, #12148 ) ) ;
#2275=CARTESIAN_POINT ( 'NONE',  ( -24.35520125494996435, 11.39272192119609706, -1.399999999999998801 ) ) ;
#2277=FACE_OUTER_BOUND ( 'NONE', #27313, .T. ) ;
#2285=DIRECTION ( 'NONE',  ( -1.000000000000000000, 0.000000000000000000, 0.000000000000000000 ) ) ;
#2287=CARTESIAN_POINT ( 'NONE',  ( 9.999999999959999997, -24.92624923460000019, -26.23177046869999884 ) ) ;
#2294=DIRECTION ( 'NONE',  ( 0.000000000000000000, 1.000000000000000000, 0.000000000000000000 ) ) ;
#2295=AXIS2_PLACEMENT_3D ( 'NONE', #9813, #21621, #21773 ) ;
#2302=ORIENTED_EDGE ( 'NONE', *, *, #16603, .T. ) ;
#2309=CARTESIAN_POINT ( 'NONE',  ( 9.999999999539999962, 19.99999999999999645, -42.42023091910999710 ) ) ;
#2311=CARTESIAN_POINT ( 'NONE',  ( -10.69999999989999928, -30.49251257979999963, -21.04205368470000082 ) ) ;
#2313=ORIENTED_EDGE ( 'NONE', *, *, #26633, .T. ) ;
#2315=EDGE_CURVE ( 'NONE', #16525, #8872, #29756, .T. ) ;
#2320=DIRECTION ( 'NONE',  ( -0.000000000000000000, 1.000000000000000000, -2.258510841069999963E-12 ) ) ;
#2326=DIRECTION ( 'NONE',  ( -1.000000000000000000, -2.587524353642439916E-24, -2.257144471329210308E-12 ) ) ;
#2344=CARTESIAN_POINT ( 'NONE',  ( 9.000000000029999114, 21.69999999990000106, -70.09999999999999432 ) ) ;
#2358=PRODUCT_DEFINITION ( 'UNKNOWN', '', #14869, #22583 ) ;
#2363=CARTESIAN_POINT ( 'NONE',  ( 8.999999999770000869, 21.53714677049999793, -44.32440694871200293 ) ) ;
#2364=ORIENTED_EDGE ( 'NONE', *, *, #17787, .T. ) ;
#2366=EDGE_CURVE ( 'NONE', #3831, #19704, #12772, .T. ) ;
#2367=CARTESIAN_POINT ( 'NONE',  ( 17.16657240420000008, 11.00000000000000355, -0.8000000000000020428 ) ) ;
#2373=VECTOR ( 'NONE', #6541, 1000.000000000000000 ) ;
#2379=CARTESIAN_POINT ( 'NONE',  ( 10.69999999999999929, -127.2537437101000108, -34.36317024011000143 ) ) ;
#2390=LINE ( 'NONE', #11670, #11281 ) ;
#2391=DIRECTION ( 'NONE',  ( -1.000000000000000000, 0.000000000000000000, -2.257144471330000330E-12 ) ) ;
#2394=AXIS2_PLACEMENT_3D ( 'NONE', #6785, #16381, #4577 ) ;
#2401=ORIENTED_EDGE ( 'NONE', *, *, #28748, .F. ) ;
#2403=B_SPLINE_CURVE_WITH_KNOTS ( 'NONE', 3,
 ( #15394, #22486, #12882, #3429, #15544, #10673 ),
 .UNSPECIFIED., .F., .F.,
 ( 4, 2, 4 ),
 ( 0.000000000000000000, 0.5000000000000000000, 1.000000000000000000 ),
 .UNSPECIFIED. ) ;
#2406=EDGE_CURVE ( 'NONE', #30214, #27320, #10267, .T. ) ;
#2417=DIRECTION ( 'NONE',  ( -1.000000000000000000, 0.000000000000000000, -2.257144471330000330E-12 ) ) ;
#2419=LINE ( 'NONE', #9962, #9011 ) ;
#2425=FACE_BOUND ( 'NONE', #238, .T. ) ;
#2429=CARTESIAN_POINT ( 'NONE',  ( 12.51136270434944109, 21.69999999994217532, -69.72111648971724662 ) ) ;
#2434=CARTESIAN_POINT ( 'NONE',  ( 9.999999999969999109, -29.12127062269999911, -30.52127062070000107 ) ) ;
#2437=VERTEX_POINT ( 'NONE', #29293 ) ;
#2438=ADVANCED_FACE ( 'NONE', ( #3322 ), #12927, .T. ) ;
#2439=CARTESIAN_POINT ( 'NONE',  ( -9.999999999909999104, -25.00000000000000000, -2.399999999999999467 ) ) ;
#2441=EDGE_CURVE ( 'NONE', #1750, #26472, #30812, .T. ) ;
#2444=DIRECTION ( 'NONE',  ( 0.000000000000000000, 2.257157423930000049E-12, 1.000000000000000000 ) ) ;
#2461=CARTESIAN_POINT ( 'NONE',  ( 9.999999999959799268, -29.23060343765324731, -26.39054106487359164 ) ) ;
#2469=CARTESIAN_POINT ( 'NONE',  ( 10.69999999999454232, -129.9401694263537479, -39.98253760374566923 ) ) ;
#2479=ORIENTED_EDGE ( 'NONE', *, *, #11146, .T. ) ;
#2480=DIRECTION ( 'NONE',  ( -1.000000000000000000, 0.000000000000000000, -2.257144471330000330E-12 ) ) ;
#2481=CIRCLE ( 'NONE', #494, 3.999999999669999973 ) ;
#2483=DIRECTION ( 'NONE',  ( -1.000000000000000000, 0.000000000000000000, 0.000000000000000000 ) ) ;
#2487=VERTEX_POINT ( 'NONE', #30968 ) ;
#2490=ORIENTED_EDGE ( 'NONE', *, *, #28681, .T. ) ;
#2496=CARTESIAN_POINT ( 'NONE',  ( 0.000000000000000000, 0.000000000000000000, -44.00000000000000000 ) ) ;
#2500=DIRECTION ( 'NONE',  ( 0.000000000000000000, -1.000000000000000000, 0.000000000000000000 ) ) ;
#2501=AXIS2_PLACEMENT_3D ( 'NONE', #22301, #27019, #5916 ) ;
#2503=CARTESIAN_POINT ( 'NONE',  ( 8.999999999770000869, 20.99999999999999645, -60.10000000000000142 ) ) ;
#2517=CARTESIAN_POINT ( 'NONE',  ( 10.00000000070000183, -120.5233595624000174, -31.26042064949999855 ) ) ;
#2518=ORIENTED_EDGE ( 'NONE', *, *, #6735, .F. ) ;
#2522=ORIENTED_EDGE ( 'NONE', *, *, #26927, .T. ) ;
#2524=EDGE_CURVE ( 'NONE', #6267, #3589, #27162, .T. ) ;
#2535=CARTESIAN_POINT ( 'NONE',  ( -8.999999999796672867, 20.89222690361001256, -44.57801334123718107 ) ) ;
#2547=CARTESIAN_POINT ( 'NONE',  ( 16.51284149387604216, 10.10369150398561544, -1.400000000000001910 ) ) ;
#2551=ADVANCED_FACE ( 'NONE', ( #28140 ), #6578, .F. ) ;
#2561=ORIENTED_EDGE ( 'NONE', *, *, #25280, .T. ) ;
#2562=FACE_OUTER_BOUND ( 'NONE', #19509, .T. ) ;
#2568=CARTESIAN_POINT ( 'NONE',  ( -13.92191802975810866, 20.99999999990301447, -67.88524365274894024 ) ) ;
#2571=VERTEX_POINT ( 'NONE', #451 ) ;
#2577=EDGE_CURVE ( 'NONE', #6914, #4001, #2636, .T. ) ;
#2580=CARTESIAN_POINT ( 'NONE',  ( 10.99999999979999998, 20.99999999999999645, -58.51619795479999908 ) ) ;
#2585=CARTESIAN_POINT ( 'NONE',  ( -11.59065746630000149, -24.20066399839999960, -1.404983722500002807 ) ) ;
#2586=CARTESIAN_POINT ( 'NONE',  ( -13.62111648911912631, 21.69999999994467998, -68.61136270525845759 ) ) ;
#2588=CARTESIAN_POINT ( 'NONE',  ( -10.69999999999999929, -24.59781467760000240, -30.21505918890000331 ) ) ;
#2595=FACE_OUTER_BOUND ( 'NONE', #17595, .T. ) ;
#2598=ORIENTED_EDGE ( 'NONE', *, *, #20579, .F. ) ;
#2608=DIRECTION ( 'NONE',  ( -0.4911057670060950398, 1.966019939440381643E-12, 0.8710999515631688839 ) ) ;
#2613=CARTESIAN_POINT ( 'NONE',  ( -10.69999999989999928, -45.00000000000000000, -7.274962170800002070 ) ) ;
#2614=B_SPLINE_CURVE_WITH_KNOTS ( 'NONE', 3,
 ( #13940, #27944, #7010, #20873 ),
 .UNSPECIFIED., .F., .F.,
 ( 4, 4 ),
 ( 0.000000000000000000, 1.000000000000000000 ),
 .UNSPECIFIED. ) ;
#2620=LINE ( 'NONE', #12064, #6727 ) ;
#2622=CARTESIAN_POINT ( 'NONE',  ( 12.55799324160000019, 20.99999999999999645, -55.95247857500000066 ) ) ;
#2626=CARTESIAN_POINT ( 'NONE',  ( -16.83342759579999637, 11.00000000000000355, -0.8000000000000020428 ) ) ;
#2627=CARTESIAN_POINT ( 'NONE',  ( 0.000000000000000000, 0.000000000000000000, 0.000000000000000000 ) ) ;
#2636=LINE ( 'NONE', #19783, #15101 ) ;
#2637=ORIENTED_EDGE ( 'NONE', *, *, #5282, .T. ) ;
#2653=CARTESIAN_POINT ( 'NONE',  ( 17.16657240490000191, -8.999999999699998199, -1.399999999999998579 ) ) ;
#2663=ORIENTED_EDGE ( 'NONE', *, *, #7083, .F. ) ;
#2665=CARTESIAN_POINT ( 'NONE',  ( 9.999999999970647480, -121.7869891337928010, -31.32664466927749558 ) ) ;
#2667=CARTESIAN_POINT ( 'NONE',  ( -10.00000000001340617, -31.36353147789393958, -21.95991608827594987 ) ) ;
#2678=EDGE_CURVE ( 'NONE', #6922, #23430, #23727, .T. ) ;
#2705=CARTESIAN_POINT ( 'NONE',  ( -10.69999999930000101, -120.5233595624000174, -31.26042064949999855 ) ) ;
#2719=ORIENTED_EDGE ( 'NONE', *, *, #9384, .T. ) ;
#2721=VECTOR ( 'NONE', #18193, 1000.000000000000000 ) ;
#2725=CARTESIAN_POINT ( 'NONE',  ( 8.999999999770000869, 20.99999999999999645, -53.60000000000000142 ) ) ;
#2726=ORIENTED_EDGE ( 'NONE', *, *, #8710, .F. ) ;
#2727=EDGE_CURVE ( 'NONE', #11580, #4569, #17252, .T. ) ;
#2734=CARTESIAN_POINT ( 'NONE',  ( 17.83928249680000278, 19.99999999999999645, -1.399999999299995856 ) ) ;
#2736=CARTESIAN_POINT ( 'NONE',  ( -10.69999999999999929, -24.87867968679999819, -26.27867968680000033 ) ) ;
#2737=CARTESIAN_POINT ( 'NONE',  ( -10.69999999999999929, -26.32120392050000035, -31.35200361700000471 ) ) ;
#2738=EDGE_CURVE ( 'NONE', #19721, #12957, #16948, .T. ) ;
#2745=VECTOR ( 'NONE', #24286, 1000.000000000000000 ) ;
#2758=FACE_OUTER_BOUND ( 'NONE', #6176, .T. ) ;
#2764=CARTESIAN_POINT ( 'NONE',  ( -15.73738422052369046, 11.17152825612159717, -1.400000000000001910 ) ) ;
#2775=CARTESIAN_POINT ( 'NONE',  ( -11.69999999989999928, -24.11120071670000087, -0.6999999999999992895 ) ) ;
#2790=ORIENTED_EDGE ( 'NONE', *, *, #7528, .F. ) ;
#2795=ORIENTED_EDGE ( 'NONE', *, *, #598, .F. ) ;
#2800=LINE ( 'NONE', #26711, #25375 ) ;
#2804=EDGE_LOOP ( 'NONE', ( #26260, #13279, #6185, #18214 ) ) ;
#2818=FACE_OUTER_BOUND ( 'NONE', #1439, .T. ) ;
#2822=CARTESIAN_POINT ( 'NONE',  ( 9.999999999970629716, -25.15635984103874279, -30.79900052789801990 ) ) ;
#2831=LINE ( 'NONE', #22041, #12259 ) ;
#2856=CARTESIAN_POINT ( 'NONE',  ( 10.69999999999658691, -24.37864083502648072, -26.88914305872019028 ) ) ;
#2859=DIRECTION ( 'NONE',  ( 0.000000000000000000, 0.000000000000000000, -1.000000000000000000 ) ) ;
#2860=VERTEX_POINT ( 'NONE', #10925 ) ;
#2862=ORIENTED_EDGE ( 'NONE', *, *, #13335, .T. ) ;
#2864=ORIENTED_EDGE ( 'NONE', *, *, #11367, .T. ) ;
#2865=LINE ( 'NONE', #9637, #8425 ) ;
#2867=EDGE_CURVE ( 'NONE', #19078, #22879, #28065, .T. ) ;
#2877=DIRECTION ( 'NONE',  ( -2.256480420250000087E-12, 0.000000000000000000, 1.000000000000000000 ) ) ;
#2881=CARTESIAN_POINT ( 'NONE',  ( -10.69999999989999928, -25.00000000000000000, -7.274962171499997687 ) ) ;
#2884=DIRECTION ( 'NONE',  ( -0.000000000000000000, 1.000000000000000000, -2.257145581549999994E-12 ) ) ;
#2886=CARTESIAN_POINT ( 'NONE',  ( -10.35000000039999968, -43.95328087560000085, -27.24755286599999948 ) ) ;
#2898=B_SPLINE_CURVE_WITH_KNOTS ( 'NONE', 3,
 ( #659, #19850, #5055, #14818, #10399, #194 ),
 .UNSPECIFIED., .F., .F.,
 ( 4, 2, 4 ),
 ( 0.000000000000000000, 0.5000000000000000000, 1.000000000000000000 ),
 .UNSPECIFIED. ) ;
#2902=CARTESIAN_POINT ( 'NONE',  ( -10.00000000021857183, -125.3357287863419458, -32.69504109500191902 ) ) ;
#2906=DIRECTION ( 'NONE',  ( 0.000000000000000000, -0.7071067811870488384, -0.7071067811860461960 ) ) ;
#2911=FACE_OUTER_BOUND ( 'NONE', #4815, .T. ) ;
#2925=EDGE_CURVE ( 'NONE', #17588, #2487, #13103, .T. ) ;
#2929=DIRECTION ( 'NONE',  ( -1.000000000000000000, 0.000000000000000000, -2.257144471330000330E-12 ) ) ;
#2935=DIRECTION ( 'NONE',  ( -1.180736691910036071E-13, -0.9986295347540310452, -0.05233595625330160483 ) ) ;
#2940=ORIENTED_EDGE ( 'NONE', *, *, #29110, .T. ) ;
#2943=CARTESIAN_POINT ( 'NONE',  ( -8.999999999299999942, 20.99999999999999645, -58.10000000000000142 ) ) ;
#2945=ORIENTED_EDGE ( 'NONE', *, *, #23441, .T. ) ;
#2966=CARTESIAN_POINT ( 'NONE',  ( 10.69999999999900986, -25.58868802767188555, -25.72767439674187528 ) ) ;
#2983=ORIENTED_EDGE ( 'NONE', *, *, #8777, .F. ) ;
#2994=CARTESIAN_POINT ( 'NONE',  ( -10.69999999995387263, -31.36675497167934523, -21.96261822718243550 ) ) ;
#3013=ORIENTED_EDGE ( 'NONE', *, *, #8927, .F. ) ;
#3015=ORIENTED_EDGE ( 'NONE', *, *, #26276, .T. ) ;
#3017=ORIENTED_EDGE ( 'NONE', *, *, #2577, .T. ) ;
#3026=CARTESIAN_POINT ( 'NONE',  ( -13.99999999969999820, 20.99999999999999645, -67.09999999999999432 ) ) ;
#3031=CARTESIAN_POINT ( 'NONE',  ( -16.83342759559999635, -9.000000000000001776, -0.6999999999999992895 ) ) ;
#3042=B_SPLINE_CURVE_WITH_KNOTS ( 'NONE', 5,
 ( #16125, #11870, #2287, #9346, #14086, #11567 ),
 .UNSPECIFIED., .F., .F.,
 ( 6, 6 ),
 ( 3.365644447000000206, 3.604192656009999940 ),
 .UNSPECIFIED. ) ;
#3050=ORIENTED_EDGE ( 'NONE', *, *, #8582, .F. ) ;
#3052=CARTESIAN_POINT ( 'NONE',  ( -10.69999999999999929, 19.99999999999999645, -42.39999999999999858 ) ) ;
#3059=EDGE_CURVE ( 'NONE', #5518, #24435, #31054, .T. ) ;
#3070=CARTESIAN_POINT ( 'NONE',  ( 9.999999999959999997, -25.00000000000000000, -26.16393202319999745 ) ) ;
#3076=CARTESIAN_POINT ( 'NONE',  ( -10.69999999997499351, -27.78484171395010804, -31.32227941850083397 ) ) ;
#3077=CARTESIAN_POINT ( 'NONE',  ( -10.69999999999999929, -30.00000000000000000, -28.40000000000000213 ) ) ;
#3082=ORIENTED_EDGE ( 'NONE', *, *, #15426, .T. ) ;
#3084=EDGE_CURVE ( 'NONE', #8540, #29211, #2419, .T. ) ;
#3092=ORIENTED_EDGE ( 'NONE', *, *, #28090, .T. ) ;
#3096=VECTOR ( 'NONE', #14509, 1000.000000000000000 ) ;
#3112=DIRECTION ( 'NONE',  ( 0.000000000000000000, -2.257145581549999994E-12, -1.000000000000000000 ) ) ;
#3114=CARTESIAN_POINT ( 'NONE',  ( -10.69999999999999929, -29.06671945329999929, -26.22544931050000017 ) ) ;
#3127=EDGE_LOOP ( 'NONE', ( #7404, #13071, #30892, #11102, #5046, #28053 ) ) ;
#3130=ORIENTED_EDGE ( 'NONE', *, *, #25626, .F. ) ;
#3139=CARTESIAN_POINT ( 'NONE',  ( 9.000000000029999114, 21.35000000040000145, -60.10000000000000142 ) ) ;
#3149=CARTESIAN_POINT ( 'NONE',  ( 11.69999999989999928, 19.99999999999999645, -2.399999999999999467 ) ) ;
#3157=EDGE_LOOP ( 'NONE', ( #25969, #6804, #3794, #5773 ) ) ;
#3160=ORIENTED_EDGE ( 'NONE', *, *, #845, .T. ) ;
#3163=ORIENTED_EDGE ( 'NONE', *, *, #27536, .F. ) ;
#3166=VERTEX_POINT ( 'NONE', #28993 ) ;
#3172=EDGE_CURVE ( 'NONE', #17104, #4684, #4618, .T. ) ;
#3176=CARTESIAN_POINT ( 'NONE',  ( 10.00000000070000183, 19.99999999999999645, -42.39999999999999858 ) ) ;
#3177=AXIS2_PLACEMENT_3D ( 'NONE', #3188, #24602, #22240 ) ;
#3178=ORIENTED_EDGE ( 'NONE', *, *, #23303, .T. ) ;
#3188=CARTESIAN_POINT ( 'NONE',  ( 13.99999999979999821, 20.99999999999999645, -51.10000000000000142 ) ) ;
#3192=EDGE_LOOP ( 'NONE', ( #5990, #23265, #16706, #1155 ) ) ;
#3199=ORIENTED_EDGE ( 'NONE', *, *, #9216, .F. ) ;
#3208=ORIENTED_EDGE ( 'NONE', *, *, #13945, .T. ) ;
#3212=CARTESIAN_POINT ( 'NONE',  ( 10.93704958068320643, 20.99999999999893419, -55.10811739799955689 ) ) ;
#3228=FACE_OUTER_BOUND ( 'NONE', #5978, .T. ) ;
#3238=CARTESIAN_POINT ( 'NONE',  ( 11.02757639490000052, -24.42656466549999905, -0.8308236885000014338 ) ) ;
#3240=CARTESIAN_POINT ( 'NONE',  ( -26.87372837451908580, 0.8705246371642829661, -0.6999999999999992895 ) ) ;
#3249=ADVANCED_FACE ( 'NONE', ( #10274 ), #19718, .F. ) ;
#3256=LINE ( 'NONE', #15849, #26592 ) ;
#3269=EDGE_CURVE ( 'NONE', #6914, #5911, #27101, .T. ) ;
#3275=AXIS2_PLACEMENT_3D ( 'NONE', #21118, #18744, #1300 ) ;
#3287=CARTESIAN_POINT ( 'NONE',  ( -9.999999999559999964, 21.00000000069999473, -60.10000000000000142 ) ) ;
#3295=CYLINDRICAL_SURFACE ( 'NONE', #11976, 1.000000000000000666 ) ;
#3308=EDGE_LOOP ( 'NONE', ( #8149, #14807, #2940, #19782 ) ) ;
#3322=FACE_OUTER_BOUND ( 'NONE', #15210, .T. ) ;
#3355=CARTESIAN_POINT ( 'NONE',  ( 12.12499559729999810, 20.99999999999999645, -55.73512174120000395 ) ) ;
#3374=CARTESIAN_POINT ( 'NONE',  ( 9.999999999961632469, -26.63382382736001119, -25.40000000000000568 ) ) ;
#3388=CARTESIAN_POINT ( 'NONE',  ( 11.16922184919999950, -24.52928866599999935, -1.544021042100003571 ) ) ;
#3392=ORIENTED_EDGE ( 'NONE', *, *, #13273, .T. ) ;
#3398=ORIENTED_EDGE ( 'NONE', *, *, #17876, .F. ) ;
#3402=CARTESIAN_POINT ( 'NONE',  ( -13.99999999969999820, 20.99999999999999645, -67.09999999999999432 ) ) ;
#3421=CARTESIAN_POINT ( 'NONE',  ( -10.69999999999940599, -28.79128384712763022, -25.96367195638410763 ) ) ;
#3423=LINE ( 'NONE', #7990, #20269 ) ;
#3429=CARTESIAN_POINT ( 'NONE',  ( 13.62125039882827160, 21.69999999994467998, -68.61132621245515395 ) ) ;
#3433=ORIENTED_EDGE ( 'NONE', *, *, #20089, .T. ) ;
#3435=CARTESIAN_POINT ( 'NONE',  ( -10.99999999969999998, 20.99999999999999645, -67.09999999999999432 ) ) ;
#3443=CARTESIAN_POINT ( 'NONE',  ( 10.69999999997499884, -27.78485145323708494, -31.32209366266220485 ) ) ;
#3445=EDGE_CURVE ( 'NONE', #23857, #30391, #9133, .T. ) ;
#3450=LINE ( 'NONE', #27072, #6193 ) ;
#3455=DIRECTION ( 'NONE',  ( -0.000000000000000000, 1.000000000000000000, -2.257145581549999994E-12 ) ) ;
#3468=ORIENTED_EDGE ( 'NONE', *, *, #19054, .T. ) ;
#3469=ORIENTED_EDGE ( 'NONE', *, *, #6228, .T. ) ;
#3488=CARTESIAN_POINT ( 'NONE',  ( 10.69999999999999929, -24.87867965640000278, -26.27867965640000136 ) ) ;
#3496=CARTESIAN_POINT ( 'NONE',  ( 10.00000000000000000, 20.99999999999999645, -62.10000000019999788 ) ) ;
#3503=ORIENTED_EDGE ( 'NONE', *, *, #17876, .T. ) ;
#3510=ORIENTED_EDGE ( 'NONE', *, *, #26633, .F. ) ;
#3518=DIRECTION ( 'NONE',  ( 0.000000000000000000, 0.000000000000000000, 1.000000000000000000 ) ) ;
#3530=CARTESIAN_POINT ( 'NONE',  ( -10.69999999999999929, -30.00000000000000000, -28.40000000000000213 ) ) ;
#3536=CARTESIAN_POINT ( 'NONE',  ( -10.93755790490000024, -24.69832375660000423, -1.748184584100004324 ) ) ;
#3538=ORIENTED_EDGE ( 'NONE', *, *, #15143, .F. ) ;
#3539=CARTESIAN_POINT ( 'NONE',  ( -10.69999999997431672, -28.51136270451570454, -31.02111648946564415 ) ) ;
#3541=B_SPLINE_CURVE_WITH_KNOTS ( 'NONE', 5,
 ( #1998, #28258, #1681, #13790, #21035, #11433, #30782, #9210, #18815, #9685, #2309, #3176 ),
 .UNSPECIFIED., .F., .F.,
 ( 6, 3, 3, 6 ),
 ( 1.118801870760000039, 1.395630273020000089, 2.093431498840000238, 2.237519762620000296 ),
 .UNSPECIFIED. ) ;
#3545=CARTESIAN_POINT ( 'NONE',  ( 11.32877539780000120, -24.28840541759999994, -0.7339858088999950958 ) ) ;
#3552=ORIENTED_EDGE ( 'NONE', *, *, #643, .T. ) ;
#3557=ORIENTED_EDGE ( 'NONE', *, *, #7133, .T. ) ;
#3564=CARTESIAN_POINT ( 'NONE',  ( 10.69999999999999929, -27.00000000000000000, -28.40000000000000213 ) ) ;
#3575=CARTESIAN_POINT ( 'NONE',  ( -17.63560569383767529, 11.76631802938718430, -1.400000000000001910 ) ) ;
#3580=VERTEX_POINT ( 'NONE', #5499 ) ;
#3583=FACE_OUTER_BOUND ( 'NONE', #5563, .T. ) ;
#3589=VERTEX_POINT ( 'NONE', #10850 ) ;
#3592=CYLINDRICAL_SURFACE ( 'NONE', #25544, 3.000000000000003997 ) ;
#3593=DIRECTION ( 'NONE',  ( 1.000000000000000000, -6.668066630619518976E-24, -2.257150022442225012E-12 ) ) ;
#3609=B_SPLINE_CURVE_WITH_KNOTS ( 'NONE', 3,
 ( #17171, #14827, #17477, #12446, #27084, #22065 ),
 .UNSPECIFIED., .F., .F.,
 ( 4, 2, 4 ),
 ( 0.000000000000000000, 0.5000000000000000000, 1.000000000000000000 ),
 .UNSPECIFIED. ) ;
#3615=EDGE_CURVE ( 'NONE', #15176, #14782, #18064, .T. ) ;
#3620=CARTESIAN_POINT ( 'NONE',  ( -10.46446609379999870, 20.99999999999999645, -54.63553390589999736 ) ) ;
#3631=ORIENTED_EDGE ( 'NONE', *, *, #21369, .T. ) ;
#3638=ADVANCED_FACE ( 'NONE', ( #13356 ), #4077, .F. ) ;
#3646=CARTESIAN_POINT ( 'NONE',  ( 10.69999999996564810, -42.68493023230600159, -27.18108142580972952 ) ) ;
#3648=LINE ( 'NONE', #3496, #5158 ) ;
#3680=EDGE_LOOP ( 'NONE', ( #20350, #14514, #29906, #25706 ) ) ;
#3693=CARTESIAN_POINT ( 'NONE',  ( -11.32877539260000077, -24.28840542069999842, -0.7339858089999984347 ) ) ;
#3695=VERTEX_POINT ( 'NONE', #4233 ) ;
#3697=VECTOR ( 'NONE', #8029, 1000.000000000000000 ) ;
#3700=ADVANCED_FACE ( 'NONE', ( #22803 ), #22650, .F. ) ;
#3707=LINE ( 'NONE', #745, #23520 ) ;
#3717=AXIS2_PLACEMENT_3D ( 'NONE', #5298, #2326, #14899 ) ;
#3731=CARTESIAN_POINT ( 'NONE',  ( -9.000000000000000000, -54.99999999999998579, -42.39999999999999858 ) ) ;
#3733=CARTESIAN_POINT ( 'NONE',  ( 9.999999999974161113, -24.60099947350716576, -30.24364016088963325 ) ) ;
#3748=CIRCLE ( 'NONE', #22283, 1.100000000390000787 ) ;
#3756=ORIENTED_EDGE ( 'NONE', *, *, #27121, .F. ) ;
#3777=DIRECTION ( 'NONE',  ( 0.000000000000000000, -2.259525899719999991E-12, -1.000000000000000000 ) ) ;
#3784=ORIENTED_EDGE ( 'NONE', *, *, #14756, .T. ) ;
#3791=CARTESIAN_POINT ( 'NONE',  ( 9.999999999957283947, -34.37899275736651106, -24.26894200096920073 ) ) ;
#3793=CARTESIAN_POINT ( 'NONE',  ( -26.57440914490000239, -3.469982507400000582, -0.6999999995999997005 ) ) ;
#3794=ORIENTED_EDGE ( 'NONE', *, *, #26245, .F. ) ;
#3802=CARTESIAN_POINT ( 'NONE',  ( -16.83342759579999637, -9.000000000000001776, -0.8000000000000020428 ) ) ;
#3813=CARTESIAN_POINT ( 'NONE',  ( 26.57440914490000239, -3.469982507400000582, -1.399999999999998579 ) ) ;
#3818=CARTESIAN_POINT ( 'NONE',  ( 9.999999999979998222, -127.2537437101000108, -34.36317024011000143 ) ) ;
#3822=CARTESIAN_POINT ( 'NONE',  ( 10.99289321870000080, -24.65831413369999936, -1.692893218799999877 ) ) ;
#3826=VERTEX_POINT ( 'NONE', #7211 ) ;
#3831=VERTEX_POINT ( 'NONE', #14302 ) ;
#3838=PLANE ( 'NONE',  #26526 ) ;
#3841=B_SPLINE_CURVE_WITH_KNOTS ( 'NONE', 3,
 ( #22458, #10807, #24966, #10499, #18021, #29687 ),
 .UNSPECIFIED., .F., .F.,
 ( 4, 2, 4 ),
 ( 0.000000000000000000, 0.5000000000000000000, 1.000000000000000000 ),
 .UNSPECIFIED. ) ;
#3849=CYLINDRICAL_SURFACE ( 'NONE', #5264, 3.000000000000000444 ) ;
#3858=CARTESIAN_POINT ( 'NONE',  ( -11.66358246699999945, -24.14124255240000139, -1.399999999999998579 ) ) ;
#3859=FACE_OUTER_BOUND ( 'NONE', #27204, .T. ) ;
#3870=CARTESIAN_POINT ( 'NONE',  ( -10.94971440929931106, -24.68950648801511605, -1.737779038943164212 ) ) ;
#3873=ORIENTED_EDGE ( 'NONE', *, *, #3445, .T. ) ;
#3878=ORIENTED_EDGE ( 'NONE', *, *, #10373, .F. ) ;
#3893=CARTESIAN_POINT ( 'NONE',  ( 0.000000000000000000, -50.49316738903675628, -44.10000000000000142 ) ) ;
#3911=VERTEX_POINT ( 'NONE', #17905 ) ;
#3914=ORIENTED_EDGE ( 'NONE', *, *, #8898, .T. ) ;
#3930=EDGE_CURVE ( 'NONE', #3949, #20395, #20436, .T. ) ;
#3931=CARTESIAN_POINT ( 'NONE',  ( -13.99999999969999820, 21.69999999929999390, -58.51619611000000276 ) ) ;
#3944=LINE ( 'NONE', #30541, #7209 ) ;
#3949=VERTEX_POINT ( 'NONE', #11157 ) ;
#3973=VECTOR ( 'NONE', #20105, 1000.000000000000000 ) ;
#3976=DIRECTION ( 'NONE',  ( -2.257102469710000208E-12, 0.000000000000000000, 1.000000000000000000 ) ) ;
#3977=EDGE_LOOP ( 'NONE', ( #24352, #599, #11382, #10107 ) ) ;
#3979=DIRECTION ( 'NONE',  ( 1.000000000000000000, 0.000000000000000000, 0.000000000000000000 ) ) ;
#3982=ORIENTED_EDGE ( 'NONE', *, *, #15869, .T. ) ;
#3984=VECTOR ( 'NONE', #20531, 1000.000000000000000 ) ;
#3998=CARTESIAN_POINT ( 'NONE',  ( -10.99289321870000080, -2.500000000000002220, -1.692893218799999877 ) ) ;
#3999=CARTESIAN_POINT ( 'NONE',  ( 9.000000000000000000, -55.00000000000001421, -42.39999999999999858 ) ) ;
#4001=VERTEX_POINT ( 'NONE', #2344 ) ;
#4002=CARTESIAN_POINT ( 'NONE',  ( -26.38145030669853952, 5.195434873298933276, -1.399999999999998579 ) ) ;
#4009=CARTESIAN_POINT ( 'NONE',  ( 17.83928249670000099, 20.00000000010000178, -0.6999999999999992895 ) ) ;
#4022=B_SPLINE_CURVE_WITH_KNOTS ( 'NONE', 3,
 ( #4404, #6297, #14007, #13690 ),
 .UNSPECIFIED., .F., .F.,
 ( 4, 4 ),
 ( 0.000000000000000000, 1.000000000000000000 ),
 .UNSPECIFIED. ) ;
#4044=DIRECTION ( 'NONE',  ( 3.092054264588954770E-24, -1.000000000000000000, 2.257145581552149937E-12 ) ) ;
#4049=CARTESIAN_POINT ( 'NONE',  ( -9.707106781189999367, -130.0000000000000000, -43.10710678118599759 ) ) ;
#4050=DIRECTION ( 'NONE',  ( 1.000000000000000000, 0.000000000000000000, 0.000000000000000000 ) ) ;
#4061=B_SPLINE_CURVE_WITH_KNOTS ( 'NONE', 3,
 ( #5073, #21609, #4606, #19087, #12001, #24123 ),
 .UNSPECIFIED., .F., .F.,
 ( 4, 2, 4 ),
 ( 0.000000000000000000, 0.5000000000000000000, 1.000000000000000000 ),
 .UNSPECIFIED. ) ;
#4070=ORIENTED_EDGE ( 'NONE', *, *, #10913, .F. ) ;
#4072=EDGE_CURVE ( 'NONE', #3826, #21635, #28454, .T. ) ;
#4074=FACE_BOUND ( 'NONE', #26241, .T. ) ;
#4077=PLANE ( 'NONE',  #25661 ) ;
#4082=DIRECTION ( 'NONE',  ( 0.5882352941176968164, 0.000000000000000000, -0.8086898285215826654 ) ) ;
#4086=CARTESIAN_POINT ( 'NONE',  ( 4.175165894169885483, -50.49316738903675628, -63.39999999999999858 ) ) ;
#4091=CYLINDRICAL_SURFACE ( 'NONE', #11230, 1.099999999999999201 ) ;
#4093=DIRECTION ( 'NONE',  ( 0.000000000000000000, 0.9986295347545772749, 0.05233595624287791515 ) ) ;
#4108=CARTESIAN_POINT ( 'NONE',  ( -10.69999999999999929, -25.00000000000000000, -26.16393202249999916 ) ) ;
#4148=ORIENTED_EDGE ( 'NONE', *, *, #5761, .F. ) ;
#4157=VECTOR ( 'NONE', #27316, 1000.000000000000000 ) ;
#4164=CIRCLE ( 'NONE', #26265, 1.700000000000000178 ) ;
#4166=CARTESIAN_POINT ( 'NONE',  ( 26.38279268013727474, 5.187539658929759767, -1.399999999999998579 ) ) ;
#4167=DIRECTION ( 'NONE',  ( -1.595945597898660305E-12, -0.7071067811865475727, -0.7071067811865475727 ) ) ;
#4176=EDGE_CURVE ( 'NONE', #68, #7509, #22002, .T. ) ;
#4181=CARTESIAN_POINT ( 'NONE',  ( -10.00000000020644997, -24.37864083493787604, -26.88914305888777534 ) ) ;
#4182=AXIS2_PLACEMENT_3D ( 'NONE', #24679, #3112, #12096 ) ;
#4190=FACE_OUTER_BOUND ( 'NONE', #1859, .T. ) ;
#4191=CARTESIAN_POINT ( 'NONE',  ( 10.00000000060000005, -25.00000000000000000, -7.274962170899998526 ) ) ;
#4200=EDGE_CURVE ( 'NONE', #7630, #30907, #2800, .T. ) ;
#4204=DIRECTION ( 'NONE',  ( 0.000000000000000000, 1.000000000000000000, 0.000000000000000000 ) ) ;
#4208=EDGE_CURVE ( 'NONE', #17102, #2571, #24337, .T. ) ;
#4209=DIRECTION ( 'NONE',  ( 0.000000000000000000, -1.000000000000000000, 2.257145581549999994E-12 ) ) ;
#4223=VECTOR ( 'NONE', #10793, 1000.000000000000000 ) ;
#4233=CARTESIAN_POINT ( 'NONE',  ( 4.175165894169885483, -50.49316738903675628, -43.39999999999999858 ) ) ;
#4263=SURFACE_STYLE_USAGE ( .BOTH. , #27548 ) ;
#4267=VECTOR ( 'NONE', #11990, 1000.000000000000000 ) ;
#4276=CARTESIAN_POINT ( 'NONE',  ( -8.999999999710000864, 18.79791847199999921, -43.89791847198399921 ) ) ;
#4278=B_SPLINE_CURVE_WITH_KNOTS ( 'NONE', 3,
 ( #11008, #27672, #27373, #5812, #13359, #27991 ),
 .UNSPECIFIED., .F., .F.,
 ( 4, 2, 4 ),
 ( 0.000000000000000000, 0.5000000000000000000, 1.000000000000000000 ),
 .UNSPECIFIED. ) ;
#4283=ADVANCED_FACE ( 'NONE', ( #5920 ), #1216, .T. ) ;
#4292=CARTESIAN_POINT ( 'NONE',  ( -10.00000000033029224, -25.95491900952040965, -13.51082902143504860 ) ) ;
#4296=EDGE_LOOP ( 'NONE', ( #11783, #29685, #16860, #15548 ) ) ;
#4303=DIRECTION ( 'NONE',  ( 0.000000000000000000, -1.000000000000000000, 0.000000000000000000 ) ) ;
#4310=MECHANICAL_DESIGN_GEOMETRIC_PRESENTATION_REPRESENTATION('',(#14357),#26896);
#4313=CYLINDRICAL_SURFACE ( 'NONE', #6886, 3.000000000000005329 ) ;
#4323=ORIENTED_EDGE ( 'NONE', *, *, #10749, .T. ) ;
#4324=FACE_OUTER_BOUND ( 'NONE', #28948, .T. ) ;
#4332=CARTESIAN_POINT ( 'NONE',  ( -10.00000000052381921, -26.21475634692178858, -31.32191803000645436 ) ) ;
#4334=ADVANCED_FACE ( 'NONE', ( #18660 ), #6702, .F. ) ;
#4341=ORIENTED_EDGE ( 'NONE', *, *, #1965, .T. ) ;
#4348=CARTESIAN_POINT ( 'NONE',  ( -16.83342759559999635, 11.00000000000000355, -0.6999999999999992895 ) ) ;
#4351=DIRECTION ( 'NONE',  ( -1.000000000000000000, 0.000000000000000000, 0.000000000000000000 ) ) ;
#4354=DIRECTION ( 'NONE',  ( 2.256992747040000044E-12, -0.000000000000000000, -1.000000000000000000 ) ) ;
#4359=CARTESIAN_POINT ( 'NONE',  ( 11.69999999989999928, -24.11120071670000087, -0.6999999995999997005 ) ) ;
#4369=CARTESIAN_POINT ( 'NONE',  ( -13.88917081232333395, 20.99999999996956745, -57.58165165637253580 ) ) ;
#4372=EDGE_CURVE ( 'NONE', #409, #15021, #22825, .T. ) ;
#4376=ORIENTED_EDGE ( 'NONE', *, *, #22972, .T. ) ;
#4404=CARTESIAN_POINT ( 'NONE',  ( -9.707106781189999367, 19.99999999999999645, -43.10710678118599759 ) ) ;
#4409=VECTOR ( 'NONE', #12848, 1000.000000000000000 ) ;
#4424=DIRECTION ( 'NONE',  ( 0.000000000000000000, 0.000000000000000000, -1.000000000000000000 ) ) ;
#4428=FACE_OUTER_BOUND ( 'NONE', #27819, .T. ) ;
#4430=CYLINDRICAL_SURFACE ( 'NONE', #30067, 2.999999999999998668 ) ;
#4455=CARTESIAN_POINT ( 'NONE',  ( -10.00000000000000000, 20.99999999990000887, -70.10000000019999788 ) ) ;
#4467=SURFACE_SIDE_STYLE ('',( #11547 ) ) ;
#4473=CARTESIAN_POINT ( 'NONE',  ( 11.14649462760000098, -24.37257236010000128, -0.7852065437999946607 ) ) ;
#4482=CARTESIAN_POINT ( 'NONE',  ( 11.30445670279999959, -24.42656466549999905, -1.476955110899999646 ) ) ;
#4485=CARTESIAN_POINT ( 'NONE',  ( 12.70717268325767968, 20.99999999997303135, -56.04772914979974985 ) ) ;
#4488=CARTESIAN_POINT ( 'NONE',  ( -10.69999999999999929, -24.73190191370000335, -30.37453596639999986 ) ) ;
#4492=CARTESIAN_POINT ( 'NONE',  ( 10.69999999999999929, -24.87867965640000278, -30.52132034359999935 ) ) ;
#4493=DIRECTION ( 'NONE',  ( 0.000000000000000000, 1.000000000000000000, 0.000000000000000000 ) ) ;
#4495=ORIENTED_EDGE ( 'NONE', *, *, #24886, .F. ) ;
#4496=DIRECTION ( 'NONE',  ( -1.000000000000000000, 0.000000000000000000, 0.000000000000000000 ) ) ;
#4500=ORIENTED_EDGE ( 'NONE', *, *, #31039, .T. ) ;
#4512=CARTESIAN_POINT ( 'NONE',  ( -10.69999999993478923, -25.95311069648830937, -13.50784318091593406 ) ) ;
#4519=CARTESIAN_POINT ( 'NONE',  ( -10.99289321870000080, 19.99999999999999645, -1.692893218799999877 ) ) ;
#4531=ORIENTED_EDGE ( 'NONE', *, *, #16998, .T. ) ;
#4546=VERTEX_POINT ( 'NONE', #12658 ) ;
#4547=DIRECTION ( 'NONE',  ( 0.000000000000000000, -2.257145581549999994E-12, -1.000000000000000000 ) ) ;
#4548=AXIS2_PLACEMENT_3D ( 'NONE', #16178, #1866, #25790 ) ;
#4558=LINE ( 'NONE', #23766, #2255 ) ;
#4560=FACE_OUTER_BOUND ( 'NONE', #29563, .T. ) ;
#4563=CARTESIAN_POINT ( 'NONE',  ( 10.87708494459999997, 19.99999999999999645, -1.827228080399999399 ) ) ;
#4569=VERTEX_POINT ( 'NONE', #5883 ) ;
#4571=ORIENTED_EDGE ( 'NONE', *, *, #9036, .T. ) ;
#4577=DIRECTION ( 'NONE',  ( -1.020425574104003999E-15, 0.000000000000000000, -1.000000000000000000 ) ) ;
#4579=DIRECTION ( 'NONE',  ( 2.612942924549014782E-24, -1.000000000000000000, 2.257145581549775024E-12 ) ) ;
#4591=CARTESIAN_POINT ( 'NONE',  ( -25.66631072470286412, -7.791349473814749516, -1.399999999999998579 ) ) ;
#4592=ORIENTED_EDGE ( 'NONE', *, *, #10403, .F. ) ;
#4597=ORIENTED_EDGE ( 'NONE', *, *, #27196, .F. ) ;
#4600=EDGE_LOOP ( 'NONE', ( #8740, #17630 ) ) ;
#4606=CARTESIAN_POINT ( 'NONE',  ( 9.999999999958941288, -28.46561708990600081, -25.75493691892357617 ) ) ;
#4608=EDGE_CURVE ( 'NONE', #25001, #9747, #10070, .T. ) ;
#4610=ORIENTED_EDGE ( 'NONE', *, *, #26734, .F. ) ;
#4612=DIRECTION ( 'NONE',  ( 1.180736691910036071E-13, -0.9986295347540310452, -0.05233595625330160483 ) ) ;
#4618=B_SPLINE_CURVE_WITH_KNOTS ( 'NONE', 3,
 ( #4925, #5078, #7440, #29144 ),
 .UNSPECIFIED., .F., .F.,
 ( 4, 4 ),
 ( 0.000000000000000000, 1.000000000000000000 ),
 .UNSPECIFIED. ) ;
#4625=CARTESIAN_POINT ( 'NONE',  ( -10.69999999999999929, -127.6591310166000142, -34.79037178941999997 ) ) ;
#4634=VECTOR ( 'NONE', #26799, 1000.000000000000000 ) ;
#4651=AXIS2_PLACEMENT_3D ( 'NONE', #17236, #27301, #5744 ) ;
#4657=CARTESIAN_POINT ( 'NONE',  ( -10.69999999992642259, -25.11960129118233809, -9.802886333996065460 ) ) ;
#4665=CARTESIAN_POINT ( 'NONE',  ( 8.999999999770000869, 21.35000000040000145, -64.10000000000000853 ) ) ;
#4673=CARTESIAN_POINT ( 'NONE',  ( 13.88949358619128027, 20.99999999996956745, -57.58230229939546518 ) ) ;
#4675=ADVANCED_BREP_SHAPE_REPRESENTATION ( '', ( #10459, #17722 ), #10330 ) ;
#4684=VERTEX_POINT ( 'NONE', #1811 ) ;
#4691=CARTESIAN_POINT ( 'NONE',  ( 9.291972389019999667, 19.99999999999999645, -43.36399323947500051 ) ) ;
#4700=DIRECTION ( 'NONE',  ( 1.000000000000000000, 0.000000000000000000, 0.000000000000000000 ) ) ;
#4704=EDGE_CURVE ( 'NONE', #5374, #28074, #20846, .T. ) ;
#4714=VECTOR ( 'NONE', #15692, 1000.000000000000000 ) ;
#4719=CARTESIAN_POINT ( 'NONE',  ( -11.69999999989999928, 19.99999999999999645, -0.6999999999999992895 ) ) ;
#4722=ORIENTED_EDGE ( 'NONE', *, *, #12979, .F. ) ;
#4723=LINE ( 'NONE', #30109, #30351 ) ;
#4732=ORIENTED_EDGE ( 'NONE', *, *, #8956, .T. ) ;
#4744=CIRCLE ( 'NONE', #12775, 1.700000000000000178 ) ;
#4751=B_SPLINE_CURVE_WITH_KNOTS ( 'NONE', 5,
 ( #22984, #17923, #20303, #18242, #17775, #22824, #20458, #10407, #27233, #22372, #24722, #15428 ),
 .UNSPECIFIED., .F., .F.,
 ( 6, 3, 3, 6 ),
 ( 0.000000000000000000, 1.357884647149999902, 2.715789077610000213, 3.784579751189999897 ),
 .UNSPECIFIED. ) ;
#4758=LINE ( 'NONE', #23336, #15758 ) ;
#4764=ORIENTED_EDGE ( 'NONE', *, *, #9621, .T. ) ;
#4779=ORIENTED_EDGE ( 'NONE', *, *, #10749, .F. ) ;
#4780=ADVANCED_FACE ( 'NONE', ( #25417 ), #3849, .F. ) ;
#4781=FACE_OUTER_BOUND ( 'NONE', #28752, .T. ) ;
#4784=VECTOR ( 'NONE', #11927, 1000.000000000000000 ) ;
#4788=CARTESIAN_POINT ( 'NONE',  ( 11.51411768920000078, -24.20066399999999973, -0.7084723288000027708 ) ) ;
#4790=PLANE ( 'NONE',  #9276 ) ;
#4800=DIRECTION ( 'NONE',  ( 0.000000000000000000, -1.000000000000000000, 0.000000000000000000 ) ) ;
#4806=CARTESIAN_POINT ( 'NONE',  ( -9.000000000000000000, 20.99999999990000887, -67.10000000019999788 ) ) ;
#4807=CIRCLE ( 'NONE', #2295, 3.999999999669999973 ) ;
#4811=CARTESIAN_POINT ( 'NONE',  ( 10.69999999997017248, -24.07790633733921126, -29.18485145324821772 ) ) ;
#4815=EDGE_LOOP ( 'NONE', ( #5174, #19426, #23159, #12950 ) ) ;
#4817=DIRECTION ( 'NONE',  ( 0.8775825618903718706, -0.4794255386042047262, 0.000000000000000000 ) ) ;
#4822=ADVANCED_FACE ( 'NONE', ( #7599, #2425, #31061 ), #4790, .T. ) ;
#4824=CARTESIAN_POINT ( 'NONE',  ( 9.999999999959999997, -29.30501631460000311, -26.47986984960000001 ) ) ;
#4826=CARTESIAN_POINT ( 'NONE',  ( -17.83928249649999742, 19.99999999999999645, -1.399999999999998579 ) ) ;
#4835=CARTESIAN_POINT ( 'NONE',  ( 13.99999999979999821, 20.99999999999999645, -67.09999999999999432 ) ) ;
#4838=FACE_OUTER_BOUND ( 'NONE', #30028, .T. ) ;
#4841=CARTESIAN_POINT ( 'NONE',  ( 10.69999999930000101, -29.06671945340000107, -26.22544931050000017 ) ) ;
#4862=ADVANCED_FACE ( 'NONE', ( #2277 ), #5084, .F. ) ;
#4865=CARTESIAN_POINT ( 'NONE',  ( -9.130136616382021231, 21.00000000000501643, -52.40873942185827161 ) ) ;
#4867=PLANE ( 'NONE',  #17666 ) ;
#4869=CARTESIAN_POINT ( 'NONE',  ( 10.69999999999999929, -27.00000000000000000, -25.39999999999999858 ) ) ;
#4873=EDGE_LOOP ( 'NONE', ( #27142, #1559, #15542, #15942 ) ) ;
#4875=DIRECTION ( 'NONE',  ( 0.000000000000000000, -1.000000000000000000, 0.000000000000000000 ) ) ;
#4881=AXIS2_PLACEMENT_3D ( 'NONE', #21799, #26371, #7775 ) ;
#4885=EDGE_CURVE ( 'NONE', #11584, #29101, #4807, .T. ) ;
#4889=CARTESIAN_POINT ( 'NONE',  ( 9.999999999968435915, -29.93910046810518111, -27.70552897400620296 ) ) ;
#4912=ORIENTED_EDGE ( 'NONE', *, *, #15869, .F. ) ;
#4916=ORIENTED_EDGE ( 'NONE', *, *, #15918, .T. ) ;
#4918=EDGE_LOOP ( 'NONE', ( #22766, #19058, #4779, #4993 ) ) ;
#4920=VECTOR ( 'NONE', #8697, 1000.000000000000000 ) ;
#4922=CARTESIAN_POINT ( 'NONE',  ( -10.00000000070000183, 19.99999999999999645, -22.39999999999999858 ) ) ;
#4925=CARTESIAN_POINT ( 'NONE',  ( -12.77820031409999935, 21.69999999929999390, -56.09999999999999432 ) ) ;
#4940=DIRECTION ( 'NONE',  ( -2.254051133279049930E-12, -0.05233595624287792208, 0.9986295347545773859 ) ) ;
#4950=EDGE_CURVE ( 'NONE', #14341, #26977, #30438, .T. ) ;
#4952=B_SPLINE_CURVE_WITH_KNOTS ( 'NONE', 3,
 ( #21626, #21777, #2429, #9972, #78, #26495 ),
 .UNSPECIFIED., .F., .F.,
 ( 4, 2, 4 ),
 ( 0.000000000000000000, 0.5000000000000000000, 1.000000000000000000 ),
 .UNSPECIFIED. ) ;
#4968=DIRECTION ( 'NONE',  ( 1.180736691910036071E-13, -0.9986295347540310452, -0.05233595625330160483 ) ) ;
#4970=VERTEX_POINT ( 'NONE', #20177 ) ;
#4974=DIRECTION ( 'NONE',  ( 0.000000000000000000, -1.000000000000000000, 0.000000000000000000 ) ) ;
#4975=FACE_OUTER_BOUND ( 'NONE', #18975, .T. ) ;
#4993=ORIENTED_EDGE ( 'NONE', *, *, #16546, .F. ) ;
#4999=EDGE_CURVE ( 'NONE', #30538, #14788, #17800, .T. ) ;
#5007=ORIENTED_EDGE ( 'NONE', *, *, #26382, .F. ) ;
#5020=DIRECTION ( 'NONE',  ( 2.966217977826874882E-25, -1.000000000000000000, 2.257145581549900232E-12 ) ) ;
#5024=VERTEX_POINT ( 'NONE', #15604 ) ;
#5027=ORIENTED_EDGE ( 'NONE', *, *, #5785, .F. ) ;
#5030=ORIENTED_EDGE ( 'NONE', *, *, #5785, .T. ) ;
#5046=ORIENTED_EDGE ( 'NONE', *, *, #18737, .F. ) ;
#5049=FACE_OUTER_BOUND ( 'NONE', #5107, .T. ) ;
#5051=CARTESIAN_POINT ( 'NONE',  ( -10.69999999989999928, -25.00000000000000000, -14.32712675259999813 ) ) ;
#5055=CARTESIAN_POINT ( 'NONE',  ( 9.999999999966631137, -24.07798516454965920, -27.61520910695477227 ) ) ;
#5062=CARTESIAN_POINT ( 'NONE',  ( 10.69999999999999929, -24.87867965640000278, -26.27867965640000136 ) ) ;
#5069=EDGE_LOOP ( 'NONE', ( #16550, #29713, #5334, #30585 ) ) ;
#5070=VERTEX_POINT ( 'NONE', #3813 ) ;
#5073=CARTESIAN_POINT ( 'NONE',  ( 9.999999999959999997, -29.06670649020000141, -26.22546295170000263 ) ) ;
#5076=ORIENTED_EDGE ( 'NONE', *, *, #18040, .T. ) ;
#5078=CARTESIAN_POINT ( 'NONE',  ( -13.15526697139052814, 21.69999999929937928, -56.37750232931335148 ) ) ;
#5084=PLANE ( 'NONE',  #8805 ) ;
#5086=LINE ( 'NONE', #27110, #4634 ) ;
#5087=CARTESIAN_POINT ( 'NONE',  ( -10.69999999999999929, -36.62914859500000375, -26.86371135770000151 ) ) ;
#5091=CARTESIAN_POINT ( 'NONE',  ( -10.99289321870000080, -24.65831413349999934, -1.692893218799999877 ) ) ;
#5092=CARTESIAN_POINT ( 'NONE',  ( -14.00000000000000178, 21.69999999994719886, -67.49453140416896701 ) ) ;
#5099=EDGE_LOOP ( 'NONE', ( #19272, #3557 ) ) ;
#5107=EDGE_LOOP ( 'NONE', ( #25076, #5491, #8819, #22333, #25699, #7087, #29094, #26436 ) ) ;
#5114=CARTESIAN_POINT ( 'NONE',  ( -10.69999999999999929, -24.78546131799999941, -26.37189816670000297 ) ) ;
#5119=EDGE_CURVE ( 'NONE', #15021, #6694, #22852, .T. ) ;
#5123=CARTESIAN_POINT ( 'NONE',  ( 10.00000000070000183, -27.00000000000000000, -25.39999999999999858 ) ) ;
#5129=CARTESIAN_POINT ( 'NONE',  ( 9.129724771679379458, 21.69999999998125872, -52.40755693945581584 ) ) ;
#5145=EDGE_CURVE ( 'NONE', #20583, #14645, #27660, .T. ) ;
#5150=DIRECTION ( 'NONE',  ( -0.000000000000000000, 1.000000000000000000, -2.257145581549999994E-12 ) ) ;
#5153=CARTESIAN_POINT ( 'NONE',  ( -10.69999999999999929, -130.0000000000000000, -42.39999999999999858 ) ) ;
#5154=EDGE_CURVE ( 'NONE', #18993, #29098, #13321, .T. ) ;
#5156=CARTESIAN_POINT ( 'NONE',  ( 12.77819780750000156, 21.69999999929999390, -56.09999999999999432 ) ) ;
#5158=VECTOR ( 'NONE', #13245, 1000.000000000000000 ) ;
#5165=CARTESIAN_POINT ( 'NONE',  ( -10.69999999930000101, -24.00000000000000000, -28.40000000000000213 ) ) ;
#5168=CARTESIAN_POINT ( 'NONE',  ( 8.999999999770000869, 21.21773977379998755, -43.89049139494199636 ) ) ;
#5171=VERTEX_POINT ( 'NONE', #23011 ) ;
#5174=ORIENTED_EDGE ( 'NONE', *, *, #7196, .F. ) ;
#5189=FACE_OUTER_BOUND ( 'NONE', #21412, .T. ) ;
#5199=VECTOR ( 'NONE', #14128, 1000.000000000000000 ) ;
#5202=VECTOR ( 'NONE', #26615, 1000.000000000000000 ) ;
#5203=CIRCLE ( 'NONE', #7232, 1.100000000390000787 ) ;
#5212=ORIENTED_EDGE ( 'NONE', *, *, #10971, .T. ) ;
#5216=ORIENTED_EDGE ( 'NONE', *, *, #14280, .F. ) ;
#5220=ADVANCED_FACE ( 'NONE', ( #9141 ), #6791, .T. ) ;
#5223=VECTOR ( 'NONE', #10015, 1000.000000000000000 ) ;
#5233=CARTESIAN_POINT ( 'NONE',  ( -13.62135916515834388, 20.99999999990137312, -68.61085694035826066 ) ) ;
#5234=CARTESIAN_POINT ( 'NONE',  ( 10.69999999994746887, -28.83990707537207143, -19.12610387680327761 ) ) ;
#5235=ORIENTED_EDGE ( 'NONE', *, *, #17787, .F. ) ;
#5237=CARTESIAN_POINT ( 'NONE',  ( 13.12132034340000075, 20.99999999990000887, -69.22132034359999864 ) ) ;
#5245=CARTESIAN_POINT ( 'NONE',  ( 12.77819780750000156, 20.99999999999999645, -56.09999999999999432 ) ) ;
#5250=PLANE ( 'NONE',  #30366 ) ;
#5251=AXIS2_PLACEMENT_3D ( 'NONE', #18600, #13725, #14047 ) ;
#5260=ORIENTED_EDGE ( 'NONE', *, *, #4372, .F. ) ;
#5264=AXIS2_PLACEMENT_3D ( 'NONE', #13438, #23054, #11090 ) ;
#5265=CARTESIAN_POINT ( 'NONE',  ( -9.999999999979998222, -127.2536115484999897, -34.36329565063000047 ) ) ;
#5268=CYLINDRICAL_SURFACE ( 'NONE', #23984, 0.9999999999999988898 ) ;
#5281=ADVANCED_FACE ( 'NONE', ( #5049 ), #28500, .F. ) ;
#5282=EDGE_CURVE ( 'NONE', #11580, #23901, #2390, .T. ) ;
#5298=CARTESIAN_POINT ( 'NONE',  ( 10.69999999989999928, -45.00000000000000000, -7.274962170899998526 ) ) ;
#5306=CARTESIAN_POINT ( 'NONE',  ( -10.00000000000000000, 20.99999999999999645, -62.10000000019999788 ) ) ;
#5313=CARTESIAN_POINT ( 'NONE',  ( 17.56757767936423775, 12.03437313983793011, -1.400000000000002132 ) ) ;
#5314=CARTESIAN_POINT ( 'NONE',  ( 10.69999999999999929, -29.30501631380000305, -26.47986985000000004 ) ) ;
#5317=ORIENTED_EDGE ( 'NONE', *, *, #6110, .F. ) ;
#5328=DIRECTION ( 'NONE',  ( 2.257144471330000330E-12, -0.000000000000000000, -1.000000000000000000 ) ) ;
#5332=ORIENTED_EDGE ( 'NONE', *, *, #22076, .T. ) ;
#5334=ORIENTED_EDGE ( 'NONE', *, *, #19066, .T. ) ;
#5340=SHAPE_DEFINITION_REPRESENTATION ( #11415, #25228 ) ;
#5341=ORIENTED_EDGE ( 'NONE', *, *, #16783, .T. ) ;
#5350=CARTESIAN_POINT ( 'NONE',  ( 13.12132034340000075, 21.69999999990000106, -69.22132034359999864 ) ) ;
#5369=DIRECTION ( 'NONE',  ( 0.000000000000000000, 0.000000000000000000, -1.000000000000000000 ) ) ;
#5374=VERTEX_POINT ( 'NONE', #19216 ) ;
#5382=CARTESIAN_POINT ( 'NONE',  ( -10.69999999999999929, -24.90229870320000316, -26.25506064210000190 ) ) ;
#5383=EDGE_LOOP ( 'NONE', ( #28747, #11348, #16725, #28288 ) ) ;
#5394=DIRECTION ( 'NONE',  ( 1.000000000000000000, -0.000000000000000000, -2.257150022439999944E-12 ) ) ;
#5395=LINE ( 'NONE', #17354, #2745 ) ;
#5396=CARTESIAN_POINT ( 'NONE',  ( 10.00000000070000183, 19.99999999999999645, -22.39999999999999858 ) ) ;
#5398=CARTESIAN_POINT ( 'NONE',  ( -10.69999999999999929, -24.97190126590000148, -30.61453681870000310 ) ) ;
#5408=AXIS2_PLACEMENT_3D ( 'NONE', #17904, #3593, #15404 ) ;
#5412=EDGE_LOOP ( 'NONE', ( #16250, #14062, #10377, #22637 ) ) ;
#5419=DIRECTION ( 'NONE',  ( 1.635844237846128888E-12, 0.6889064844606307414, -0.7248502298186121351 ) ) ;
#5422=CARTESIAN_POINT ( 'NONE',  ( -11.69999999989999928, -2.500000000000002220, -1.399999999999998579 ) ) ;
#5424=ORIENTED_EDGE ( 'NONE', *, *, #3059, .F. ) ;
#5430=CARTESIAN_POINT ( 'NONE',  ( 8.999999999770000869, 21.70000000000000284, -53.60000000000000142 ) ) ;
#5431=LINE ( 'NONE', #10008, #1236 ) ;
#5445=ORIENTED_EDGE ( 'NONE', *, *, #25645, .T. ) ;
#5447=CARTESIAN_POINT ( 'NONE',  ( 11.63809019220000174, -24.14124255329999968, -0.6999999999999992895 ) ) ;
#5455=AXIS2_PLACEMENT_3D ( 'NONE', #22550, #29464, #20024 ) ;
#5460=FACE_OUTER_BOUND ( 'NONE', #20828, .T. ) ;
#5462=CARTESIAN_POINT ( 'NONE',  ( 10.69999999996534967, -29.70167663135993408, -27.04935189346707602 ) ) ;
#5466=DIRECTION ( 'NONE',  ( -1.181300906760215537E-13, 0.9986295347541825906, 0.05233595625040957794 ) ) ;
#5471=DIRECTION ( 'NONE',  ( 0.000000000000000000, -1.000000000000000000, 0.000000000000000000 ) ) ;
#5474=CARTESIAN_POINT ( 'NONE',  ( 9.999999999959999997, -25.00000000000000000, -26.16393202319999745 ) ) ;
#5484=EDGE_CURVE ( 'NONE', #18608, #26133, #19843, .T. ) ;
#5486=DIRECTION ( 'NONE',  ( 0.000000000000000000, -1.000000000000000000, 0.000000000000000000 ) ) ;
#5491=ORIENTED_EDGE ( 'NONE', *, *, #24846, .F. ) ;
#5492=ORIENTED_EDGE ( 'NONE', *, *, #5484, .F. ) ;
#5497=VECTOR ( 'NONE', #17865, 1000.000000000000000 ) ;
#5498=VECTOR ( 'NONE', #7890, 1000.000000000000000 ) ;
#5499=CARTESIAN_POINT ( 'NONE',  ( 9.707106781189999367, 19.99999999999999645, -43.10710678118599759 ) ) ;
#5502=CARTESIAN_POINT ( 'NONE',  ( -10.00000000000000000, -130.0000000000000000, -41.24671599790000442 ) ) ;
#5514=B_SPLINE_CURVE_WITH_KNOTS ( 'NONE', 5,
 ( #7755, #24754, #2737, #391, #12334, #19575, #17357, #5398, #22241 ),
 .UNSPECIFIED., .F., .F.,
 ( 6, 3, 6 ),
 ( 0.000000000000000000, 2.405120303699999962, 3.339306057409999973 ),
 .UNSPECIFIED. ) ;
#5518=VERTEX_POINT ( 'NONE', #18031 ) ;
#5526=ORIENTED_EDGE ( 'NONE', *, *, #7540, .T. ) ;
#5539=EDGE_CURVE ( 'NONE', #27866, #9943, #28428, .T. ) ;
#5540=CARTESIAN_POINT ( 'NONE',  ( -10.69999999994747064, -28.84009800776623678, -19.12627107572801677 ) ) ;
#5547=CARTESIAN_POINT ( 'NONE',  ( 10.69999999995574491, -32.31918898725707123, -22.79246800231758741 ) ) ;
#5551=CARTESIAN_POINT ( 'NONE',  ( 10.90985366930000033, -24.71798678640000091, -1.786271610999999648 ) ) ;
#5554=LINE ( 'NONE', #14707, #23379 ) ;
#5558=EDGE_CURVE ( 'NONE', #3580, #4546, #16464, .T. ) ;
#5559=EDGE_LOOP ( 'NONE', ( #22727, #13586, #8208, #8068 ) ) ;
#5561=ADVANCED_FACE ( 'NONE', ( #9374 ), #11745, .F. ) ;
#5563=EDGE_LOOP ( 'NONE', ( #17924, #26344, #25983, #11477 ) ) ;
#5567=ORIENTED_EDGE ( 'NONE', *, *, #18472, .F. ) ;
#5574=CARTESIAN_POINT ( 'NONE',  ( -13.99999999969999820, 21.34999999960000139, -67.09999999999999432 ) ) ;
#5581=ORIENTED_EDGE ( 'NONE', *, *, #23852, .F. ) ;
#5597=EDGE_CURVE ( 'NONE', #2860, #28481, #16154, .T. ) ;
#5608=ORIENTED_EDGE ( 'NONE', *, *, #14778, .T. ) ;
#5613=B_SPLINE_CURVE_WITH_KNOTS ( 'NONE', 3,
 ( #22619, #15069, #19794, #5462, #29220, #5314 ),
 .UNSPECIFIED., .F., .F.,
 ( 4, 2, 4 ),
 ( 0.000000000000000000, 0.5000000000000000000, 1.000000000000000000 ),
 .UNSPECIFIED. ) ;
#5615=EDGE_CURVE ( 'NONE', #26138, #9514, #5431, .T. ) ;
#5618=VERTEX_POINT ( 'NONE', #17390 ) ;
#5629=CARTESIAN_POINT ( 'NONE',  ( -16.57246140003591250, 12.07825306296973800, -1.400000000000001910 ) ) ;
#5642=ORIENTED_EDGE ( 'NONE', *, *, #12325, .F. ) ;
#5667=PLANE ( 'NONE',  #10216 ) ;
#5673=CARTESIAN_POINT ( 'NONE',  ( 8.999999999770000869, 21.70000000000000284, -60.10000000000000142 ) ) ;
#5674=ORIENTED_EDGE ( 'NONE', *, *, #17117, .T. ) ;
#5678=ORIENTED_EDGE ( 'NONE', *, *, #19856, .F. ) ;
#5696=AXIS2_PLACEMENT_3D ( 'NONE', #27541, #8648, #18246 ) ;
#5712=VECTOR ( 'NONE', #7340, 1000.000000000000000 ) ;
#5744=DIRECTION ( 'NONE',  ( 0.7071067811870476172, 0.000000000000000000, 0.7071067811860475283 ) ) ;
#5759=VECTOR ( 'NONE', #1006, 1000.000000000000000 ) ;
#5761=EDGE_CURVE ( 'NONE', #4001, #26442, #28546, .T. ) ;
#5765=CARTESIAN_POINT ( 'NONE',  ( 9.999999999979825915, -27.78524365354916981, -31.32191802991157914 ) ) ;
#5768=B_SPLINE_CURVE_WITH_KNOTS ( 'NONE', 3,
 ( #13471, #13949, #27954, #11736 ),
 .UNSPECIFIED., .F., .F.,
 ( 4, 4 ),
 ( 0.000000000000000000, 1.000000000000000000 ),
 .UNSPECIFIED. ) ;
#5773=ORIENTED_EDGE ( 'NONE', *, *, #18876, .F. ) ;
#5785=EDGE_CURVE ( 'NONE', #23190, #24264, #26503, .T. ) ;
#5796=EDGE_LOOP ( 'NONE', ( #6690, #14912, #10472, #17055 ) ) ;
#5797=CYLINDRICAL_SURFACE ( 'NONE', #10273, 10.00000000000001421 ) ;
#5812=CARTESIAN_POINT ( 'NONE',  ( -10.00000000021355184, -29.62135916506342070, -29.91085694111316329 ) ) ;
#5817=CARTESIAN_POINT ( 'NONE',  ( -13.99999999968414777, 21.69999999999800622, -58.04802220338182650 ) ) ;
#5818=DIRECTION ( 'NONE',  ( -1.000000000000000000, 0.000000000000000000, 0.000000000000000000 ) ) ;
#5826=DIRECTION ( 'NONE',  ( 0.000000000000000000, 1.000000000000000000, 0.000000000000000000 ) ) ;
#5828=VERTEX_POINT ( 'NONE', #16121 ) ;
#5831=EDGE_CURVE ( 'NONE', #27161, #20099, #26801, .T. ) ;
#5839=EDGE_CURVE ( 'NONE', #13159, #9489, #388, .T. ) ;
#5842=CARTESIAN_POINT ( 'NONE',  ( 8.999999999770000869, 20.99999999999999645, -56.09999999999999432 ) ) ;
#5853=DIRECTION ( 'NONE',  ( 0.000000000000000000, 0.000000000000000000, -1.000000000000000000 ) ) ;
#5869=CARTESIAN_POINT ( 'NONE',  ( -7.797918471980000099, -130.0000000000000000, -43.60208152801600079 ) ) ;
#5877=CARTESIAN_POINT ( 'NONE',  ( 10.69999999930000101, -24.87867965640000278, -26.27867965640000136 ) ) ;
#5881=EDGE_LOOP ( 'NONE', ( #22589, #5212, #22489, #7323, #423 ) ) ;
#5883=CARTESIAN_POINT ( 'NONE',  ( -10.00000000000000000, 20.99999999999999645, -64.10000000019999788 ) ) ;
#5885=ORIENTED_EDGE ( 'NONE', *, *, #3172, .T. ) ;
#5895=VERTEX_POINT ( 'NONE', #19728 ) ;
#5903=CARTESIAN_POINT ( 'NONE',  ( -9.999999999959999997, -36.62914859500000375, -26.86371135770000151 ) ) ;
#5910=VECTOR ( 'NONE', #28995, 1000.000000000000000 ) ;
#5911=VERTEX_POINT ( 'NONE', #14393 ) ;
#5915=EDGE_CURVE ( 'NONE', #11396, #3695, #9973, .T. ) ;
#5916=DIRECTION ( 'NONE',  ( 0.000000000000000000, -2.257145581549999994E-12, -1.000000000000000000 ) ) ;
#5919=AXIS2_PLACEMENT_3D ( 'NONE', #9127, #13387, #20469 ) ;
#5920=FACE_OUTER_BOUND ( 'NONE', #14485, .T. ) ;
#5944=VERTEX_POINT ( 'NONE', #19260 ) ;
#5946=DIRECTION ( 'NONE',  ( 1.000000000000000000, 5.998481157687279274E-24, -2.257150022441830001E-12 ) ) ;
#5951=VERTEX_POINT ( 'NONE', #10734 ) ;
#5963=LINE ( 'NONE', #10690, #12487 ) ;
#5967=VECTOR ( 'NONE', #22471, 1000.000000000000000 ) ;
#5978=EDGE_LOOP ( 'NONE', ( #26617, #17970, #3199, #30382 ) ) ;
#5990=ORIENTED_EDGE ( 'NONE', *, *, #9420, .T. ) ;
#5994=EDGE_CURVE ( 'NONE', #669, #12725, #29624, .T. ) ;
#5997=CYLINDRICAL_SURFACE ( 'NONE', #13318, 1.099999999999999201 ) ;
#6011=CARTESIAN_POINT ( 'NONE',  ( -10.69999999930000101, -127.2537437101000108, -34.36317024006000054 ) ) ;
#6012=EDGE_CURVE ( 'NONE', #24262, #24608, #17459, .T. ) ;
#6036=CARTESIAN_POINT ( 'NONE',  ( 10.45989669369999930, 19.99999999999999645, -43.32262108698500214 ) ) ;
#6047=CARTESIAN_POINT ( 'NONE',  ( -10.69999999996683826, -29.94027628697359944, -27.70856505396162106 ) ) ;
#6052=EDGE_CURVE ( 'NONE', #18608, #17864, #27606, .T. ) ;
#6054=CARTESIAN_POINT ( 'NONE',  ( -11.37440858360000107, -24.37257237719999736, -1.450121501800003099 ) ) ;
#6058=CARTESIAN_POINT ( 'NONE',  ( -9.000000000229999131, 21.70000000000000284, -45.10000000000000142 ) ) ;
#6072=ORIENTED_EDGE ( 'NONE', *, *, #12590, .F. ) ;
#6076=CARTESIAN_POINT ( 'NONE',  ( 0.000000000000000000, -50.49316738903675628, -43.39999999999999858 ) ) ;
#6079=CARTESIAN_POINT ( 'NONE',  ( -13.99999999969999820, 20.99999999999999645, -58.51619611000000276 ) ) ;
#6088=CARTESIAN_POINT ( 'NONE',  ( -17.94252184376523118, 10.97464310239704410, -1.400000000000001910 ) ) ;
#6094=CARTESIAN_POINT ( 'NONE',  ( 10.00000000000000000, 21.35000000040000145, -64.10000000000000853 ) ) ;
#6098=EDGE_CURVE ( 'NONE', #9489, #16174, #12628, .T. ) ;
#6099=FACE_OUTER_BOUND ( 'NONE', #15198, .T. ) ;
#6101=ORIENTED_EDGE ( 'NONE', *, *, #21414, .T. ) ;
#6102=ADVANCED_FACE ( 'NONE', ( #20491 ), #15003, .F. ) ;
#6104=AXIS2_PLACEMENT_3D ( 'NONE', #26389, #9694, #19298 ) ;
#6106=ORIENTED_EDGE ( 'NONE', *, *, #4704, .T. ) ;
#6109=DIRECTION ( 'NONE',  ( -2.965499939100700266E-25, -1.000000000000000000, 2.257145581549900232E-12 ) ) ;
#6110=EDGE_CURVE ( 'NONE', #15341, #3911, #20093, .T. ) ;
#6112=DIRECTION ( 'NONE',  ( -1.000000000000000000, 0.000000000000000000, 0.000000000000000000 ) ) ;
#6134=ORIENTED_EDGE ( 'NONE', *, *, #12507, .T. ) ;
#6135=LINE ( 'NONE', #18084, #16791 ) ;
#6148=VECTOR ( 'NONE', #5394, 1000.000000000000000 ) ;
#6151=EDGE_CURVE ( 'NONE', #12805, #5070, #18596, .T. ) ;
#6169=EDGE_CURVE ( 'NONE', #9481, #2437, #12617, .T. ) ;
#6172=ORIENTED_EDGE ( 'NONE', *, *, #2101, .F. ) ;
#6176=EDGE_LOOP ( 'NONE', ( #21367, #1483, #5030, #2983 ) ) ;
#6183=CARTESIAN_POINT ( 'NONE',  ( 10.73600574249999973, 19.99999999999999645, -2.108020795500001210 ) ) ;
#6185=ORIENTED_EDGE ( 'NONE', *, *, #27154, .T. ) ;
#6187=ORIENTED_EDGE ( 'NONE', *, *, #30828, .T. ) ;
#6191=VECTOR ( 'NONE', #8041, 1000.000000000000000 ) ;
#6193=VECTOR ( 'NONE', #27523, 1000.000000000000000 ) ;
#6196=CARTESIAN_POINT ( 'NONE',  ( 10.20952265640000078, 19.99999999999999645, -43.61772437372000155 ) ) ;
#6197=VECTOR ( 'NONE', #24314, 1000.000000000000000 ) ;
#6222=DIRECTION ( 'NONE',  ( -1.000000000000000000, 0.000000000000000000, 0.000000000000000000 ) ) ;
#6224=ADVANCED_FACE ( 'NONE', ( #13055 ), #29738, .T. ) ;
#6228=EDGE_CURVE ( 'NONE', #5171, #5374, #14245, .T. ) ;
#6234=AXIS2_PLACEMENT_3D ( 'NONE', #22906, #1346, #10940 ) ;
#6239=FACE_OUTER_BOUND ( 'NONE', #11323, .T. ) ;
#6245=LINE ( 'NONE', #11284, #29513 ) ;
#6246=CARTESIAN_POINT ( 'NONE',  ( 10.00000000000000000, 20.99999999999999645, -64.10000000019999788 ) ) ;
#6257=CARTESIAN_POINT ( 'NONE',  ( -10.00000000020000002, -25.00000000000000000, -2.357243106799994159 ) ) ;
#6267=VERTEX_POINT ( 'NONE', #22516 ) ;
#6272=ADVANCED_FACE ( 'NONE', ( #27225 ), #5667, .F. ) ;
#6277=CARTESIAN_POINT ( 'NONE',  ( 3.510330247560000227, 1.917702154400000136, -43.40000000037299799 ) ) ;
#6288=DIRECTION ( 'NONE',  ( -1.000000000000000000, 0.000000000000000000, -2.257144471330000330E-12 ) ) ;
#6295=B_SPLINE_CURVE_WITH_KNOTS ( 'NONE', 3,
 ( #13469, #20555, #14950, #24547, #24856, #6393 ),
 .UNSPECIFIED., .F., .F.,
 ( 4, 2, 4 ),
 ( 0.000000000000000000, 0.5000000000000000000, 1.000000000000000000 ),
 .UNSPECIFIED. ) ;
#6297=CARTESIAN_POINT ( 'NONE',  ( -9.892226903239841107, 20.00000000000001066, -42.92198665947150715 ) ) ;
#6299=ORIENTED_EDGE ( 'NONE', *, *, #3172, .F. ) ;
#6303=ORIENTED_EDGE ( 'NONE', *, *, #15465, .T. ) ;
#6314=ORIENTED_EDGE ( 'NONE', *, *, #6228, .F. ) ;
#6321=EDGE_CURVE ( 'NONE', #24088, #11396, #14004, .T. ) ;
#6339=EDGE_CURVE ( 'NONE', #18717, #19721, #16047, .T. ) ;
#6346=ORIENTED_EDGE ( 'NONE', *, *, #22972, .F. ) ;
#6350=CARTESIAN_POINT ( 'NONE',  ( -13.12132034329999897, 20.99999999990000887, -69.22132034359999864 ) ) ;
#6357=DIRECTION ( 'NONE',  ( 0.000000000000000000, -1.000000000000000000, 0.000000000000000000 ) ) ;
#6358=CARTESIAN_POINT ( 'NONE',  ( -11.69999999989999928, 19.99999999999999645, -1.399999999999998579 ) ) ;
#6360=ORIENTED_EDGE ( 'NONE', *, *, #16373, .T. ) ;
#6361=LINE ( 'NONE', #17834, #26071 ) ;
#6362=EDGE_CURVE ( 'NONE', #23901, #29453, #8801, .T. ) ;
#6365=CARTESIAN_POINT ( 'NONE',  ( 8.999999999770000869, 20.99999999999999645, -58.10000000000000142 ) ) ;
#6367=CARTESIAN_POINT ( 'NONE',  ( -10.69999999996466755, -29.52945879161127252, -26.74930136228349298 ) ) ;
#6368=DIRECTION ( 'NONE',  ( 0.000000000000000000, -1.000000000000000000, 2.257145581549999994E-12 ) ) ;
#6369=CARTESIAN_POINT ( 'NONE',  ( -8.999999999710000864, 20.70710678120000381, -44.39289321881399530 ) ) ;
#6371=CARTESIAN_POINT ( 'NONE',  ( 10.99289321870000080, -24.65831413369999936, -1.692893218799999877 ) ) ;
#6374=CARTESIAN_POINT ( 'NONE',  ( -11.69999999989999928, -24.11120071670000087, -0.6999999999999992895 ) ) ;
#6375=DIRECTION ( 'NONE',  ( 1.000000000000000000, 0.000000000000000000, 0.000000000000000000 ) ) ;
#6384=CARTESIAN_POINT ( 'NONE',  ( -14.00000000000000000, 20.99999999999999645, -62.80809805499999499 ) ) ;
#6388=ORIENTED_EDGE ( 'NONE', *, *, #13396, .F. ) ;
#6389=LINE ( 'NONE', #13782, #2373 ) ;
#6390=ORIENTED_EDGE ( 'NONE', *, *, #9589, .F. ) ;
#6393=CARTESIAN_POINT ( 'NONE',  ( -13.12132034329999897, 20.99999999990000887, -69.22132034359999864 ) ) ;
#6399=ORIENTED_EDGE ( 'NONE', *, *, #12685, .F. ) ;
#6406=DIRECTION ( 'NONE',  ( -1.000000000000000000, 2.463770379189999939E-24, 2.257150022439999944E-12 ) ) ;
#6413=EDGE_CURVE ( 'NONE', #68, #24422, #1489, .T. ) ;
#6419=CARTESIAN_POINT ( 'NONE',  ( 10.69999999997431672, -25.48863729555974444, -31.02111648952697820 ) ) ;
#6422=EDGE_LOOP ( 'NONE', ( #22173, #27738 ) ) ;
#6427=B_SPLINE_CURVE_WITH_KNOTS ( 'NONE', 3,
 ( #26684, #9853, #7792, #21975, #7490, #19765, #12669, #2469, #12207, #21665 ),
 .UNSPECIFIED., .F., .F.,
 ( 4, 2, 2, 2, 4 ),
 ( 0.000000000000000000, 0.2500000000000000000, 0.5000000000000000000, 0.7500000000000000000, 1.000000000000000000 ),
 .UNSPECIFIED. ) ;
#6440=FACE_OUTER_BOUND ( 'NONE', #1933, .T. ) ;
#6455=CARTESIAN_POINT ( 'NONE',  ( 9.999999999953960383, -32.32189936811070652, -22.79484972463425052 ) ) ;
#6460=FILL_AREA_STYLE_COLOUR ( '', #7316 ) ;
#6471=CARTESIAN_POINT ( 'NONE',  ( -10.69999999999999929, -29.12132034360000077, -30.52132034359999935 ) ) ;
#6472=CYLINDRICAL_SURFACE ( 'NONE', #31088, 1.700000000000000178 ) ;
#6486=ORIENTED_EDGE ( 'NONE', *, *, #13199, .T. ) ;
#6490=ORIENTED_EDGE ( 'NONE', *, *, #24998, .T. ) ;
#6494=ORIENTED_EDGE ( 'NONE', *, *, #1629, .F. ) ;
#6505=CARTESIAN_POINT ( 'NONE',  ( 10.00000000000000000, 20.99999999990000887, -70.10000000019999788 ) ) ;
#6520=EDGE_LOOP ( 'NONE', ( #374, #6390, #6388, #12606, #16024, #14058, #26207 ) ) ;
#6528=CARTESIAN_POINT ( 'NONE',  ( -11.04680313119999902, -24.61949706369999902, -1.636966784999999147 ) ) ;
#6537=VERTEX_POINT ( 'NONE', #19242 ) ;
#6541=DIRECTION ( 'NONE',  ( -1.000000000000000000, 0.000000000000000000, 0.000000000000000000 ) ) ;
#6546=CARTESIAN_POINT ( 'NONE',  ( -10.69999999999999929, -127.2537393281999982, -34.36317439833000265 ) ) ;
#6554=CYLINDRICAL_SURFACE ( 'NONE', #22542, 3.000000000000002220 ) ;
#6555=CARTESIAN_POINT ( 'NONE',  ( 10.69999999999999929, -27.00000000000000000, -25.39999999999999858 ) ) ;
#6564=FACE_OUTER_BOUND ( 'NONE', #13866, .T. ) ;
#6572=ORIENTED_EDGE ( 'NONE', *, *, #15208, .F. ) ;
#6578=CYLINDRICAL_SURFACE ( 'NONE', #4548, 3.000000000000000444 ) ;
#6580=ORIENTED_EDGE ( 'NONE', *, *, #21512, .F. ) ;
#6583=FACE_BOUND ( 'NONE', #13743, .T. ) ;
#6584=EDGE_CURVE ( 'NONE', #22335, #19928, #12774, .T. ) ;
#6586=CARTESIAN_POINT ( 'NONE',  ( -8.999999999710000864, 21.35000000010000321, -45.09999999954499827 ) ) ;
#6596=DIRECTION ( 'NONE',  ( -0.000000000000000000, -0.000000000000000000, 1.000000000000000000 ) ) ;
#6599=CARTESIAN_POINT ( 'NONE',  ( -10.00000000000000000, 21.70000000000000284, -62.10000000019999788 ) ) ;
#6602=CARTESIAN_POINT ( 'NONE',  ( 8.999999999770000869, 21.00000000069999473, -48.10000000000000142 ) ) ;
#6609=EDGE_LOOP ( 'NONE', ( #8458, #14631, #10183, #3130, #4610, #7151, #8339, #24576, #13958, #4070, #18935, #17773 ) ) ;
#6616=ORIENTED_EDGE ( 'NONE', *, *, #22230, .F. ) ;
#6620=EDGE_CURVE ( 'NONE', #29101, #29098, #10420, .T. ) ;
#6624=CARTESIAN_POINT ( 'NONE',  ( 21.09633121001184719, -16.56519925036682039, -1.399999999999998579 ) ) ;
#6633=FACE_OUTER_BOUND ( 'NONE', #17150, .T. ) ;
#6640=ORIENTED_EDGE ( 'NONE', *, *, #3084, .T. ) ;
#6647=ORIENTED_EDGE ( 'NONE', *, *, #27996, .F. ) ;
#6652=ORIENTED_EDGE ( 'NONE', *, *, #7023, .F. ) ;
#6657=DIRECTION ( 'NONE',  ( -1.000000000000000000, 0.000000000000000000, -2.257144471330000330E-12 ) ) ;
#6669=LINE ( 'NONE', #6365, #19566 ) ;
#6671=ORIENTED_EDGE ( 'NONE', *, *, #15437, .F. ) ;
#6681=ADVANCED_FACE ( 'NONE', ( #1127 ), #10718, .T. ) ;
#6690=ORIENTED_EDGE ( 'NONE', *, *, #503, .F. ) ;
#6691=CARTESIAN_POINT ( 'NONE',  ( -10.00000000057657878, -24.00000000000020250, -28.00730091830135393 ) ) ;
#6694=VERTEX_POINT ( 'NONE', #13224 ) ;
#6698=LINE ( 'NONE', #9364, #9530 ) ;
#6699=DIRECTION ( 'NONE',  ( -1.595945597898660305E-12, -0.7071067811865475727, 0.7071067811865475727 ) ) ;
#6702=CYLINDRICAL_SURFACE ( 'NONE', #29379, 3.000000000000003997 ) ;
#6704=DIRECTION ( 'NONE',  ( 1.000000000000000000, -0.000000000000000000, -2.257150022439999944E-12 ) ) ;
#6715=CARTESIAN_POINT ( 'NONE',  ( 9.999999999970887288, -23.99999999999979394, -28.79269908193450789 ) ) ;
#6720=DIRECTION ( 'NONE',  ( 0.000000000000000000, -2.257145581549999994E-12, -1.000000000000000000 ) ) ;
#6724=AXIS2_PLACEMENT_3D ( 'NONE', #17954, #14891, #29187 ) ;
#6725=ORIENTED_EDGE ( 'NONE', *, *, #6052, .T. ) ;
#6727=VECTOR ( 'NONE', #24335, 1000.000000000000000 ) ;
#6729=CIRCLE ( 'NONE', #20827, 1.099999999570000497 ) ;
#6734=ORIENTED_EDGE ( 'NONE', *, *, #633, .T. ) ;
#6735=EDGE_CURVE ( 'NONE', #15021, #9398, #9556, .T. ) ;
#6748=EDGE_CURVE ( 'NONE', #29523, #23857, #18582, .T. ) ;
#6751=AXIS2_PLACEMENT_3D ( 'NONE', #17434, #29706, #5328 ) ;
#6765=CARTESIAN_POINT ( 'NONE',  ( -11.54917764160000004, 19.99999999999999645, -0.6999999992999966780 ) ) ;
#6785=CARTESIAN_POINT ( 'NONE',  ( -9.000000000000000000, -54.99999999999998579, -42.39999999999999858 ) ) ;
#6791=PLANE ( 'NONE',  #14356 ) ;
#6804=ORIENTED_EDGE ( 'NONE', *, *, #11275, .T. ) ;
#6824=ORIENTED_EDGE ( 'NONE', *, *, #25923, .T. ) ;
#6825=CARTESIAN_POINT ( 'NONE',  ( -14.76964124820000102, 19.99999999999999645, -1.399999999299995856 ) ) ;
#6829=EDGE_LOOP ( 'NONE', ( #3469, #3015, #517, #6490 ) ) ;
#6839=CARTESIAN_POINT ( 'NONE',  ( -10.69999999999999929, -24.47788622780000267, -30.04435323410000080 ) ) ;
#6840=DIRECTION ( 'NONE',  ( -0.7071067811870488384, 0.000000000000000000, 0.7071067811860461960 ) ) ;
#6842=EDGE_CURVE ( 'NONE', #14134, #12603, #18579, .T. ) ;
#6847=CARTESIAN_POINT ( 'NONE',  ( -9.999999999969999109, -24.00000000000000000, -28.40000000000000213 ) ) ;
#6852=ORIENTED_EDGE ( 'NONE', *, *, #8582, .T. ) ;
#6856=CARTESIAN_POINT ( 'NONE',  ( -10.69999999999999929, -27.00000000000000000, -28.40000000000000213 ) ) ;
#6870=CARTESIAN_POINT ( 'NONE',  ( 4.175165894169885483, -50.49316738903675628, -44.10000000000000142 ) ) ;
#6873=ORIENTED_EDGE ( 'NONE', *, *, #27097, .T. ) ;
#6884=CARTESIAN_POINT ( 'NONE',  ( 8.999999999540001738, -130.0000000000000000, -43.75000000008299850 ) ) ;
#6886=AXIS2_PLACEMENT_3D ( 'NONE', #12318, #17344, #7129 ) ;
#6900=CARTESIAN_POINT ( 'NONE',  ( -10.02421345359999982, -25.00000000000000000, -2.058579360600006236 ) ) ;
#6906=CARTESIAN_POINT ( 'NONE',  ( 10.49791847189999849, 19.99999999999999645, -3.602081527999998034 ) ) ;
#6911=AXIS2_PLACEMENT_3D ( 'NONE', #23090, #1837, #30318 ) ;
#6913=CARTESIAN_POINT ( 'NONE',  ( -9.707106781189999367, 19.99999999999999645, -43.10710678118599759 ) ) ;
#6914=VERTEX_POINT ( 'NONE', #14177 ) ;
#6916=CARTESIAN_POINT ( 'NONE',  ( -11.25000838610000109, 19.99999999999999645, -0.7501799203000064642 ) ) ;
#6918=VECTOR ( 'NONE', #29412, 1000.000000000000000 ) ;
#6922=VERTEX_POINT ( 'NONE', #9604 ) ;
#6927=CARTESIAN_POINT ( 'NONE',  ( 11.69999999989999928, -24.11120071670000087, -0.6999999999999992895 ) ) ;
#6938=CYLINDRICAL_SURFACE ( 'NONE', #22986, 3.000000000000003997 ) ;
#6946=AXIS2_PLACEMENT_3D ( 'NONE', #9759, #12116, #16842 ) ;
#6953=CARTESIAN_POINT ( 'NONE',  ( 18.13191322229999969, 10.47263190749999495, -1.399999999599998990 ) ) ;
#6956=CARTESIAN_POINT ( 'NONE',  ( -18.93860194420127030, -19.09088854112969003, -1.399999999999998579 ) ) ;
#6959=AXIS2_PLACEMENT_3D ( 'NONE', #14805, #29419, #22349 ) ;
#6960=ORIENTED_EDGE ( 'NONE', *, *, #8269, .F. ) ;
#6963=ORIENTED_EDGE ( 'NONE', *, *, #6110, .T. ) ;
#6991=ORIENTED_EDGE ( 'NONE', *, *, #11036, .T. ) ;
#6992=CARTESIAN_POINT ( 'NONE',  ( 25.87491792499379883, 7.311113148304238862, -1.399999999999998579 ) ) ;
#6993=CARTESIAN_POINT ( 'NONE',  ( -10.69999999989999928, -25.00000000000000000, -16.71944709739999979 ) ) ;
#6996=CARTESIAN_POINT ( 'NONE',  ( -12.77820031340000106, 20.99999999999999645, -56.10000000020000499 ) ) ;
#7002=DIRECTION ( 'NONE',  ( 0.000000000000000000, 1.000000000000000000, 0.000000000000000000 ) ) ;
#7009=EDGE_LOOP ( 'NONE', ( #21809, #19618 ) ) ;
#7010=CARTESIAN_POINT ( 'NONE',  ( 11.50378924416101256, 21.69999999997430606, -55.48383121567042764 ) ) ;
#7016=EDGE_CURVE ( 'NONE', #5895, #9494, #6295, .T. ) ;
#7017=ORIENTED_EDGE ( 'NONE', *, *, #7191, .T. ) ;
#7022=CARTESIAN_POINT ( 'NONE',  ( -10.69999999994971240, -29.61921542333507773, -20.12109567583046399 ) ) ;
#7023=EDGE_CURVE ( 'NONE', #28644, #1470, #25080, .T. ) ;
#7026=DIRECTION ( 'NONE',  ( 1.000000000000000000, 0.000000000000000000, 0.000000000000000000 ) ) ;
#7032=LINE ( 'NONE', #25655, #26775 ) ;
#7041=VERTEX_POINT ( 'NONE', #22183 ) ;
#7063=CARTESIAN_POINT ( 'NONE',  ( -9.999999999909999104, -25.00000000000000000, -2.399999999999999467 ) ) ;
#7083=EDGE_CURVE ( 'NONE', #7041, #24435, #29567, .T. ) ;
#7087=ORIENTED_EDGE ( 'NONE', *, *, #2738, .F. ) ;
#7089=ORIENTED_EDGE ( 'NONE', *, *, #1516, .F. ) ;
#7103=DIRECTION ( 'NONE',  ( -1.000000000000000000, 0.000000000000000000, 0.000000000000000000 ) ) ;
#7106=DIRECTION ( 'NONE',  ( 0.000000000000000000, -1.000000000000000000, 0.000000000000000000 ) ) ;
#7122=ORIENTED_EDGE ( 'NONE', *, *, #15437, .T. ) ;
#7125=DIRECTION ( 'NONE',  ( 0.7071067811865475727, 1.595945597898661921E-12, 0.7071067811865475727 ) ) ;
#7129=DIRECTION ( 'NONE',  ( -0.7071067811865466846, 1.595945597898659700E-12, 0.7071067811865484609 ) ) ;
#7133=EDGE_CURVE ( 'NONE', #20466, #8872, #21102, .T. ) ;
#7134=VECTOR ( 'NONE', #14910, 1000.000000000000000 ) ;
#7137=CARTESIAN_POINT ( 'NONE',  ( 10.49243769669999971, -24.66097101770000322, -1.192453590699998900 ) ) ;
#7149=DIRECTION ( 'NONE',  ( 0.8086898287149010267, 0.000000000000000000, 0.5882352938519278540 ) ) ;
#7151=ORIENTED_EDGE ( 'NONE', *, *, #25427, .T. ) ;
#7152=AXIS2_PLACEMENT_3D ( 'NONE', #20214, #8873, #25421 ) ;
#7153=CARTESIAN_POINT ( 'NONE',  ( -10.69999999999999929, -24.00000000000000000, -28.40000000000000213 ) ) ;
#7163=VECTOR ( 'NONE', #4493, 1000.000000000000000 ) ;
#7165=ORIENTED_EDGE ( 'NONE', *, *, #20020, .T. ) ;
#7168=FACE_OUTER_BOUND ( 'NONE', #7616, .T. ) ;
#7175=CARTESIAN_POINT ( 'NONE',  ( -10.00000000060000005, -25.00000000000000000, -4.837481085199997644 ) ) ;
#7177=FACE_OUTER_BOUND ( 'NONE', #26512, .T. ) ;
#7178=DIRECTION ( 'NONE',  ( 2.257150022439999944E-12, 0.000000000000000000, 1.000000000000000000 ) ) ;
#7182=DIRECTION ( 'NONE',  ( 0.000000000000000000, 1.000000000000000000, 0.000000000000000000 ) ) ;
#7189=CARTESIAN_POINT ( 'NONE',  ( -9.000000000229999131, 20.99999999999999645, -48.10000000000000142 ) ) ;
#7191=EDGE_CURVE ( 'NONE', #21717, #24422, #6698, .T. ) ;
#7193=DIRECTION ( 'NONE',  ( 0.000000000000000000, 0.000000000000000000, -1.000000000000000000 ) ) ;
#7196=EDGE_CURVE ( 'NONE', #29138, #30054, #11431, .T. ) ;
#7205=AXIS2_PLACEMENT_3D ( 'NONE', #3149, #810, #25176 ) ;
#7209=VECTOR ( 'NONE', #18568, 1000.000000000000000 ) ;
#7210=DIRECTION ( 'NONE',  ( 2.250897877190000270E-12, 0.000000000000000000, 1.000000000000000000 ) ) ;
#7211=CARTESIAN_POINT ( 'NONE',  ( -8.999999999970000886, 20.99999999999999645, -45.10000000000000142 ) ) ;
#7212=CYLINDRICAL_SURFACE ( 'NONE', #20460, 3.999999999999999112 ) ;
#7217=LINE ( 'NONE', #11629, #1427 ) ;
#7224=CARTESIAN_POINT ( 'NONE',  ( -10.69999999999999929, -126.7743301060000078, -33.87904238509999999 ) ) ;
#7228=AXIS2_PLACEMENT_3D ( 'NONE', #30175, #30339, #27813 ) ;
#7229=CIRCLE ( 'NONE', #27843, 26.80000000000000071 ) ;
#7231=ORIENTED_EDGE ( 'NONE', *, *, #21668, .F. ) ;
#7232=AXIS2_PLACEMENT_3D ( 'NONE', #17061, #19118, #26661 ) ;
#7235=LINE ( 'NONE', #7954, #1645 ) ;
#7243=ORIENTED_EDGE ( 'NONE', *, *, #22943, .T. ) ;
#7250=DIRECTION ( 'NONE',  ( -1.000000000000000000, 0.000000000000000000, -2.257144471330000330E-12 ) ) ;
#7257=AXIS2_PLACEMENT_3D ( 'NONE', #16164, #4209, #30802 ) ;
#7268=CARTESIAN_POINT ( 'NONE',  ( 16.90560620815911719, 9.921746937094770402, -1.400000000000001910 ) ) ;
#7273=CARTESIAN_POINT ( 'NONE',  ( 10.69999999999999929, -24.00000000000000000, -28.40000000000000213 ) ) ;
#7293=CARTESIAN_POINT ( 'NONE',  ( -9.000000000000000000, -55.00000000000000000, -43.39999999999999858 ) ) ;
#7309=CARTESIAN_POINT ( 'NONE',  ( -11.09640325699999863, -24.58282406889999905, -1.600739421300005683 ) ) ;
#7313=FACE_OUTER_BOUND ( 'NONE', #1444, .T. ) ;
#7316=COLOUR_RGB ( '', 0.31764706, 0.68627451, 0.89019608) ;
#7321=ORIENTED_EDGE ( 'NONE', *, *, #12507, .F. ) ;
#7323=ORIENTED_EDGE ( 'NONE', *, *, #30535, .F. ) ;
#7340=DIRECTION ( 'NONE',  ( -0.000000000000000000, -0.000000000000000000, 1.000000000000000000 ) ) ;
#7346=CARTESIAN_POINT ( 'NONE',  ( 9.999999999969999109, -24.87872937930000106, -30.52127062269999769 ) ) ;
#7348=CARTESIAN_POINT ( 'NONE',  ( 12.12499559729999810, 21.69999999929999390, -55.73512174120000395 ) ) ;
#7352=CARTESIAN_POINT ( 'NONE',  ( -8.999999999699999975, 21.69999999919999212, -70.09999999999999432 ) ) ;
#7362=CARTESIAN_POINT ( 'NONE',  ( 12.27469135525410593, 20.99999999997359978, -55.79567638067133828 ) ) ;
#7365=EDGE_CURVE ( 'NONE', #19758, #8971, #29109, .T. ) ;
#7368=DIRECTION ( 'NONE',  ( 1.000000000000000000, 0.000000000000000000, 0.000000000000000000 ) ) ;
#7370=CARTESIAN_POINT ( 'NONE',  ( 13.67718073920000066, 20.99999999999999645, -57.16242423349999768 ) ) ;
#7376=FACE_BOUND ( 'NONE', #27959, .T. ) ;
#7380=CYLINDRICAL_SURFACE ( 'NONE', #24865, 5.000000000000001776 ) ;
#7381=CARTESIAN_POINT ( 'NONE',  ( -10.69999999989999928, -30.49251257979999963, -21.04205368470000082 ) ) ;
#7387=CARTESIAN_POINT ( 'NONE',  ( 9.999999999971130649, -25.48914305972228078, -31.02135916551032935 ) ) ;
#7402=DIRECTION ( 'NONE',  ( -0.000000000000000000, 1.000000000000000000, -2.257145581549999994E-12 ) ) ;
#7404=ORIENTED_EDGE ( 'NONE', *, *, #27861, .F. ) ;
#7417=DIRECTION ( 'NONE',  ( 1.000000000000000000, 0.000000000000000000, 0.000000000000000000 ) ) ;
#7428=B_SPLINE_SURFACE_WITH_KNOTS ( 'NONE', 5, 1, ( 
 ( #16630, #26239 ),
 ( #20084, #14902 ),
 ( #22748, #12846 ),
 ( #19778, #895 ),
 ( #3388, #15056 ),
 ( #27007, #3238 ),
 ( #29675, #25112 ),
 ( #10635, #3545 ),
 ( #594, #8105 ),
 ( #27164, #1043 ),
 ( #29360, #5447 ),
 ( #10177, #22448 ) ),
 .UNSPECIFIED., .F., .F., .F.,
 ( 6, 3, 3, 6 ),
 ( 2, 2 ),
 ( 0.000000000000000000, 0.5717440563929999664, 1.143488112780000066, 1.429360140980000082 ),
 ( -0.7000000000009999335, 0.002002273571169999912 ),
 .UNSPECIFIED. ) ;
#7433=CIRCLE ( 'NONE', #25015, 1.099999999570000497 ) ;
#7437=ORIENTED_EDGE ( 'NONE', *, *, #2678, .F. ) ;
#7438=( NAMED_UNIT ( * ) PLANE_ANGLE_UNIT ( ) SI_UNIT ( $, .RADIAN. ) );
#7439=AXIS2_PLACEMENT_3D ( 'NONE', #14714, #19121, #28714 ) ;
#7440=CARTESIAN_POINT ( 'NONE',  ( -13.46591448088098808, 21.69999999929855505, -56.74462827942989662 ) ) ;
#7443=CARTESIAN_POINT ( 'NONE',  ( 10.69999999999999929, -29.06671945340000107, -26.22544931050000017 ) ) ;
#7448=CARTESIAN_POINT ( 'NONE',  ( 11.69999999989999928, 19.99999999999999645, -1.399999999999998579 ) ) ;
#7454=CARTESIAN_POINT ( 'NONE',  ( 0.000000000000000000, -119.7166638525666826, -63.39999999999999858 ) ) ;
#7455=CARTESIAN_POINT ( 'NONE',  ( -11.37440858360000107, -24.37257237719999736, -1.450121501800003099 ) ) ;
#7459=B_SPLINE_CURVE_WITH_KNOTS ( 'NONE', 3,
 ( #563, #29022, #7468, #17064, #29170, #16906 ),
 .UNSPECIFIED., .F., .F.,
 ( 4, 2, 4 ),
 ( 0.000000000000000000, 0.5000000000000000000, 1.000000000000000000 ),
 .UNSPECIFIED. ) ;
#7465=DIRECTION ( 'NONE',  ( 0.000000000000000000, -1.000000000000000000, 0.000000000000000000 ) ) ;
#7468=CARTESIAN_POINT ( 'NONE',  ( -11.19478429451004153, 19.99999999999999645, -1.527457921041847966 ) ) ;
#7470=ORIENTED_EDGE ( 'NONE', *, *, #28437, .F. ) ;
#7474=AXIS2_PLACEMENT_3D ( 'NONE', #25606, #1836, #2149 ) ;
#7483=ORIENTED_EDGE ( 'NONE', *, *, #24063, .T. ) ;
#7490=CARTESIAN_POINT ( 'NONE',  ( 10.69999999998770157, -129.0530586102001962, -36.95173408317435815 ) ) ;
#7498=CARTESIAN_POINT ( 'NONE',  ( 10.69999999930000101, -120.5233595624000174, -31.26042064949999855 ) ) ;
#7502=VECTOR ( 'NONE', #3518, 1000.000000000000000 ) ;
#7509=VERTEX_POINT ( 'NONE', #17833 ) ;
#7511=EDGE_LOOP ( 'NONE', ( #28574, #28810, #13177, #4592 ) ) ;
#7516=DIRECTION ( 'NONE',  ( 0.000000000000000000, -1.000000000000000000, 0.000000000000000000 ) ) ;
#7520=DIRECTION ( 'NONE',  ( 0.000000000000000000, 0.000000000000000000, 1.000000000000000000 ) ) ;
#7521=EDGE_CURVE ( 'NONE', #28717, #11411, #23048, .T. ) ;
#7528=EDGE_CURVE ( 'NONE', #17102, #8971, #22579, .T. ) ;
#7533=CARTESIAN_POINT ( 'NONE',  ( -10.69999999999999929, -121.6050280552999965, -31.36907097850000170 ) ) ;
#7540=EDGE_CURVE ( 'NONE', #15618, #9281, #9697, .T. ) ;
#7541=EDGE_LOOP ( 'NONE', ( #20407, #27603, #30587, #24429, #10139, #7647 ) ) ;
#7552=EDGE_CURVE ( 'NONE', #20501, #23803, #29588, .T. ) ;
#7553=FACE_OUTER_BOUND ( 'NONE', #18550, .T. ) ;
#7558=CARTESIAN_POINT ( 'NONE',  ( -10.69999999995908091, -34.38191890726957212, -24.27107665818032700 ) ) ;
#7571=ORIENTED_EDGE ( 'NONE', *, *, #18210, .F. ) ;
#7572=DIRECTION ( 'NONE',  ( 0.8923935798119907448, 1.018860921557044162E-12, 0.4512579070889951582 ) ) ;
#7573=CARTESIAN_POINT ( 'NONE',  ( 10.32522729140000095, -2.500000000000002220, -1.399999999999998579 ) ) ;
#7586=EDGE_CURVE ( 'NONE', #29101, #11584, #2481, .T. ) ;
#7591=LINE ( 'NONE', #21613, #19459 ) ;
#7599=FACE_BOUND ( 'NONE', #23703, .T. ) ;
#7616=EDGE_LOOP ( 'NONE', ( #10909, #17674, #6640, #1500 ) ) ;
#7620=EDGE_LOOP ( 'NONE', ( #9636, #14828, #15973, #20165 ) ) ;
#7622=DIRECTION ( 'NONE',  ( -1.000000000000000000, 1.853796481301025284E-24, -2.257144471330669991E-12 ) ) ;
#7630=VERTEX_POINT ( 'NONE', #6358 ) ;
#7632=ADVANCED_FACE ( 'NONE', ( #20993 ), #25562, .F. ) ;
#7647=ORIENTED_EDGE ( 'NONE', *, *, #24998, .F. ) ;
#7648=FACE_OUTER_BOUND ( 'NONE', #18452, .T. ) ;
#7657=ORIENTED_EDGE ( 'NONE', *, *, #6169, .F. ) ;
#7687=AXIS2_PLACEMENT_3D ( 'NONE', #9145, #23643, #9461 ) ;
#7694=ORIENTED_EDGE ( 'NONE', *, *, #9036, .F. ) ;
#7696=CARTESIAN_POINT ( 'NONE',  ( -11.57608395609999974, -24.17108566160000294, -0.7028182529999968953 ) ) ;
#7700=EDGE_CURVE ( 'NONE', #9494, #11197, #29191, .T. ) ;
#7704=CARTESIAN_POINT ( 'NONE',  ( -10.69999999999999929, -43.95328087560000085, -27.24755286599999948 ) ) ;
#7714=CARTESIAN_POINT ( 'NONE',  ( -1.598721155459999804E-14, 0.000000000000000000, -0.6999999999999992895 ) ) ;
#7725=FACE_OUTER_BOUND ( 'NONE', #1309, .T. ) ;
#7734=DIRECTION ( 'NONE',  ( 0.000000000000000000, 0.000000000000000000, 1.000000000000000000 ) ) ;
#7739=( NAMED_UNIT ( * ) SI_UNIT ( $, .STERADIAN. ) SOLID_ANGLE_UNIT ( ) );
#7755=CARTESIAN_POINT ( 'NONE',  ( -10.69999999999999929, -27.00000000000000000, -31.39999999999999858 ) ) ;
#7763=VECTOR ( 'NONE', #23685, 1000.000000000000000 ) ;
#7775=DIRECTION ( 'NONE',  ( 1.553705081258626668E-12, 0.7253743710120288402, -0.6883545756940265825 ) ) ;
#7781=ORIENTED_EDGE ( 'NONE', *, *, #20540, .F. ) ;
#7792=CARTESIAN_POINT ( 'NONE',  ( 10.69999999998402274, -128.0799935798686136, -35.32105789699520670 ) ) ;
#7799=CARTESIAN_POINT ( 'NONE',  ( -15.86808677770000209, -9.527368092500001495, -0.7999999992999995424 ) ) ;
#7803=ORIENTED_EDGE ( 'NONE', *, *, #17109, .F. ) ;
#7807=EDGE_LOOP ( 'NONE', ( #14174, #9599, #8681, #24455 ) ) ;
#7811=ORIENTED_EDGE ( 'NONE', *, *, #7552, .T. ) ;
#7830=CARTESIAN_POINT ( 'NONE',  ( -10.69999999999999929, -120.7100010810000015, -31.27129587090000129 ) ) ;
#7842=EDGE_CURVE ( 'NONE', #14782, #28608, #20171, .T. ) ;
#7855=CARTESIAN_POINT ( 'NONE',  ( -10.69999999996523243, -41.43563524454161495, -26.99587756277172090 ) ) ;
#7867=DIRECTION ( 'NONE',  ( -0.9915824307782121760, -0.1294769592320275942, 4.045530494348897360E-18 ) ) ;
#7871=DIRECTION ( 'NONE',  ( 0.8775825618903718706, -0.4794255386042047262, 0.000000000000000000 ) ) ;
#7876=ORIENTED_EDGE ( 'NONE', *, *, #18737, .T. ) ;
#7881=ORIENTED_EDGE ( 'NONE', *, *, #26927, .F. ) ;
#7882=CARTESIAN_POINT ( 'NONE',  ( 13.67718073920000066, 21.70000000000000284, -57.16242423349999768 ) ) ;
#7886=ORIENTED_EDGE ( 'NONE', *, *, #21521, .T. ) ;
#7890=DIRECTION ( 'NONE',  ( -1.000000000000000000, 0.000000000000000000, 0.000000000000000000 ) ) ;
#7893=EDGE_CURVE ( 'NONE', #5070, #27866, #28531, .T. ) ;
#7901=ADVANCED_FACE ( 'NONE', ( #13873 ), #16535, .T. ) ;
#7902=CARTESIAN_POINT ( 'NONE',  ( 9.999999999979998222, -27.00000000000000000, -31.39999999999999858 ) ) ;
#7905=ADVANCED_FACE ( 'NONE', ( #28495 ), #1916, .T. ) ;
#7906=CARTESIAN_POINT ( 'NONE',  ( -11.06030392579999955, -24.60936423849999954, -1.629296567100001258 ) ) ;
#7915=VECTOR ( 'NONE', #20512, 1000.000000000000000 ) ;
#7920=ADVANCED_FACE ( 'NONE', ( #4428 ), #6938, .F. ) ;
#7930=EDGE_CURVE ( 'NONE', #30214, #68, #1604, .T. ) ;
#7936=VERTEX_POINT ( 'NONE', #5350 ) ;
#7954=CARTESIAN_POINT ( 'NONE',  ( -9.000000000000000000, -55.00000000000000000, -44.10000000000000142 ) ) ;
#7962=AXIS2_PLACEMENT_3D ( 'NONE', #23102, #6406, #4204 ) ;
#7969=CARTESIAN_POINT ( 'NONE',  ( -10.99999999969999998, 20.99999999999999645, -67.09999999999999432 ) ) ;
#7974=LINE ( 'NONE', #918, #27845 ) ;
#7985=VECTOR ( 'NONE', #24944, 1000.000000000000114 ) ;
#7990=CARTESIAN_POINT ( 'NONE',  ( -10.89131017139999891, -2.500000000000002220, -1.811764705899998606 ) ) ;
#7993=ORIENTED_EDGE ( 'NONE', *, *, #7930, .F. ) ;
#7996=ORIENTED_EDGE ( 'NONE', *, *, #6362, .F. ) ;
#8011=DIRECTION ( 'NONE',  ( -1.000000000000000000, 0.000000000000000000, 0.000000000000000000 ) ) ;
#8027=ADVANCED_FACE ( 'NONE', ( #30194 ), #23600, .T. ) ;
#8029=DIRECTION ( 'NONE',  ( 0.000000000000000000, -2.257157423930000049E-12, -1.000000000000000000 ) ) ;
#8031=PLANE ( 'NONE',  #13839 ) ;
#8035=ORIENTED_EDGE ( 'NONE', *, *, #26211, .T. ) ;
#8041=DIRECTION ( 'NONE',  ( 0.000000000000000000, 0.000000000000000000, -1.000000000000000000 ) ) ;
#8052=CARTESIAN_POINT ( 'NONE',  ( 0.000000000000000000, -130.0000000000000000, -44.10000000000000142 ) ) ;
#8054=CARTESIAN_POINT ( 'NONE',  ( -17.79876841479999783, 11.52736809289999620, -1.399999999999998579 ) ) ;
#8068=ORIENTED_EDGE ( 'NONE', *, *, #30535, .T. ) ;
#8072=CARTESIAN_POINT ( 'NONE',  ( -11.50543609154933300, 21.00000000000056488, -55.48449806767045800 ) ) ;
#8105=CARTESIAN_POINT ( 'NONE',  ( 11.51411768920000078, -24.20066399999999973, -0.7084723288000027708 ) ) ;
#8106=CARTESIAN_POINT ( 'NONE',  ( -11.69999999989999928, 19.99999999999999645, -2.399999999999999467 ) ) ;
#8107=CARTESIAN_POINT ( 'NONE',  ( -24.35939747514432696, 11.38309468199551766, -0.6999999999999992895 ) ) ;
#8115=LINE ( 'NONE', #20102, #27002 ) ;
#8118=B_SPLINE_CURVE_WITH_KNOTS ( 'NONE', 3,
 ( #3114, #3421, #27490, #928, #26889, #13022 ),
 .UNSPECIFIED., .F., .F.,
 ( 4, 2, 4 ),
 ( 0.000000000000000000, 0.5000000000000000000, 1.000000000000000000 ),
 .UNSPECIFIED. ) ;
#8130=ADVANCED_FACE ( 'NONE', ( #11159 ), #7212, .F. ) ;
#8134=CARTESIAN_POINT ( 'NONE',  ( 10.99999999979999998, 21.69999999919999212, -70.09999999999999432 ) ) ;
#8148=CIRCLE ( 'NONE', #19226, 1.000000000000000888 ) ;
#8149=ORIENTED_EDGE ( 'NONE', *, *, #12638, .T. ) ;
#8159=DIRECTION ( 'NONE',  ( 0.7071067811870476172, 0.000000000000000000, -0.7071067811860475283 ) ) ;
#8162=DIRECTION ( 'NONE',  ( 1.635844237846128888E-12, -0.6889064844606307414, -0.7248502298186121351 ) ) ;
#8163=CARTESIAN_POINT ( 'NONE',  ( -10.69999999989999928, 19.99999999999999645, -2.399999999999999467 ) ) ;
#8169=DIRECTION ( 'NONE',  ( 0.000000000000000000, 2.257145581549999994E-12, 1.000000000000000000 ) ) ;
#8199=AXIS2_PLACEMENT_3D ( 'NONE', #13140, #29822, #20388 ) ;
#8200=DIRECTION ( 'NONE',  ( -1.000000000000000000, 0.000000000000000000, 0.000000000000000000 ) ) ;
#8207=DIRECTION ( 'NONE',  ( 0.000000000000000000, -1.000000000000000000, 2.257145581549999994E-12 ) ) ;
#8208=ORIENTED_EDGE ( 'NONE', *, *, #1297, .T. ) ;
#8217=AXIS2_PLACEMENT_3D ( 'NONE', #2626, #7193, #30962 ) ;
#8218=ORIENTED_EDGE ( 'NONE', *, *, #28751, .F. ) ;
#8224=PLANE ( 'NONE',  #30555 ) ;
#8248=B_SPLINE_CURVE_WITH_KNOTS ( 'NONE', 3,
 ( #28956, #12426, #4889, #15104, #10077, #14799 ),
 .UNSPECIFIED., .F., .F.,
 ( 4, 2, 4 ),
 ( 0.000000000000000000, 0.5000000000000000000, 1.000000000000000000 ),
 .UNSPECIFIED. ) ;
#8251=ORIENTED_EDGE ( 'NONE', *, *, #5539, .F. ) ;
#8258=CARTESIAN_POINT ( 'NONE',  ( -10.46446609379999870, 21.70000000000000284, -54.63553390589999736 ) ) ;
#8269=EDGE_CURVE ( 'NONE', #15738, #18576, #24201, .T. ) ;
#8285=CARTESIAN_POINT ( 'NONE',  ( 9.999999999968624209, -29.62135916550975168, -29.91085694027753306 ) ) ;
#8298=CARTESIAN_POINT ( 'NONE',  ( -10.69999999999999929, -27.00000000000000000, -31.39999999999999858 ) ) ;
#8308=DIRECTION ( 'NONE',  ( 1.000000000000000000, 0.000000000000000000, 0.000000000000000000 ) ) ;
#8311=DIRECTION ( 'NONE',  ( 2.966217977826874882E-25, -1.000000000000000000, 2.257145581549900232E-12 ) ) ;
#8322=DIRECTION ( 'NONE',  ( 0.9915824307782121760, 0.1294769592320275942, -4.045530494348897360E-18 ) ) ;
#8324=DIRECTION ( 'NONE',  ( -1.000000000000000000, 0.000000000000000000, 0.000000000000000000 ) ) ;
#8333=FACE_OUTER_BOUND ( 'NONE', #22068, .T. ) ;
#8339=ORIENTED_EDGE ( 'NONE', *, *, #15827, .T. ) ;
#8341=EDGE_CURVE ( 'NONE', #23857, #27091, #5613, .T. ) ;
#8343=DIRECTION ( 'NONE',  ( 0.000000000000000000, 0.000000000000000000, -1.000000000000000000 ) ) ;
#8347=CARTESIAN_POINT ( 'NONE',  ( 8.999999999770000869, 21.70000000000000284, -57.60000000000000142 ) ) ;
#8351=DIRECTION ( 'NONE',  ( 1.020425574104003999E-15, 0.000000000000000000, -1.000000000000000000 ) ) ;
#8366=DIRECTION ( 'NONE',  ( 0.000000000000000000, 0.000000000000000000, 1.000000000000000000 ) ) ;
#8376=CARTESIAN_POINT ( 'NONE',  ( 8.999999999770000869, 20.99999999999999645, -51.10000000000000142 ) ) ;
#8380=CARTESIAN_POINT ( 'NONE',  ( 10.00000000000000000, -130.0000000000000000, -42.39999999999999858 ) ) ;
#8410=CARTESIAN_POINT ( 'NONE',  ( 10.35000000039999968, 19.99999999999999645, -42.39999999999999858 ) ) ;
#8425=VECTOR ( 'NONE', #28822, 1000.000000000000000 ) ;
#8426=CARTESIAN_POINT ( 'NONE',  ( 18.27566665216736297, 11.02535689755138115, -1.400000000000001910 ) ) ;
#8430=ORIENTED_EDGE ( 'NONE', *, *, #6413, .T. ) ;
#8458=ORIENTED_EDGE ( 'NONE', *, *, #25765, .T. ) ;
#8464=EDGE_CURVE ( 'NONE', #15501, #3166, #6245, .T. ) ;
#8472=EDGE_LOOP ( 'NONE', ( #3082, #25232, #17267, #4376 ) ) ;
#8477=CYLINDRICAL_SURFACE ( 'NONE', #11687, 3.000000000000000444 ) ;
#8487=DIRECTION ( 'NONE',  ( -1.000000000000000000, 0.000000000000000000, 0.000000000000000000 ) ) ;
#8493=LINE ( 'NONE', #3793, #15012 ) ;
#8502=DIRECTION ( 'NONE',  ( 0.000000000000000000, 1.000000000000000000, 0.000000000000000000 ) ) ;
#8505=CARTESIAN_POINT ( 'NONE',  ( 10.35000000039999968, -130.0000000000000000, -42.39999999999999858 ) ) ;
#8511=DIRECTION ( 'NONE',  ( 0.000000000000000000, -1.000000000000000000, 0.000000000000000000 ) ) ;
#8513=CARTESIAN_POINT ( 'NONE',  ( -10.46447140189999914, 20.99999999999999645, -54.63552859760000047 ) ) ;
#8517=CARTESIAN_POINT ( 'NONE',  ( 10.69999999999999929, -43.95328087560000085, -27.24755286599999948 ) ) ;
#8521=CARTESIAN_POINT ( 'NONE',  ( 0.000000000000000000, 21.70000000000000284, -44.10000000017312516 ) ) ;
#8526=ORIENTED_EDGE ( 'NONE', *, *, #3269, .T. ) ;
#8527=EDGE_CURVE ( 'NONE', #26138, #13706, #13534, .T. ) ;
#8533=EDGE_CURVE ( 'NONE', #28636, #5828, #24740, .T. ) ;
#8535=CARTESIAN_POINT ( 'NONE',  ( 10.71199981179999838, 19.99999999999999645, -2.204042935800003100 ) ) ;
#8540=VERTEX_POINT ( 'NONE', #689 ) ;
#8547=CARTESIAN_POINT ( 'NONE',  ( 16.20123158609999692, 11.52736809249999617, -0.7999999992999995424 ) ) ;
#8563=CARTESIAN_POINT ( 'NONE',  ( -11.69999999989999928, -24.11120071670000087, -0.6999999999999992895 ) ) ;
#8576=ORIENTED_EDGE ( 'NONE', *, *, #2925, .F. ) ;
#8582=EDGE_CURVE ( 'NONE', #28608, #2437, #30943, .T. ) ;
#8584=FACE_OUTER_BOUND ( 'NONE', #28042, .T. ) ;
#8587=DIRECTION ( 'NONE',  ( -2.965499939100700266E-25, -1.000000000000000000, 2.257145581549900232E-12 ) ) ;
#8589=CARTESIAN_POINT ( 'NONE',  ( -9.000000000229999131, 20.99999999999999645, -56.09999999999999432 ) ) ;
#8597=CYLINDRICAL_SURFACE ( 'NONE', #25204, 3.000000000000000444 ) ;
#8598=CARTESIAN_POINT ( 'NONE',  ( -15.86808677770000209, -9.527368092500001495, -0.7000000003999986564 ) ) ;
#8606=FACE_OUTER_BOUND ( 'NONE', #10678, .T. ) ;
#8616=ORIENTED_EDGE ( 'NONE', *, *, #4999, .F. ) ;
#8620=DIRECTION ( 'NONE',  ( 0.000000000000000000, 0.000000000000000000, -1.000000000000000000 ) ) ;
#8624=DIRECTION ( 'NONE',  ( 0.000000000000000000, 0.000000000000000000, -1.000000000000000000 ) ) ;
#8648=DIRECTION ( 'NONE',  ( 0.000000000000000000, -1.000000000000000000, 0.000000000000000000 ) ) ;
#8651=CARTESIAN_POINT ( 'NONE',  ( 9.000000000000000000, -130.0000000000000000, -42.39999999999999858 ) ) ;
#8655=SHAPE_REPRESENTATION_RELATIONSHIP ( 'NONE' , 'NONE' ,  #25228, #4675 ) ;
#8678=EDGE_CURVE ( 'NONE', #30538, #23803, #27976, .T. ) ;
#8681=ORIENTED_EDGE ( 'NONE', *, *, #22943, .F. ) ;
#8690=CARTESIAN_POINT ( 'NONE',  ( 10.99289321870000080, 19.99999999999999645, -1.692893218799999877 ) ) ;
#8697=DIRECTION ( 'NONE',  ( -0.000000000000000000, 1.000000000000000000, -2.257145581549999994E-12 ) ) ;
#8702=AXIS2_PLACEMENT_3D ( 'NONE', #30216, #25187, #10876 ) ;
#8709=CARTESIAN_POINT ( 'NONE',  ( -13.99999999969999820, 20.99999999999999645, -58.51619611000000276 ) ) ;
#8710=EDGE_CURVE ( 'NONE', #22335, #29610, #29241, .T. ) ;
#8722=DIRECTION ( 'NONE',  ( -1.000000000000000000, 0.000000000000000000, 0.000000000000000000 ) ) ;
#8740=ORIENTED_EDGE ( 'NONE', *, *, #21680, .T. ) ;
#8743=CARTESIAN_POINT ( 'NONE',  ( -11.02757632650000019, -24.42656469639999983, -0.8308237180999975546 ) ) ;
#8745=VECTOR ( 'NONE', #28596, 1000.000000000000000 ) ;
#8747=DIRECTION ( 'NONE',  ( 1.000000000000000000, 0.000000000000000000, 0.000000000000000000 ) ) ;
#8761=CYLINDRICAL_SURFACE ( 'NONE', #27580, 0.9999999999999988898 ) ;
#8765=CARTESIAN_POINT ( 'NONE',  ( 10.00166578780910065, 20.99999999999306155, -54.17273359987459003 ) ) ;
#8771=DIRECTION ( 'NONE',  ( 0.000000000000000000, -1.000000000000000000, 0.000000000000000000 ) ) ;
#8777=EDGE_CURVE ( 'NONE', #15341, #24264, #29204, .T. ) ;
#8784=CARTESIAN_POINT ( 'NONE',  ( -17.83928249649999742, 19.99999999999999645, -1.049999999600002898 ) ) ;
#8785=CARTESIAN_POINT ( 'NONE',  ( -9.974508415446116771, -129.9999999999999716, -42.66064002661978094 ) ) ;
#8792=VECTOR ( 'NONE', #520, 1000.000000000000000 ) ;
#8801=LINE ( 'NONE', #6599, #22280 ) ;
#8805=AXIS2_PLACEMENT_3D ( 'NONE', #26342, #19568, #12327 ) ;
#8807=PLANE ( 'NONE',  #25312 ) ;
#8813=CARTESIAN_POINT ( 'NONE',  ( -10.00000000009948309, -128.1247626082301565, -35.28103264363292624 ) ) ;
#8814=ORIENTED_EDGE ( 'NONE', *, *, #17463, .F. ) ;
#8819=ORIENTED_EDGE ( 'NONE', *, *, #10504, .T. ) ;
#8826=FACE_OUTER_BOUND ( 'NONE', #22254, .T. ) ;
#8843=ORIENTED_EDGE ( 'NONE', *, *, #27536, .T. ) ;
#8855=DIRECTION ( 'NONE',  ( 2.256992747040000044E-12, -0.000000000000000000, -1.000000000000000000 ) ) ;
#8864=EDGE_CURVE ( 'NONE', #21489, #25001, #3707, .T. ) ;
#8866=ORIENTED_EDGE ( 'NONE', *, *, #5539, .T. ) ;
#8867=CARTESIAN_POINT ( 'NONE',  ( 11.02757639490000052, -24.42656466549999905, -0.8308236885000014338 ) ) ;
#8872=VERTEX_POINT ( 'NONE', #24959 ) ;
#8873=DIRECTION ( 'NONE',  ( 1.000000000000000000, 3.757855673434259506E-24, -2.257150022441365115E-12 ) ) ;
#8874=CARTESIAN_POINT ( 'NONE',  ( -10.69999999999999929, -130.0000000000000000, -41.24671599790000442 ) ) ;
#8889=( GEOMETRIC_REPRESENTATION_CONTEXT ( 3 ) GLOBAL_UNCERTAINTY_ASSIGNED_CONTEXT ( ( #15067 ) ) GLOBAL_UNIT_ASSIGNED_CONTEXT ( ( #19091, #7438, #7739 ) ) REPRESENTATION_CONTEXT ( 'NONE', 'WORKASPACE' ) );
#8890=DIRECTION ( 'NONE',  ( 0.000000000000000000, -2.256505319260000033E-12, -1.000000000000000000 ) ) ;
#8897=ORIENTED_EDGE ( 'NONE', *, *, #1516, .T. ) ;
#8898=EDGE_CURVE ( 'NONE', #10599, #9943, #22292, .T. ) ;
#8910=PLANE ( 'NONE',  #10509 ) ;
#8915=VECTOR ( 'NONE', #19008, 1000.000000000000000 ) ;
#8919=VECTOR ( 'NONE', #2877, 1000.000000000000000 ) ;
#8927=EDGE_CURVE ( 'NONE', #23122, #20043, #10867, .T. ) ;
#8929=ORIENTED_EDGE ( 'NONE', *, *, #25405, .T. ) ;
#8931=DIRECTION ( 'NONE',  ( 0.000000000000000000, 1.000000000000000000, 0.000000000000000000 ) ) ;
#8956=EDGE_CURVE ( 'NONE', #22879, #10748, #28138, .T. ) ;
#8961=EDGE_CURVE ( 'NONE', #20043, #30907, #22607, .T. ) ;
#8966=DIRECTION ( 'NONE',  ( -1.000000000000000000, 0.000000000000000000, 0.000000000000000000 ) ) ;
#8971=VERTEX_POINT ( 'NONE', #15202 ) ;
#9011=VECTOR ( 'NONE', #17036, 1000.000000000000000 ) ;
#9027=CARTESIAN_POINT ( 'NONE',  ( 10.79767714369999965, -24.52928866599999935, -0.9448357716000042039 ) ) ;
#9034=DIRECTION ( 'NONE',  ( 1.000000000000000000, 0.000000000000000000, 0.000000000000000000 ) ) ;
#9036=EDGE_CURVE ( 'NONE', #2487, #6694, #11589, .T. ) ;
#9046=EDGE_CURVE ( 'NONE', #28677, #29912, #2614, .T. ) ;
#9048=EDGE_CURVE ( 'NONE', #17900, #11176, #11421, .T. ) ;
#9049=DIRECTION ( 'NONE',  ( -5.551115123049999208E-18, 0.000000000000000000, -1.000000000000000000 ) ) ;
#9052=ORIENTED_EDGE ( 'NONE', *, *, #7700, .T. ) ;
#9053=FACE_BOUND ( 'NONE', #10376, .T. ) ;
#9057=ADVANCED_FACE ( 'NONE', ( #9053, #1989, #21024 ), #26057, .T. ) ;
#9062=FACE_OUTER_BOUND ( 'NONE', #21284, .T. ) ;
#9067=DIRECTION ( 'NONE',  ( 0.000000000000000000, 2.255973186040000320E-12, 1.000000000000000000 ) ) ;
#9068=ORIENTED_EDGE ( 'NONE', *, *, #15047, .F. ) ;
#9070=CARTESIAN_POINT ( 'NONE',  ( -10.69999999999999929, 19.99999999999999645, -42.39999999999999858 ) ) ;
#9081=CARTESIAN_POINT ( 'NONE',  ( 9.130136616458420562, 20.99999999999704059, -52.40873942179641887 ) ) ;
#9090=DIRECTION ( 'NONE',  ( -9.982533390641031007E-25, -1.000000000000000000, 2.257145581550764975E-12 ) ) ;
#9102=EDGE_LOOP ( 'NONE', ( #3503, #25090, #7993, #11188 ) ) ;
#9125=( NAMED_UNIT ( * ) PLANE_ANGLE_UNIT ( ) SI_UNIT ( $, .RADIAN. ) );
#9127=CARTESIAN_POINT ( 'NONE',  ( -11.69999999989999928, -2.500000000000002220, -2.399999999999999467 ) ) ;
#9133=LINE ( 'NONE', #21424, #28657 ) ;
#9141=FACE_OUTER_BOUND ( 'NONE', #1055, .T. ) ;
#9142=PRODUCT ( 'Handle Housing', 'Handle Housing', '', ( #25514 ) ) ;
#9145=CARTESIAN_POINT ( 'NONE',  ( 2.910560681360000016E-11, 19.99999999999999645, -45.10000000000000142 ) ) ;
#9150=LINE ( 'NONE', #21127, #19340 ) ;
#9154=EDGE_LOOP ( 'NONE', ( #30693, #8218, #20397, #7876 ) ) ;
#9182=DIRECTION ( 'NONE',  ( -1.000000000000000000, 0.000000000000000000, 0.000000000000000000 ) ) ;
#9187=PLANE ( 'NONE',  #12962 ) ;
#9203=ORIENTED_EDGE ( 'NONE', *, *, #23887, .F. ) ;
#9210=CARTESIAN_POINT ( 'NONE',  ( 9.989498421329999545, 19.99999999999999645, -42.57860042107999732 ) ) ;
#9216=EDGE_CURVE ( 'NONE', #19078, #7630, #7459, .T. ) ;
#9228=ADVANCED_FACE ( 'NONE', ( #2595 ), #17213, .F. ) ;
#9231=DIRECTION ( 'NONE',  ( 0.000000000000000000, 0.000000000000000000, -1.000000000000000000 ) ) ;
#9255=DIRECTION ( 'NONE',  ( 0.000000000000000000, 2.259525899719999991E-12, 1.000000000000000000 ) ) ;
#9263=AXIS2_PLACEMENT_3D ( 'NONE', #13411, #8366, #3979 ) ;
#9266=VECTOR ( 'NONE', #22360, 1000.000000000000000 ) ;
#9276=AXIS2_PLACEMENT_3D ( 'NONE', #7448, #9499, #19100 ) ;
#9281=VERTEX_POINT ( 'NONE', #3355 ) ;
#9285=ORIENTED_EDGE ( 'NONE', *, *, #12162, .T. ) ;
#9292=CARTESIAN_POINT ( 'NONE',  ( -10.35000000009999965, -130.0000000000000000, -42.40000000045999684 ) ) ;
#9297=CARTESIAN_POINT ( 'NONE',  ( -8.999999999883337765, 20.99999999999999645, -44.83820061220109210 ) ) ;
#9311=CARTESIAN_POINT ( 'NONE',  ( -22.38914258936776491, -14.77116484369720339, -1.399999999999998579 ) ) ;
#9312=ORIENTED_EDGE ( 'NONE', *, *, #4885, .T. ) ;
#9314=EDGE_LOOP ( 'NONE', ( #3208, #23603, #3510, #25476 ) ) ;
#9317=ORIENTED_EDGE ( 'NONE', *, *, #16848, .T. ) ;
#9331=PRESENTATION_STYLE_ASSIGNMENT (( #14066 ) ) ;
#9335=ORIENTED_EDGE ( 'NONE', *, *, #7893, .F. ) ;
#9336=CARTESIAN_POINT ( 'NONE',  ( 11.69999999989999928, -24.11120071670000087, -0.6999999999999992895 ) ) ;
#9340=ORIENTED_EDGE ( 'NONE', *, *, #28092, .T. ) ;
#9346=CARTESIAN_POINT ( 'NONE',  ( 9.999999999959999997, -24.95051888640000115, -26.20881396970000310 ) ) ;
#9349=CARTESIAN_POINT ( 'NONE',  ( -10.69999999999999929, -24.03509441459999962, -28.95432817779999723 ) ) ;
#9364=CARTESIAN_POINT ( 'NONE',  ( -9.999999999909999104, -2.500000000000002220, -2.399999999999999467 ) ) ;
#9365=DIRECTION ( 'NONE',  ( 0.000000000000000000, -1.000000000000000000, 2.257145581549999994E-12 ) ) ;
#9366=DIRECTION ( 'NONE',  ( 2.965499939100700266E-25, -1.000000000000000000, 2.257145581549900232E-12 ) ) ;
#9369=CARTESIAN_POINT ( 'NONE',  ( -10.00000000050000004, -29.23060343719999921, -26.39054106440000069 ) ) ;
#9370=VERTEX_POINT ( 'NONE', #27130 ) ;
#9373=PLANE ( 'NONE',  #17287 ) ;
#9374=FACE_OUTER_BOUND ( 'NONE', #6829, .T. ) ;
#9377=CARTESIAN_POINT ( 'NONE',  ( 10.89131017080000063, -24.86557399950000047, -1.811764705399995901 ) ) ;
#9380=CARTESIAN_POINT ( 'NONE',  ( 17.16657240420000008, -9.000000000000001776, -0.8000000000000020428 ) ) ;
#9384=EDGE_CURVE ( 'NONE', #24262, #11888, #22842, .T. ) ;
#9390=B_SPLINE_CURVE_WITH_KNOTS ( 'NONE', 3,
 ( #18949, #21473, #4332, #26195, #11715, #25736 ),
 .UNSPECIFIED., .F., .F.,
 ( 4, 2, 4 ),
 ( 0.000000000000000000, 0.5000000000000000000, 1.000000000000000000 ),
 .UNSPECIFIED. ) ;
#9398=VERTEX_POINT ( 'NONE', #15166 ) ;
#9400=EDGE_LOOP ( 'NONE', ( #28401, #18922, #20863, #20723 ) ) ;
#9403=CARTESIAN_POINT ( 'NONE',  ( 9.620427249210001364, 19.99999999999999645, -43.18760499467699532 ) ) ;
#9404=AXIS2_PLACEMENT_3D ( 'NONE', #22460, #17259, #17867 ) ;
#9406=AXIS2_PLACEMENT_3D ( 'NONE', #18222, #8624, #15882 ) ;
#9412=ORIENTED_EDGE ( 'NONE', *, *, #7586, .T. ) ;
#9420=EDGE_CURVE ( 'NONE', #9747, #24348, #27433, .T. ) ;
#9425=CARTESIAN_POINT ( 'NONE',  ( -10.99999999969999998, 21.69999999919999212, -70.09999999999999432 ) ) ;
#9428=CARTESIAN_POINT ( 'NONE',  ( -9.999999999909999104, 19.99999999999999645, -2.399999999999999467 ) ) ;
#9433=ADVANCED_FACE ( 'NONE', ( #22882 ), #19900, .F. ) ;
#9444=CARTESIAN_POINT ( 'NONE',  ( -10.35000000039999968, -130.0000000000000000, -41.24671599790000442 ) ) ;
#9448=AXIS2_PLACEMENT_3D ( 'NONE', #12466, #4351, #24439 ) ;
#9461=DIRECTION ( 'NONE',  ( 0.000000000000000000, 0.000000000000000000, 1.000000000000000000 ) ) ;
#9479=ORIENTED_EDGE ( 'NONE', *, *, #15863, .F. ) ;
#9480=CIRCLE ( 'NONE', #21547, 0.9999999999999991118 ) ;
#9481=VERTEX_POINT ( 'NONE', #1487 ) ;
#9489=VERTEX_POINT ( 'NONE', #28375 ) ;
#9494=VERTEX_POINT ( 'NONE', #6350 ) ;
#9499=DIRECTION ( 'NONE',  ( 0.000000000000000000, 0.000000000000000000, -1.000000000000000000 ) ) ;
#9504=FACE_OUTER_BOUND ( 'NONE', #21447, .T. ) ;
#9507=DIRECTION ( 'NONE',  ( 1.000000000000000000, 5.998481157687279274E-24, -2.257150022441830001E-12 ) ) ;
#9512=CARTESIAN_POINT ( 'NONE',  ( 10.69999999999999929, -127.2537437101000108, -34.36317024011000143 ) ) ;
#9514=VERTEX_POINT ( 'NONE', #16103 ) ;
#9515=CARTESIAN_POINT ( 'NONE',  ( -10.00000000052381743, -27.78524365307784549, -31.32191803000652186 ) ) ;
#9530=VECTOR ( 'NONE', #28723, 1000.000000000000000 ) ;
#9533=DIRECTION ( 'NONE',  ( -0.8086898285215826654, 0.000000000000000000, 0.5882352941176968164 ) ) ;
#9538=CARTESIAN_POINT ( 'NONE',  ( 12.84364015881248733, 20.99999999989936228, -69.49900052785271498 ) ) ;
#9540=ORIENTED_EDGE ( 'NONE', *, *, #8341, .F. ) ;
#9541=CYLINDRICAL_SURFACE ( 'NONE', #20533, 2.999999999999999556 ) ;
#9544=CARTESIAN_POINT ( 'NONE',  ( -4.175165894169885483, -119.7166638525666826, -63.39999999999999858 ) ) ;
#9550=LINE ( 'NONE', #14432, #20650 ) ;
#9556=B_SPLINE_CURVE_WITH_KNOTS ( 'NONE', 5,
 ( #30075, #5382, #14990, #19871, #17491, #4108 ),
 .UNSPECIFIED., .F., .F.,
 ( 6, 6 ),
 ( 3.338999440259999840, 3.575680517940000414 ),
 .UNSPECIFIED. ) ;
#9561=ORIENTED_EDGE ( 'NONE', *, *, #1297, .F. ) ;
#9565=DIRECTION ( 'NONE',  ( 0.000000000000000000, 1.000000000000000000, 0.000000000000000000 ) ) ;
#9578=CARTESIAN_POINT ( 'NONE',  ( -9.999999999969999109, -120.5233595632000174, -31.26042064989999858 ) ) ;
#9582=CARTESIAN_POINT ( 'NONE',  ( -10.00134423289999930, -25.00000000000000000, -2.314486209600001398 ) ) ;
#9586=LINE ( 'NONE', #26269, #23804 ) ;
#9588=DIRECTION ( 'NONE',  ( -0.7071067811865475727, 1.595945597898661921E-12, 0.7071067811865475727 ) ) ;
#9589=EDGE_CURVE ( 'NONE', #23628, #20876, #4061, .T. ) ;
#9594=DIRECTION ( 'NONE',  ( 0.8775825618903718706, -0.4794255386042047262, 0.000000000000000000 ) ) ;
#9595=ORIENTED_EDGE ( 'NONE', *, *, #27014, .F. ) ;
#9599=ORIENTED_EDGE ( 'NONE', *, *, #28493, .F. ) ;
#9601=EDGE_LOOP ( 'NONE', ( #3468, #26808, #522, #11651, #7811 ) ) ;
#9604=CARTESIAN_POINT ( 'NONE',  ( -9.000000000000000000, -130.0000000000000000, -43.39999999999999858 ) ) ;
#9611=CARTESIAN_POINT ( 'NONE',  ( -16.83342759579999637, -9.000000000000001776, -0.8000000000000020428 ) ) ;
#9618=ADVANCED_FACE ( 'NONE', ( #2562 ), #19555, .F. ) ;
#9621=EDGE_CURVE ( 'NONE', #17104, #23118, #12149, .T. ) ;
#9627=FACE_OUTER_BOUND ( 'NONE', #3157, .T. ) ;
#9631=LINE ( 'NONE', #4455, #27394 ) ;
#9632=CARTESIAN_POINT ( 'NONE',  ( 13.15526517074354196, 21.70000000000177209, -56.37750224591909642 ) ) ;
#9636=ORIENTED_EDGE ( 'NONE', *, *, #8864, .F. ) ;
#9637=CARTESIAN_POINT ( 'NONE',  ( 0.000000000000000000, 19.99999999999999645, -44.10000000000000142 ) ) ;
#9638=EDGE_CURVE ( 'NONE', #23803, #23190, #2865, .T. ) ;
#9671=ORIENTED_EDGE ( 'NONE', *, *, #15322, .F. ) ;
#9685=CARTESIAN_POINT ( 'NONE',  ( 9.999488386939999529, 19.99999999999999645, -42.44046182635000264 ) ) ;
#9694=DIRECTION ( 'NONE',  ( 0.000000000000000000, -1.000000000000000000, 0.000000000000000000 ) ) ;
#9697=B_SPLINE_CURVE_WITH_KNOTS ( 'NONE', 3,
 ( #15485, #3212, #22424, #868 ),
 .UNSPECIFIED., .F., .F.,
 ( 4, 4 ),
 ( 0.000000000000000000, 1.000000000000000000 ),
 .UNSPECIFIED. ) ;
#9703=DIRECTION ( 'NONE',  ( 1.000000000000000000, 0.000000000000000000, 0.000000000000000000 ) ) ;
#9707=LINE ( 'NONE', #4841, #25841 ) ;
#9719=CARTESIAN_POINT ( 'NONE',  ( 12.41901213044714680, 20.99999999997343636, -55.86814804320044914 ) ) ;
#9724=CARTESIAN_POINT ( 'NONE',  ( 4.175165894169885483, -55.00000000000000000, -44.10000000000000142 ) ) ;
#9730=DIRECTION ( 'NONE',  ( 1.000000000000000000, 0.000000000000000000, -2.257150022439999944E-12 ) ) ;
#9734=CARTESIAN_POINT ( 'NONE',  ( 10.69999999999827622, -26.63513617188653626, -25.40000000000000213 ) ) ;
#9736=CARTESIAN_POINT ( 'NONE',  ( 13.99999999979999821, 21.69999999929999390, -58.51619795559999915 ) ) ;
#9738=VECTOR ( 'NONE', #8771, 1000.000000000000000 ) ;
#9739=CIRCLE ( 'NONE', #27327, 1.700000000000000178 ) ;
#9743=VECTOR ( 'NONE', #19929, 1000.000000000000000 ) ;
#9747=VERTEX_POINT ( 'NONE', #7882 ) ;
#9750=ORIENTED_EDGE ( 'NONE', *, *, #11880, .F. ) ;
#9759=CARTESIAN_POINT ( 'NONE',  ( 10.69999999999999929, -27.00000000000000000, -28.40000000000000213 ) ) ;
#9764=DIRECTION ( 'NONE',  ( -0.8775825618903718706, 0.4794255386042047262, 0.000000000000000000 ) ) ;
#9775=B_SPLINE_CURVE_WITH_KNOTS ( 'NONE', 3,
 ( #11238, #23206, #24935, #25413 ),
 .UNSPECIFIED., .F., .F.,
 ( 4, 4 ),
 ( -0.08350576075630000705, 0.08350576075630000705 ),
 .UNSPECIFIED. ) ;
#9788=ADVANCED_FACE ( 'NONE', ( #13546 ), #1755, .F. ) ;
#9795=ORIENTED_EDGE ( 'NONE', *, *, #27996, .T. ) ;
#9806=CARTESIAN_POINT ( 'NONE',  ( -13.12132034329999897, 20.99999999990000887, -69.22132034359999864 ) ) ;
#9813=CARTESIAN_POINT ( 'NONE',  ( -1.110223024630000146E-16, 0.000000000000000000, -43.39999999999999858 ) ) ;
#9816=DIRECTION ( 'NONE',  ( 1.000000000000000000, -0.000000000000000000, -2.257150022439999944E-12 ) ) ;
#9817=AXIS2_PLACEMENT_3D ( 'NONE', #10708, #16055, #22671 ) ;
#9824=VERTEX_POINT ( 'NONE', #25982 ) ;
#9846=CARTESIAN_POINT ( 'NONE',  ( 11.49999999979999998, 20.99999999990000887, -70.09999999999999432 ) ) ;
#9853=CARTESIAN_POINT ( 'NONE',  ( 10.69999999998290008, -127.6903210698857549, -34.82346581440141620 ) ) ;
#9854=DIRECTION ( 'NONE',  ( 0.000000000000000000, 0.000000000000000000, -1.000000000000000000 ) ) ;
#9857=LINE ( 'NONE', #10168, #22810 ) ;
#9864=ORIENTED_EDGE ( 'NONE', *, *, #17117, .F. ) ;
#9866=CARTESIAN_POINT ( 'NONE',  ( -12.36097874953984466, 21.69999999999976836, -55.83956240900247536 ) ) ;
#9899=LINE ( 'NONE', #318, #16298 ) ;
#9905=CARTESIAN_POINT ( 'NONE',  ( 9.999999999975235809, -125.3357287891403757, -32.69504109670850767 ) ) ;
#9906=EDGE_LOOP ( 'NONE', ( #16697, #30884, #10641, #24962 ) ) ;
#9943=VERTEX_POINT ( 'NONE', #6927 ) ;
#9962=CARTESIAN_POINT ( 'NONE',  ( 16.20123158609999692, -8.472631907500000281, -0.7999999992999995424 ) ) ;
#9963=CIRCLE ( 'NONE', #24029, 26.80000000000000071 ) ;
#9965=LINE ( 'NONE', #7293, #5910 ) ;
#9972=CARTESIAN_POINT ( 'NONE',  ( 11.78484171507088085, 21.69999999994148965, -70.02227941812002143 ) ) ;
#9973=LINE ( 'NONE', #23993, #25364 ) ;
#9987=EDGE_LOOP ( 'NONE', ( #4495, #22096, #12662, #19433 ) ) ;
#9988=CARTESIAN_POINT ( 'NONE',  ( 10.69999999997181028, -24.37874960104799626, -29.91132621206058317 ) ) ;
#9994=FACE_OUTER_BOUND ( 'NONE', #27441, .T. ) ;
#10004=CARTESIAN_POINT ( 'NONE',  ( 10.69999999999999929, -36.62914859500000375, -26.86371135770000151 ) ) ;
#10008=CARTESIAN_POINT ( 'NONE',  ( -10.69999999930000101, -30.49251257979999963, -21.04205368470000082 ) ) ;
#10009=FACE_OUTER_BOUND ( 'NONE', #1524, .T. ) ;
#10015=DIRECTION ( 'NONE',  ( -0.000000000000000000, 1.000000000000000000, -2.255973188440000244E-12 ) ) ;
#10016=EDGE_CURVE ( 'NONE', #23190, #15903, #13464, .T. ) ;
#10027=CARTESIAN_POINT ( 'NONE',  ( 0.000000000000000000, 20.70710678120000381, -44.39289321881399530 ) ) ;
#10052=B_SPLINE_SURFACE_WITH_KNOTS ( 'NONE', 5, 1, ( 
 ( #18485, #30132 ),
 ( #3536, #27767 ),
 ( #29970, #10625 ),
 ( #6528, #10783 ),
 ( #20379, #29812 ),
 ( #22905, #18330 ),
 ( #6054, #23065 ),
 ( #25261, #3693 ),
 ( #15820, #13296 ),
 ( #1345, #27933 ),
 ( #3858, #1508 ),
 ( #11100, #6374 ) ),
 .UNSPECIFIED., .F., .F., .F.,
 ( 6, 3, 3, 6 ),
 ( 2, 2 ),
 ( 0.000000000000000000, 0.5717440563379999618, 1.143488112680000057, 1.429360140840000071 ),
 ( -0.7000000000009999335, 0.002002273473629999963 ),
 .UNSPECIFIED. ) ;
#10060=LINE ( 'NONE', #21556, #16282 ) ;
#10064=CARTESIAN_POINT ( 'NONE',  ( -10.00000000026539126, -35.47767383571155619, -24.90806880955480551 ) ) ;
#10067=ORIENTED_EDGE ( 'NONE', *, *, #8927, .T. ) ;
#10070=B_SPLINE_CURVE_WITH_KNOTS ( 'NONE', 3,
 ( #723, #27293, #1178, #10468 ),
 .UNSPECIFIED., .F., .F.,
 ( 4, 4 ),
 ( 0.000000000000000000, 1.000000000000000000 ),
 .UNSPECIFIED. ) ;
#10075=CARTESIAN_POINT ( 'NONE',  ( -10.79767709090000061, -24.52928868880000124, -0.9448358073000027169 ) ) ;
#10077=CARTESIAN_POINT ( 'NONE',  ( 9.999999999966270536, -29.52728889296171744, -26.74669651331937104 ) ) ;
#10080=EDGE_CURVE ( 'NONE', #20395, #15903, #6389, .T. ) ;
#10107=ORIENTED_EDGE ( 'NONE', *, *, #19213, .F. ) ;
#10118=EDGE_CURVE ( 'NONE', #11243, #24111, #18502, .T. ) ;
#10120=CARTESIAN_POINT ( 'NONE',  ( 4.175165894169885483, -119.7166638525666826, -43.39999999999999858 ) ) ;
#10131=DIRECTION ( 'NONE',  ( -1.000000000000000000, 0.000000000000000000, 0.000000000000000000 ) ) ;
#10133=CARTESIAN_POINT ( 'NONE',  ( -13.99999999969999820, 21.69999999929999390, -67.09999999999999432 ) ) ;
#10139=ORIENTED_EDGE ( 'NONE', *, *, #11548, .T. ) ;
#10164=CARTESIAN_POINT ( 'NONE',  ( 9.999999999962405184, -25.59333594965072223, -25.74355301541976360 ) ) ;
#10168=CARTESIAN_POINT ( 'NONE',  ( -10.32522729140000095, -24.86557399950000047, -1.399999999999998579 ) ) ;
#10177=CARTESIAN_POINT ( 'NONE',  ( 11.69999999989999928, -24.11120071670000087, -1.399999999999998579 ) ) ;
#10183=ORIENTED_EDGE ( 'NONE', *, *, #8533, .F. ) ;
#10204=VECTOR ( 'NONE', #29469, 1000.000000000000000 ) ;
#10207=CARTESIAN_POINT ( 'NONE',  ( -10.69999999999999929, -126.5194192958999935, -33.65254911369999746 ) ) ;
#10215=ORIENTED_EDGE ( 'NONE', *, *, #13092, .F. ) ;
#10216=AXIS2_PLACEMENT_3D ( 'NONE', #15267, #963, #10554 ) ;
#10222=ORIENTED_EDGE ( 'NONE', *, *, #5597, .T. ) ;
#10225=ORIENTED_EDGE ( 'NONE', *, *, #1388, .F. ) ;
#10227=VECTOR ( 'NONE', #14577, 1000.000000000000000 ) ;
#10228=ADVANCED_FACE ( 'NONE', ( #29331 ), #26518, .F. ) ;
#10231=CARTESIAN_POINT ( 'NONE',  ( 9.999999999899998215, -2.500000000000002220, -2.399999999999999467 ) ) ;
#10263=ADVANCED_FACE ( 'NONE', ( #2758 ), #5268, .F. ) ;
#10265=ORIENTED_EDGE ( 'NONE', *, *, #28555, .F. ) ;
#10267=LINE ( 'NONE', #20167, #25210 ) ;
#10273=AXIS2_PLACEMENT_3D ( 'NONE', #15696, #5946, #15237 ) ;
#10274=FACE_OUTER_BOUND ( 'NONE', #3680, .T. ) ;
#10285=CARTESIAN_POINT ( 'NONE',  ( 8.999999999770000869, 20.80003289834280977, -44.48586295459759299 ) ) ;
#10286=DIRECTION ( 'NONE',  ( -0.000000000000000000, -0.000000000000000000, 1.000000000000000000 ) ) ;
#10290=CIRCLE ( 'NONE', #5251, 26.80000000000000071 ) ;
#10299=ADVANCED_FACE ( 'NONE', ( #7168 ), #16754, .F. ) ;
#10302=EDGE_LOOP ( 'NONE', ( #29864, #13920, #3878, #9340, #21212, #25702, #6647 ) ) ;
#10312=CARTESIAN_POINT ( 'NONE',  ( -15.79905445585067270, 10.59899472511377816, -1.400000000000001910 ) ) ;
#10313=ORIENTED_EDGE ( 'NONE', *, *, #8956, .F. ) ;
#10321=ADVANCED_FACE ( 'NONE', ( #9994 ), #15027, .F. ) ;
#10328=CARTESIAN_POINT ( 'NONE',  ( 8.999999999540001738, 19.99999999999999645, -44.09999999970998630 ) ) ;
#10329=VECTOR ( 'NONE', #18435, 1000.000000000000000 ) ;
#10330=( GEOMETRIC_REPRESENTATION_CONTEXT ( 3 ) GLOBAL_UNCERTAINTY_ASSIGNED_CONTEXT ( ( #15338 ) ) GLOBAL_UNIT_ASSIGNED_CONTEXT ( ( #16215, #9125, #18575 ) ) REPRESENTATION_CONTEXT ( 'NONE', 'WORKASPACE' ) );
#10342=ORIENTED_EDGE ( 'NONE', *, *, #10016, .F. ) ;
#10345=CARTESIAN_POINT ( 'NONE',  ( 9.999999999979143794, -28.51085694194899389, -31.02135916461767096 ) ) ;
#10347=DIRECTION ( 'NONE',  ( 1.000000000000000000, 0.000000000000000000, 0.000000000000000000 ) ) ;
#10351=LINE ( 'NONE', #29537, #31109 ) ;
#10356=B_SPLINE_CURVE_WITH_KNOTS ( 'NONE', 3,
 ( #26484, #19564, #378, #7443 ),
 .UNSPECIFIED., .F., .F.,
 ( 4, 4 ),
 ( 0.000000000000000000, 1.000000000000000000 ),
 .UNSPECIFIED. ) ;
#10359=CARTESIAN_POINT ( 'NONE',  ( -10.69999999999999929, -130.0000000000000000, -41.24671599790000442 ) ) ;
#10360=CARTESIAN_POINT ( 'NONE',  ( 9.999999999969999109, -29.12127062269999911, -30.52127062070000107 ) ) ;
#10364=PLANE ( 'NONE',  #27308 ) ;
#10373=EDGE_CURVE ( 'NONE', #28151, #22644, #18253, .T. ) ;
#10376=EDGE_LOOP ( 'NONE', ( #22640, #23210, #15874, #7781 ) ) ;
#10377=ORIENTED_EDGE ( 'NONE', *, *, #10080, .F. ) ;
#10379=ORIENTED_EDGE ( 'NONE', *, *, #8961, .T. ) ;
#10388=LINE ( 'NONE', #21730, #14515 ) ;
#10389=FACE_OUTER_BOUND ( 'NONE', #7541, .T. ) ;
#10399=CARTESIAN_POINT ( 'NONE',  ( 9.999999999964241937, -24.59985587209093083, -26.55753809894806494 ) ) ;
#10403=EDGE_CURVE ( 'NONE', #6537, #17588, #17831, .T. ) ;
#10407=CARTESIAN_POINT ( 'NONE',  ( 10.92440694870000151, 19.99999999999999645, -0.8628532294999990970 ) ) ;
#10411=ORIENTED_EDGE ( 'NONE', *, *, #14851, .F. ) ;
#10420=LINE ( 'NONE', #29757, #6191 ) ;
#10443=DIRECTION ( 'NONE',  ( 1.000000000000000000, 0.000000000000000000, 0.000000000000000000 ) ) ;
#10459=MANIFOLD_SOLID_BREP ( 'PartBody', #29636 ) ;
#10461=ADVANCED_FACE ( 'NONE', ( #11854 ), #4313, .T. ) ;
#10463=LINE ( 'NONE', #5574, #19951 ) ;
#10468=CARTESIAN_POINT ( 'NONE',  ( 13.67718073920000066, 21.70000000000000284, -57.16242423349999768 ) ) ;
#10469=ADVANCED_FACE ( 'NONE', ( #4781 ), #23824, .F. ) ;
#10471=DIRECTION ( 'NONE',  ( 1.000000000000000000, 0.000000000000000000, 0.000000000000000000 ) ) ;
#10472=ORIENTED_EDGE ( 'NONE', *, *, #2315, .T. ) ;
#10493=ORIENTED_EDGE ( 'NONE', *, *, #16998, .F. ) ;
#10499=CARTESIAN_POINT ( 'NONE',  ( -10.96000317937597757, 21.69999999997520845, -55.08353444139804367 ) ) ;
#10501=CARTESIAN_POINT ( 'NONE',  ( -9.999999999969999109, -29.12127062080000073, -30.52127062269999769 ) ) ;
#10504=EDGE_CURVE ( 'NONE', #3911, #3826, #7591, .T. ) ;
#10509=AXIS2_PLACEMENT_3D ( 'NONE', #18512, #28114, #16460 ) ;
#10512=CARTESIAN_POINT ( 'NONE',  ( 12.12499541220000054, 20.99999999999999645, -55.73512219869999740 ) ) ;
#10517=CARTESIAN_POINT ( 'NONE',  ( -17.72973609203700462, 11.65373091001462669, -1.400000000000002132 ) ) ;
#10527=CARTESIAN_POINT ( 'NONE',  ( 0.000000000000000000, 0.000000000000000000, -44.00000000000000000 ) ) ;
#10531=ORIENTED_EDGE ( 'NONE', *, *, #26909, .F. ) ;
#10544=CARTESIAN_POINT ( 'NONE',  ( 10.69999999997381757, -28.84240556167032921, -30.80012576576890027 ) ) ;
#10545=DIRECTION ( 'NONE',  ( 0.000000000000000000, 1.000000000000000000, 0.000000000000000000 ) ) ;
#10554=DIRECTION ( 'NONE',  ( -0.000000000000000000, 1.000000000000000000, -2.257145581549999994E-12 ) ) ;
#10562=CARTESIAN_POINT ( 'NONE',  ( 0.000000000000000000, 20.99999999999999645, -44.10000000017154065 ) ) ;
#10564=ORIENTED_EDGE ( 'NONE', *, *, #17527, .T. ) ;
#10567=ADVANCED_FACE ( 'NONE', ( #28685 ), #375, .F. ) ;
#10587=CARTESIAN_POINT ( 'NONE',  ( 10.69999999996523243, -41.43508060205707721, -26.99581415663967121 ) ) ;
#10591=CARTESIAN_POINT ( 'NONE',  ( 10.89131017139999891, -24.73114799890000270, -1.811764705899998606 ) ) ;
#10599=VERTEX_POINT ( 'NONE', #20321 ) ;
#10602=ORIENTED_EDGE ( 'NONE', *, *, #5994, .T. ) ;
#10613=EDGE_LOOP ( 'NONE', ( #18923, #9595, #9671, #19163, #16218, #6852, #7657, #19963, #25221, #5424, #6572, #31044, #26745, #3756, #1781, #30099, #28963 ) ) ;
#10619=CARTESIAN_POINT ( 'NONE',  ( -10.69999999999999929, -29.30501631370000482, -26.47986984990000181 ) ) ;
#10625=CARTESIAN_POINT ( 'NONE',  ( -10.49243769149999927, -24.66097101990000340, -1.192453596599994725 ) ) ;
#10635=CARTESIAN_POINT ( 'NONE',  ( 11.48163258689999999, -24.28840541759999994, -1.419991652300001128 ) ) ;
#10639=DIRECTION ( 'NONE',  ( 1.000000000000000000, 0.000000000000000000, 0.000000000000000000 ) ) ;
#10641=ORIENTED_EDGE ( 'NONE', *, *, #25615, .T. ) ;
#10663=DIRECTION ( 'NONE',  ( -0.000000000000000000, 1.000000000000000000, -2.257145581549999994E-12 ) ) ;
#10673=CARTESIAN_POINT ( 'NONE',  ( 13.12132034340000075, 21.69999999990000106, -69.22132034359999864 ) ) ;
#10675=ORIENTED_EDGE ( 'NONE', *, *, #19830, .F. ) ;
#10678=EDGE_LOOP ( 'NONE', ( #3398, #26715, #25842, #12538, #28913 ) ) ;
#10682=CARTESIAN_POINT ( 'NONE',  ( 2.910383045670000247E-11, 21.70000000000000284, -64.10000000000000853 ) ) ;
#10687=B_SPLINE_CURVE_WITH_KNOTS ( 'NONE', 3,
 ( #28982, #16407, #9632, #26014 ),
 .UNSPECIFIED., .F., .F.,
 ( 4, 4 ),
 ( 0.000000000000000000, 1.000000000000000000 ),
 .UNSPECIFIED. ) ;
#10688=VECTOR ( 'NONE', #234, 1000.000000000000000 ) ;
#10690=CARTESIAN_POINT ( 'NONE',  ( -8.999999999559999964, 21.35000000040000145, -64.10000000000000853 ) ) ;
#10704=DIRECTION ( 'NONE',  ( 0.000000000000000000, -1.000000000000000000, 0.000000000000000000 ) ) ;
#10707=VECTOR ( 'NONE', #13215, 1000.000000000000000 ) ;
#10708=CARTESIAN_POINT ( 'NONE',  ( 8.999999999770000869, 18.79791847199999921, -43.89791847198399921 ) ) ;
#10710=AXIS2_PLACEMENT_3D ( 'NONE', #27342, #10663, #10983 ) ;
#10711=ORIENTED_EDGE ( 'NONE', *, *, #28681, .F. ) ;
#10712=CARTESIAN_POINT ( 'NONE',  ( -9.000000000229999131, 21.70000000000000284, -60.10000000000000142 ) ) ;
#10718=PLANE ( 'NONE',  #516 ) ;
#10734=CARTESIAN_POINT ( 'NONE',  ( 18.13191322300000152, -9.527368092900001528, -0.6999999999999992895 ) ) ;
#10744=ORIENTED_EDGE ( 'NONE', *, *, #6339, .T. ) ;
#10748=VERTEX_POINT ( 'NONE', #18260 ) ;
#10749=EDGE_CURVE ( 'NONE', #9824, #18576, #22009, .T. ) ;
#10762=DIRECTION ( 'NONE',  ( -1.000000000000000000, 0.000000000000000000, -2.257144471330000330E-12 ) ) ;
#10769=AXIS2_PLACEMENT_3D ( 'NONE', #8521, #8207, #24915 ) ;
#10770=CARTESIAN_POINT ( 'NONE',  ( 10.88909890409999903, 21.70000000000000284, -56.10000000020000499 ) ) ;
#10775=CIRCLE ( 'NONE', #15290, 1.100000000390000787 ) ;
#10783=CARTESIAN_POINT ( 'NONE',  ( -10.58956532309999865, -24.61949706369999902, -1.102843534499998945 ) ) ;
#10792=ADVANCED_FACE ( 'NONE', ( #22499 ), #24860, .F. ) ;
#10793=DIRECTION ( 'NONE',  ( 0.000000000000000000, -2.256683728769999802E-12, -1.000000000000000000 ) ) ;
#10796=CARTESIAN_POINT ( 'NONE',  ( -10.90985356904797321, -24.71798678610834443, -1.786271532367390114 ) ) ;
#10803=EDGE_CURVE ( 'NONE', #28481, #30214, #29570, .T. ) ;
#10804=VERTEX_POINT ( 'NONE', #29724 ) ;
#10806=EDGE_LOOP ( 'NONE', ( #26405, #12810, #21128, #10675 ) ) ;
#10807=CARTESIAN_POINT ( 'NONE',  ( -11.81476342111506561, 21.69999999997402540, -55.60962715557913327 ) ) ;
#10818=DIRECTION ( 'NONE',  ( -0.5193310806158223381, -1.929012505286207873E-12, -0.8545731265997089654 ) ) ;
#10827=CARTESIAN_POINT ( 'NONE',  ( -17.23443287097794752, 9.965626860168409706, -1.400000000000002132 ) ) ;
#10829=ADVANCED_FACE ( 'NONE', ( #1091 ), #17454, .F. ) ;
#10830=FACE_OUTER_BOUND ( 'NONE', #16023, .T. ) ;
#10850=CARTESIAN_POINT ( 'NONE',  ( -10.00000000070000183, -30.00000000000000000, -28.40000000000000213 ) ) ;
#10855=CYLINDRICAL_SURFACE ( 'NONE', #24561, 3.000000000000003997 ) ;
#10861=ADVANCED_FACE ( 'NONE', ( #6583, #4074, #13988 ), #25947, .F. ) ;
#10862=LINE ( 'NONE', #22359, #18184 ) ;
#10865=CARTESIAN_POINT ( 'NONE',  ( 10.00000000000000000, 20.99999999999999645, -60.10000000019999788 ) ) ;
#10867=B_SPLINE_CURVE_WITH_KNOTS ( 'NONE', 3,
 ( #18175, #17857, #3240, #12995, #20230, #8107, #27777, #29519, #27317, #13307 ),
 .UNSPECIFIED., .F., .F.,
 ( 4, 2, 2, 2, 4 ),
 ( 0.000000000000000000, 0.2499999999999998890, 0.4999999999999998890, 0.7500000000000000000, 1.000000000000000000 ),
 .UNSPECIFIED. ) ;
#10875=CARTESIAN_POINT ( 'NONE',  ( -9.000000000000000000, 19.99999999999999645, -44.10000000000000142 ) ) ;
#10876=DIRECTION ( 'NONE',  ( 2.257150022439999944E-12, 0.000000000000000000, 1.000000000000000000 ) ) ;
#10881=ORIENTED_EDGE ( 'NONE', *, *, #15426, .F. ) ;
#10882=B_SPLINE_CURVE_WITH_KNOTS ( 'NONE', 5,
 ( #25882, #26181, #7137, #26032, #9027, #8867, #4473, #19097, #4788, #16575, #18471, #9336 ),
 .UNSPECIFIED., .F., .F.,
 ( 6, 3, 3, 6 ),
 ( 0.000000000000000000, 0.5717440563929999664, 1.143488112780000066, 1.429360140980000082 ),
 .UNSPECIFIED. ) ;
#10889=CARTESIAN_POINT ( 'NONE',  ( 9.000000000000000000, 19.99999999999999645, -43.39999999999999858 ) ) ;
#10904=ORIENTED_EDGE ( 'NONE', *, *, #21745, .F. ) ;
#10909=ORIENTED_EDGE ( 'NONE', *, *, #21707, .F. ) ;
#10912=LINE ( 'NONE', #30845, #418 ) ;
#10913=EDGE_CURVE ( 'NONE', #19402, #18717, #20750, .T. ) ;
#10925=CARTESIAN_POINT ( 'NONE',  ( -10.69999999989999928, -25.00000000000000000, -2.399999999999999467 ) ) ;
#10926=DIRECTION ( 'NONE',  ( 0.000000000000000000, 0.000000000000000000, 1.000000000000000000 ) ) ;
#10937=CARTESIAN_POINT ( 'NONE',  ( -10.69999999930000101, -29.30501631370000482, -26.47986984990000181 ) ) ;
#10938=CARTESIAN_POINT ( 'NONE',  ( -13.99999999969999820, 21.69999999929999390, -58.51619611000000276 ) ) ;
#10939=CARTESIAN_POINT ( 'NONE',  ( -12.68069379941013253, 20.99999999997307398, -56.02824004937883018 ) ) ;
#10940=DIRECTION ( 'NONE',  ( 1.000000000000000000, -0.000000000000000000, -9.868649108069999529E-17 ) ) ;
#10941=ORIENTED_EDGE ( 'NONE', *, *, #9420, .F. ) ;
#10944=AXIS2_PLACEMENT_3D ( 'NONE', #10682, #29877, #8308 ) ;
#10948=B_SPLINE_CURVE_WITH_KNOTS ( 'NONE', 3,
 ( #8513, #18114, #21230, #4865, #18273, #25532 ),
 .UNSPECIFIED., .F., .F.,
 ( 4, 2, 4 ),
 ( 0.000000000000000000, 0.5000000000000000000, 1.000000000000000000 ),
 .UNSPECIFIED. ) ;
#10968=DIRECTION ( 'NONE',  ( -1.000000000000000000, 6.565028073413479156E-24, -2.257144471327815248E-12 ) ) ;
#10971=EDGE_CURVE ( 'NONE', #23430, #7509, #288, .T. ) ;
#10983=DIRECTION ( 'NONE',  ( 0.000000000000000000, -2.257145581549999994E-12, -1.000000000000000000 ) ) ;
#10998=ORIENTED_EDGE ( 'NONE', *, *, #7552, .F. ) ;
#10999=CYLINDRICAL_SURFACE ( 'NONE', #16286, 3.000000000000005329 ) ;
#11001=PLANE ( 'NONE',  #21517 ) ;
#11002=DIRECTION ( 'NONE',  ( 0.000000000000000000, 0.000000000000000000, 1.000000000000000000 ) ) ;
#11004=CARTESIAN_POINT ( 'NONE',  ( 9.000000000000000000, -55.00000000000000000, -43.39999999999999858 ) ) ;
#11005=CARTESIAN_POINT ( 'NONE',  ( 31.69999999989999395, 19.99999999999999645, -0.6999999999999992895 ) ) ;
#11008=CARTESIAN_POINT ( 'NONE',  ( -10.00000000070000183, -30.00000000000000000, -28.40000000000000213 ) ) ;
#11009=DIRECTION ( 'NONE',  ( -1.595945597898660305E-12, 0.7071067811865475727, -0.7071067811865475727 ) ) ;
#11030=EDGE_CURVE ( 'NONE', #20395, #3580, #18652, .T. ) ;
#11036=EDGE_CURVE ( 'NONE', #30538, #3949, #16490, .T. ) ;
#11046=CARTESIAN_POINT ( 'NONE',  ( 16.39979399493674705, -21.22530604129068266, -1.399999999999998357 ) ) ;
#11068=CARTESIAN_POINT ( 'NONE',  ( 10.00000000000000000, 21.70000000000000284, -62.10000000000000142 ) ) ;
#11069=ORIENTED_EDGE ( 'NONE', *, *, #16930, .F. ) ;
#11079=CARTESIAN_POINT ( 'NONE',  ( -9.999999999969999109, -120.5233595632000174, -31.26042064989999858 ) ) ;
#11082=B_SPLINE_CURVE_WITH_KNOTS ( 'NONE', 5,
 ( #20669, #15784, #8535, #6183, #16517, #4563, #23771, #25396, #8690 ),
 .UNSPECIFIED., .F., .F.,
 ( 6, 3, 6 ),
 ( 0.000000000000000000, 0.6973066784960000319, 1.117931991580000117 ),
 .UNSPECIFIED. ) ;
#11087=ORIENTED_EDGE ( 'NONE', *, *, #16138, .F. ) ;
#11090=DIRECTION ( 'NONE',  ( -1.635844237846128888E-12, -0.6889064844606307414, 0.7248502298186121351 ) ) ;
#11100=CARTESIAN_POINT ( 'NONE',  ( -11.69999999989999928, -24.11120071670000087, -1.399999999999998579 ) ) ;
#11101=CARTESIAN_POINT ( 'NONE',  ( 9.999999999770000869, 21.70000000000000284, -64.10000000000000853 ) ) ;
#11102=ORIENTED_EDGE ( 'NONE', *, *, #21369, .F. ) ;
#11109=CIRCLE ( 'NONE', #16625, 1.000000000000000888 ) ;
#11113=VERTEX_POINT ( 'NONE', #15066 ) ;
#11121=CARTESIAN_POINT ( 'NONE',  ( -4.175165894169885483, -50.49316738903675628, -44.10000000000000142 ) ) ;
#11126=ORIENTED_EDGE ( 'NONE', *, *, #11427, .F. ) ;
#11130=ADVANCED_FACE ( 'NONE', ( #5460 ), #13006, .T. ) ;
#11136=CARTESIAN_POINT ( 'NONE',  ( -17.78039861525124365, 10.42209091420443379, -1.400000000000001910 ) ) ;
#11142=CARTESIAN_POINT ( 'NONE',  ( -13.67718144140000014, 20.99999999999999645, -57.16242377749999548 ) ) ;
#11146=EDGE_CURVE ( 'NONE', #4569, #27858, #8115, .T. ) ;
#11153=AXIS2_PLACEMENT_3D ( 'NONE', #12385, #9565, #26406 ) ;
#11157=CARTESIAN_POINT ( 'NONE',  ( 9.000000000000000000, -130.0000000000000000, -43.40000000074500264 ) ) ;
#11159=FACE_OUTER_BOUND ( 'NONE', #781, .T. ) ;
#11176=VERTEX_POINT ( 'NONE', #10501 ) ;
#11180=CARTESIAN_POINT ( 'NONE',  ( 9.999999999963856467, -42.68965130474573755, -27.18132884639398839 ) ) ;
#11188=ORIENTED_EDGE ( 'NONE', *, *, #10803, .F. ) ;
#11197=VERTEX_POINT ( 'NONE', #3402 ) ;
#11200=CARTESIAN_POINT ( 'NONE',  ( -10.69999999930000101, -24.87867965640000278, -26.27867965640000136 ) ) ;
#11207=B_SPLINE_CURVE_WITH_KNOTS ( 'NONE', 3,
 ( #24176, #21508, #14430, #13524, #23136, #26229 ),
 .UNSPECIFIED., .F., .F.,
 ( 4, 2, 4 ),
 ( 0.000000000000000000, 0.5000000000000000000, 1.000000000000000000 ),
 .UNSPECIFIED. ) ;
#11210=CARTESIAN_POINT ( 'NONE',  ( -15.51200411779723254, -21.88251757794091290, -1.399999999999998357 ) ) ;
#11216=ADVANCED_FACE ( 'NONE', ( #6239 ), #13155, .F. ) ;
#11222=ORIENTED_EDGE ( 'NONE', *, *, #4176, .T. ) ;
#11230=AXIS2_PLACEMENT_3D ( 'NONE', #26121, #18562, #14159 ) ;
#11237=ORIENTED_EDGE ( 'NONE', *, *, #4999, .T. ) ;
#11238=CARTESIAN_POINT ( 'NONE',  ( -9.999999999959999997, -24.87868334570000073, -26.27868334529999927 ) ) ;
#11242=DIRECTION ( 'NONE',  ( 0.000000000000000000, -2.255973186040000320E-12, -1.000000000000000000 ) ) ;
#11243=VERTEX_POINT ( 'NONE', #11121 ) ;
#11260=AXIS2_PLACEMENT_3D ( 'NONE', #26770, #5369, #7871 ) ;
#11267=DIRECTION ( 'NONE',  ( 1.000000000000000000, -0.000000000000000000, -2.257150022439999944E-12 ) ) ;
#11275=EDGE_CURVE ( 'NONE', #3695, #22220, #14985, .T. ) ;
#11281=VECTOR ( 'NONE', #2239, 1000.000000000000000 ) ;
#11284=CARTESIAN_POINT ( 'NONE',  ( 10.69999999989999928, -25.00000000000000000, -4.837481085799996805 ) ) ;
#11286=VERTEX_POINT ( 'NONE', #4191 ) ;
#11292=LINE ( 'NONE', #20896, #30103 ) ;
#11293=CARTESIAN_POINT ( 'NONE',  ( 12.12499559729999810, 21.69999999929999390, -55.73512174120000395 ) ) ;
#11294=CARTESIAN_POINT ( 'NONE',  ( -16.38556888388364641, 9.985034189104762703, -1.400000000000002132 ) ) ;
#11297=CARTESIAN_POINT ( 'NONE',  ( 8.999999999799992878, 20.99999999999851497, -51.75449846949787513 ) ) ;
#11302=CARTESIAN_POINT ( 'NONE',  ( -12.12499970530000049, 21.69999999919999212, -55.73512393530000253 ) ) ;
#11313=AXIS2_PLACEMENT_3D ( 'NONE', #7969, #8587, #13007 ) ;
#11319=CARTESIAN_POINT ( 'NONE',  ( 10.69999999999999929, -130.0000000000000000, -41.82335799894999440 ) ) ;
#11323=EDGE_LOOP ( 'NONE', ( #20498, #23449, #1995, #23191 ) ) ;
#11343=CARTESIAN_POINT ( 'NONE',  ( -10.00000000057973359, -129.9999999999998010, -39.98135228930375007 ) ) ;
#11346=ORIENTED_EDGE ( 'NONE', *, *, #1348, .T. ) ;
#11348=ORIENTED_EDGE ( 'NONE', *, *, #24567, .F. ) ;
#11351=EDGE_CURVE ( 'NONE', #15903, #6922, #9965, .T. ) ;
#11353=CARTESIAN_POINT ( 'NONE',  ( -10.00000000020000002, -28.65356604289999964, -25.83278327859999735 ) ) ;
#11357=CARTESIAN_POINT ( 'NONE',  ( 12.55799324160000019, 21.70000000000000284, -55.95247857500000066 ) ) ;
#11367=EDGE_CURVE ( 'NONE', #27091, #21618, #10356, .T. ) ;
#11377=DIRECTION ( 'NONE',  ( 0.000000000000000000, 0.000000000000000000, -1.000000000000000000 ) ) ;
#11382=ORIENTED_EDGE ( 'NONE', *, *, #16930, .T. ) ;
#11387=ORIENTED_EDGE ( 'NONE', *, *, #24498, .F. ) ;
#11396=VERTEX_POINT ( 'NONE', #10120 ) ;
#11397=ADVANCED_FACE ( 'NONE', ( #19247 ), #14689, .F. ) ;
#11402=EDGE_LOOP ( 'NONE', ( #16636, #29922, #24546, #26731 ) ) ;
#11404=CARTESIAN_POINT ( 'NONE',  ( -10.69999999999999929, -128.0330808734999835, -35.24741685077000142 ) ) ;
#11407=CARTESIAN_POINT ( 'NONE',  ( 11.59065746419999954, -24.20066399999999973, -1.404983722799999057 ) ) ;
#11410=CARTESIAN_POINT ( 'NONE',  ( 10.69999999997749640, -124.7625450005068615, -32.43068487539576950 ) ) ;
#11411=VERTEX_POINT ( 'NONE', #22081 ) ;
#11415=PRODUCT_DEFINITION_SHAPE ( 'NONE', 'NONE',  #2358 ) ;
#11421=LINE ( 'NONE', #16291, #17470 ) ;
#11422=EDGE_CURVE ( 'NONE', #26986, #49, #24277, .T. ) ;
#11427=EDGE_CURVE ( 'NONE', #3166, #18608, #15577, .T. ) ;
#11431=LINE ( 'NONE', #30480, #19573 ) ;
#11433=CARTESIAN_POINT ( 'NONE',  ( 9.929578881719999472, 19.99999999999999645, -42.78784606711000293 ) ) ;
#11439=CARTESIAN_POINT ( 'NONE',  ( 10.69999999989999928, 19.99999999999999645, -2.399999999999999467 ) ) ;
#11463=AXIS2_PLACEMENT_3D ( 'NONE', #5869, #15479, #1323 ) ;
#11477=ORIENTED_EDGE ( 'NONE', *, *, #1690, .T. ) ;
#11493=CARTESIAN_POINT ( 'NONE',  ( -10.92440694859999972, 19.99999999999999645, -0.8628532294999990970 ) ) ;
#11499=VECTOR ( 'NONE', #5150, 1000.000000000000000 ) ;
#11500=ORIENTED_EDGE ( 'NONE', *, *, #20430, .T. ) ;
#11518=DIRECTION ( 'NONE',  ( 0.000000000000000000, -1.000000000000000000, 2.257145581549999994E-12 ) ) ;
#11521=EDGE_CURVE ( 'NONE', #20223, #21635, #10912, .T. ) ;
#11522=VECTOR ( 'NONE', #9067, 1000.000000000000000 ) ;
#11525=CARTESIAN_POINT ( 'NONE',  ( -10.00000000054610005, -24.99999999999988987, -8.540325878496638268 ) ) ;
#11547=SURFACE_STYLE_FILL_AREA ( #23519 ) ;
#11548=EDGE_CURVE ( 'NONE', #13159, #5171, #11082, .T. ) ;
#11560=CARTESIAN_POINT ( 'NONE',  ( 26.57440914490000239, -3.469982507400000582, -1.399999999999998579 ) ) ;
#11564=FACE_BOUND ( 'NONE', #5099, .T. ) ;
#11567=CARTESIAN_POINT ( 'NONE',  ( 9.999999999959999997, -25.00000000000000000, -26.16393202319999745 ) ) ;
#11568=FACE_OUTER_BOUND ( 'NONE', #9987, .T. ) ;
#11570=DIRECTION ( 'NONE',  ( 0.000000000000000000, 0.000000000000000000, -1.000000000000000000 ) ) ;
#11580=VERTEX_POINT ( 'NONE', #3287 ) ;
#11582=ADVANCED_FACE ( 'NONE', ( #25160 ), #3592, .F. ) ;
#11584=VERTEX_POINT ( 'NONE', #6277 ) ;
#11589=B_SPLINE_CURVE_WITH_KNOTS ( 'NONE', 3,
 ( #6847, #6691, #23398, #4181, #1829, #28412 ),
 .UNSPECIFIED., .F., .F.,
 ( 4, 2, 4 ),
 ( 0.000000000000000000, 0.5000000000000000000, 1.000000000000000000 ),
 .UNSPECIFIED. ) ;
#11593=ORIENTED_EDGE ( 'NONE', *, *, #19066, .F. ) ;
#11597=DIRECTION ( 'NONE',  ( -1.000000000000000000, 0.000000000000000000, 0.000000000000000000 ) ) ;
#11601=CARTESIAN_POINT ( 'NONE',  ( 12.27487041388367395, 21.70000000000035811, -55.79574881355755878 ) ) ;
#11605=AXIS2_PLACEMENT_3D ( 'NONE', #28738, #23728, #24180 ) ;
#11617=ORIENTED_EDGE ( 'NONE', *, *, #27014, .T. ) ;
#11629=CARTESIAN_POINT ( 'NONE',  ( 10.00000000000000000, 21.70000000000000284, -62.10000000019999788 ) ) ;
#11644=AXIS2_PLACEMENT_3D ( 'NONE', #3893, #25134, #4050 ) ;
#11651=ORIENTED_EDGE ( 'NONE', *, *, #26573, .T. ) ;
#11654=EDGE_LOOP ( 'NONE', ( #5678, #22673 ) ) ;
#11665=ORIENTED_EDGE ( 'NONE', *, *, #26276, .F. ) ;
#11670=CARTESIAN_POINT ( 'NONE',  ( -9.999999999559999964, 21.35000000040000145, -60.10000000000000142 ) ) ;
#11672=FACE_OUTER_BOUND ( 'NONE', #5412, .T. ) ;
#11684=VERTEX_POINT ( 'NONE', #27507 ) ;
#11687=AXIS2_PLACEMENT_3D ( 'NONE', #806, #22658, #8162 ) ;
#11695=ADVANCED_FACE ( 'NONE', ( #1407 ), #11001, .T. ) ;
#11708=VECTOR ( 'NONE', #29158, 1000.000000000000000 ) ;
#11710=CARTESIAN_POINT ( 'NONE',  ( 26.79009884939612363, -1.309321278689688173, -1.399999999999998801 ) ) ;
#11715=CARTESIAN_POINT ( 'NONE',  ( -10.00000000010863133, -25.15635984007449721, -30.79900052719556669 ) ) ;
#11719=PLANE ( 'NONE',  #21836 ) ;
#11721=CARTESIAN_POINT ( 'NONE',  ( -10.69999999999999929, -29.06671945329999929, -26.22544931050000017 ) ) ;
#11723=VECTOR ( 'NONE', #8722, 1000.000000000000000 ) ;
#11736=CARTESIAN_POINT ( 'NONE',  ( -12.77820031409999935, 21.69999999929999390, -56.09999999999999432 ) ) ;
#11740=CARTESIAN_POINT ( 'NONE',  ( -10.00000000020000002, -29.15099216359999801, -26.30554312050000121 ) ) ;
#11744=AXIS2_PLACEMENT_3D ( 'NONE', #16821, #14630, #12256 ) ;
#11745=CYLINDRICAL_SURFACE ( 'NONE', #15293, 1.000000000000000666 ) ;
#11746=PLANE ( 'NONE',  #21318 ) ;
#11762=EDGE_CURVE ( 'NONE', #16094, #20043, #28294, .T. ) ;
#11783=ORIENTED_EDGE ( 'NONE', *, *, #28437, .T. ) ;
#11789=VECTOR ( 'NONE', #156, 1000.000000000000000 ) ;
#11797=DIRECTION ( 'NONE',  ( 0.000000000000000000, 0.7071067811870488384, 0.7071067811860461960 ) ) ;
#11799=CARTESIAN_POINT ( 'NONE',  ( -10.49049139480000115, 19.99999999999999645, -1.182260226200000597 ) ) ;
#11802=CYLINDRICAL_SURFACE ( 'NONE', #27260, 1.099999999999999201 ) ;
#11804=ORIENTED_EDGE ( 'NONE', *, *, #29973, .T. ) ;
#11809=ORIENTED_EDGE ( 'NONE', *, *, #8464, .T. ) ;
#11818=B_SPLINE_CURVE_WITH_KNOTS ( 'NONE', 3,
 ( #3070, #26683, #17541, #10164, #12668, #22593, #3374, #5123 ),
 .UNSPECIFIED., .F., .F.,
 ( 4, 2, 2, 4 ),
 ( 0.000000000000000000, 0.2500000000000015543, 0.5000000000000031086, 1.000000000000000000 ),
 .UNSPECIFIED. ) ;
#11819=B_SPLINE_CURVE_WITH_KNOTS ( 'NONE', 5,
 ( #22027, #14326, #320, #628, #158, #5168, #478, #2363, #19188, #11947, #26272, #28940 ),
 .UNSPECIFIED., .F., .F.,
 ( 6, 3, 3, 6 ),
 ( 0.000000000000000000, 1.357884646170000043, 2.715789077110000171, 3.784579750909999873 ),
 .UNSPECIFIED. ) ;
#11824=CARTESIAN_POINT ( 'NONE',  ( 10.69999999999999929, 19.99999999999999645, -42.39999999999999858 ) ) ;
#11839=CYLINDRICAL_SURFACE ( 'NONE', #25337, 4.175165894169885483 ) ;
#11845=ORIENTED_EDGE ( 'NONE', *, *, #13199, .F. ) ;
#11854=FACE_OUTER_BOUND ( 'NONE', #3308, .T. ) ;
#11868=CARTESIAN_POINT ( 'NONE',  ( -13.67718144140000014, 20.99999999999999645, -57.16242377749999548 ) ) ;
#11870=CARTESIAN_POINT ( 'NONE',  ( 9.999999999959999997, -24.90230200559999574, -26.25506237459999781 ) ) ;
#11874=CARTESIAN_POINT ( 'NONE',  ( -10.69999999999999929, -24.00000000000000000, -28.40910480009999617 ) ) ;
#11879=ORIENTED_EDGE ( 'NONE', *, *, #26802, .T. ) ;
#11880=EDGE_CURVE ( 'NONE', #29903, #9281, #18597, .T. ) ;
#11888=VERTEX_POINT ( 'NONE', #14452 ) ;
#11894=CARTESIAN_POINT ( 'NONE',  ( -10.69999999994264250, -27.47131626858717368, -16.98885458297168327 ) ) ;
#11897=ORIENTED_EDGE ( 'NONE', *, *, #5282, .F. ) ;
#11906=LINE ( 'NONE', #21511, #21671 ) ;
#11924=CARTESIAN_POINT ( 'NONE',  ( 9.195955003099999914, 19.99999999999999645, -43.38800044014699608 ) ) ;
#11927=DIRECTION ( 'NONE',  ( 0.000000000000000000, 1.000000000000000000, 9.516197338740001367E-15 ) ) ;
#11928=B_SPLINE_CURVE_WITH_KNOTS ( 'NONE', 5,
 ( #10591, #5551, #30095, #20184, #27267, #3822 ),
 .UNSPECIFIED., .F., .F.,
 ( 6, 6 ),
 ( 0.000000000000000000, 0.2292465731912854965 ),
 .UNSPECIFIED. ) ;
#11930=DIRECTION ( 'NONE',  ( 0.000000000000000000, 0.000000000000000000, 1.000000000000000000 ) ) ;
#11947=CARTESIAN_POINT ( 'NONE',  ( 8.999999999770000869, 21.68327394420000687, -44.79835558794399475 ) ) ;
#11976=AXIS2_PLACEMENT_3D ( 'NONE', #955, #10545, #8159 ) ;
#11979=CARTESIAN_POINT ( 'NONE',  ( 12.55799324160000019, 20.99999999999999645, -55.95247857500000066 ) ) ;
#11988=EDGE_CURVE ( 'NONE', #18431, #9370, #18524, .T. ) ;
#11989=CARTESIAN_POINT ( 'NONE',  ( -10.69999999999999929, 19.99999999999999645, -42.39999999999999858 ) ) ;
#11990=DIRECTION ( 'NONE',  ( 0.000000000000000000, 1.000000000000000000, 0.000000000000000000 ) ) ;
#12000=ORIENTED_EDGE ( 'NONE', *, *, #1629, .T. ) ;
#12001=CARTESIAN_POINT ( 'NONE',  ( 9.999999999958141927, -27.37998968026300872, -25.40000000000158309 ) ) ;
#12009=CARTESIAN_POINT ( 'NONE',  ( 10.69999999994971240, -29.61896394763918039, -20.12083078305406048 ) ) ;
#12028=FACE_OUTER_BOUND ( 'NONE', #22447, .T. ) ;
#12033=CARTESIAN_POINT ( 'NONE',  ( 9.000000000000000000, -130.0000000000000000, -44.10000000000000142 ) ) ;
#12039=ORIENTED_EDGE ( 'NONE', *, *, #25645, .F. ) ;
#12053=CARTESIAN_POINT ( 'NONE',  ( 9.999999999959607422, -29.15099216425362272, -26.30554312115310722 ) ) ;
#12060=DIRECTION ( 'NONE',  ( -1.553705081258626668E-12, 0.7253743710120288402, -0.6883545756940265825 ) ) ;
#12064=CARTESIAN_POINT ( 'NONE',  ( 3.510330247560000227, 1.917702154400000136, -44.00000000037249492 ) ) ;
#12075=ORIENTED_EDGE ( 'NONE', *, *, #4208, .T. ) ;
#12084=DIRECTION ( 'NONE',  ( 0.8775825618903722036, 0.4794255386042041156, 0.000000000000000000 ) ) ;
#12096=DIRECTION ( 'NONE',  ( 1.000000000000000000, 0.000000000000000000, 0.000000000000000000 ) ) ;
#12108=ORIENTED_EDGE ( 'NONE', *, *, #1449, .F. ) ;
#12116=DIRECTION ( 'NONE',  ( -1.000000000000000000, 6.565028073413479156E-24, -2.257144471327815248E-12 ) ) ;
#12134=CARTESIAN_POINT ( 'NONE',  ( 16.20123158649999695, 11.52736809289999620, -1.399999999999998579 ) ) ;
#12140=ORIENTED_EDGE ( 'NONE', *, *, #1690, .F. ) ;
#12148=ORIENTED_EDGE ( 'NONE', *, *, #29066, .T. ) ;
#12149=LINE ( 'NONE', #28987, #22026 ) ;
#12162=EDGE_CURVE ( 'NONE', #21103, #17104, #5768, .T. ) ;
#12167=CARTESIAN_POINT ( 'NONE',  ( -10.69999999999999929, -29.30501631370000482, -26.47986984990000181 ) ) ;
#12170=CARTESIAN_POINT ( 'NONE',  ( 10.69999999999999929, -77.50000000000000000, -29.00566191750000300 ) ) ;
#12175=AXIS2_PLACEMENT_3D ( 'NONE', #18436, #2241, #21270 ) ;
#12196=ADVANCED_FACE ( 'NONE', ( #9062 ), #13635, .T. ) ;
#12198=ADVANCED_FACE ( 'NONE', ( #4190 ), #15993, .T. ) ;
#12199=EDGE_CURVE ( 'NONE', #3580, #16174, #3541, .T. ) ;
#12205=DIRECTION ( 'NONE',  ( -1.000000000000000000, 0.000000000000000000, 0.000000000000000000 ) ) ;
#12207=CARTESIAN_POINT ( 'NONE',  ( 10.69999999999596341, -130.0000000000000000, -40.61155403991316604 ) ) ;
#12234=VECTOR ( 'NONE', #8890, 1000.000000000000000 ) ;
#12235=CARTESIAN_POINT ( 'NONE',  ( -10.00000000000000000, -55.00000000000000000, -42.39999999999999858 ) ) ;
#12240=PLANE ( 'NONE',  #19003 ) ;
#12248=CARTESIAN_POINT ( 'NONE',  ( 10.69999999999999929, -25.00000000000000000, -26.16393202249999916 ) ) ;
#12253=EDGE_CURVE ( 'NONE', #15738, #9398, #17035, .T. ) ;
#12256=DIRECTION ( 'NONE',  ( 0.000000000000000000, -1.000000000000000000, 0.000000000000000000 ) ) ;
#12259=VECTOR ( 'NONE', #22184, 1000.000000000000000 ) ;
#12263=CARTESIAN_POINT ( 'NONE',  ( -9.999999999949999108, -30.49286765380000119, -21.04171673159999756 ) ) ;
#12266=EDGE_CURVE ( 'NONE', #26442, #17734, #19130, .T. ) ;
#12284=AXIS2_PLACEMENT_3D ( 'NONE', #17007, #26609, #185 ) ;
#12287=VECTOR ( 'NONE', #1655, 1000.000000000000000 ) ;
#12297=LINE ( 'NONE', #14821, #29362 ) ;
#12307=ORIENTED_EDGE ( 'NONE', *, *, #6151, .F. ) ;
#12318=CARTESIAN_POINT ( 'NONE',  ( 10.99999999979999998, 20.99999999999999645, -67.09999999999999432 ) ) ;
#12322=DIRECTION ( 'NONE',  ( 0.000000000000000000, -2.256683728769999802E-12, -1.000000000000000000 ) ) ;
#12325=EDGE_CURVE ( 'NONE', #15501, #22831, #15141, .T. ) ;
#12327=DIRECTION ( 'NONE',  ( 0.000000000000000000, 0.000000000000000000, -1.000000000000000000 ) ) ;
#12330=FACE_OUTER_BOUND ( 'NONE', #30461, .T. ) ;
#12333=FACE_OUTER_BOUND ( 'NONE', #2804, .T. ) ;
#12334=CARTESIAN_POINT ( 'NONE',  ( -10.69999999999999929, -25.55727021120000231, -31.05966627990000006 ) ) ;
#12341=ADVANCED_FACE ( 'NONE', ( #8826 ), #6472, .T. ) ;
#12344=VERTEX_POINT ( 'NONE', #11357 ) ;
#12357=CARTESIAN_POINT ( 'NONE',  ( -15.75517453283980096, 10.73903380419648812, -1.400000000000001910 ) ) ;
#12372=CARTESIAN_POINT ( 'NONE',  ( -16.83342759559999635, 11.00000000000000355, -0.6999999999999992895 ) ) ;
#12385=CARTESIAN_POINT ( 'NONE',  ( -9.000000000000000000, -130.0000000000000000, -42.39999999999999858 ) ) ;
#12387=EDGE_LOOP ( 'NONE', ( #21986, #17445, #13825, #6172 ) ) ;
#12419=B_SPLINE_CURVE_WITH_KNOTS ( 'NONE', 3,
 ( #6996, #18787, #1658, #11868 ),
 .UNSPECIFIED., .F., .F.,
 ( 4, 4 ),
 ( 0.000000000000000000, 1.000000000000000000 ),
 .UNSPECIFIED. ) ;
#12424=DIRECTION ( 'NONE',  ( 1.000000000000000000, 0.000000000000000000, 0.000000000000000000 ) ) ;
#12426=CARTESIAN_POINT ( 'NONE',  ( 9.999999999969219289, -29.99999999999982236, -28.05272263597640503 ) ) ;
#12441=CARTESIAN_POINT ( 'NONE',  ( 16.15160659333890791, 10.55214128798958129, -1.400000000000001910 ) ) ;
#12445=FACE_OUTER_BOUND ( 'NONE', #5796, .T. ) ;
#12446=CARTESIAN_POINT ( 'NONE',  ( 13.62135916440115935, 20.99999999989658761, -68.61085694196312090 ) ) ;
#12447=ORIENTED_EDGE ( 'NONE', *, *, #10118, .T. ) ;
#12459=CARTESIAN_POINT ( 'NONE',  ( -10.69999999999999929, -82.23832021929999314, -29.25398675779999991 ) ) ;
#12461=ORIENTED_EDGE ( 'NONE', *, *, #643, .F. ) ;
#12466=CARTESIAN_POINT ( 'NONE',  ( 13.99999999979999821, 20.99999999999999645, -63.10000000000000142 ) ) ;
#12467=ORIENTED_EDGE ( 'NONE', *, *, #28647, .T. ) ;
#12469=CARTESIAN_POINT ( 'NONE',  ( -10.69999999993204831, -25.59800645591167267, -12.29403537759453258 ) ) ;
#12476=ADVANCED_FACE ( 'NONE', ( #16537 ), #4430, .T. ) ;
#12481=CARTESIAN_POINT ( 'NONE',  ( -8.999999999710000864, 21.70000000000000284, -57.60000000000000142 ) ) ;
#12487=VECTOR ( 'NONE', #14539, 1000.000000000000000 ) ;
#12503=CARTESIAN_POINT ( 'NONE',  ( 10.32522729140000095, -24.79836099970000163, -1.399999999999998579 ) ) ;
#12506=CIRCLE ( 'NONE', #7962, 2.999999999999999112 ) ;
#12507=EDGE_CURVE ( 'NONE', #24264, #3826, #159, .T. ) ;
#12508=LINE ( 'NONE', #7175, #23580 ) ;
#12527=CARTESIAN_POINT ( 'NONE',  ( -9.130012207994363749, 21.69999999998125162, -52.40811918958280557 ) ) ;
#12535=ORIENTED_EDGE ( 'NONE', *, *, #4704, .F. ) ;
#12538=ORIENTED_EDGE ( 'NONE', *, *, #4200, .T. ) ;
#12543=CARTESIAN_POINT ( 'NONE',  ( 18.11354342366337988, 11.57790908577752376, -1.400000000000001910 ) ) ;
#12564=CARTESIAN_POINT ( 'NONE',  ( 9.000000000000000000, 21.70000000000000284, -56.10000000020000499 ) ) ;
#12568=CARTESIAN_POINT ( 'NONE',  ( 12.77819780750000156, 20.99999999999999645, -56.09999999999999432 ) ) ;
#12581=ADVANCED_FACE ( 'NONE', ( #343 ), #499, .F. ) ;
#12584=LINE ( 'NONE', #19526, #30601 ) ;
#12590=EDGE_CURVE ( 'NONE', #27980, #21635, #10388, .T. ) ;
#12591=LINE ( 'NONE', #21902, #17678 ) ;
#12596=LINE ( 'NONE', #22204, #12705 ) ;
#12603=VERTEX_POINT ( 'NONE', #5502 ) ;
#12606=ORIENTED_EDGE ( 'NONE', *, *, #3059, .T. ) ;
#12609=ORIENTED_EDGE ( 'NONE', *, *, #21227, .T. ) ;
#12612=CARTESIAN_POINT ( 'NONE',  ( -17.79876841389999598, 11.52736809249999617, -0.7999999992999995424 ) ) ;
#12614=EDGE_CURVE ( 'NONE', #19704, #26138, #17414, .T. ) ;
#12617=B_SPLINE_CURVE_WITH_KNOTS ( 'NONE', 3,
 ( #3818, #13405, #23019, #27887, #23175, #20807 ),
 .UNSPECIFIED., .F., .F.,
 ( 4, 2, 4 ),
 ( 0.000000000000000000, 0.5000000000000000000, 1.000000000000000000 ),
 .UNSPECIFIED. ) ;
#12628=LINE ( 'NONE', #5396, #16740 ) ;
#12635=LINE ( 'NONE', #14866, #260 ) ;
#12638=EDGE_CURVE ( 'NONE', #7936, #28636, #12584, .T. ) ;
#12644=B_SPLINE_CURVE_WITH_KNOTS ( 'NONE', 3,
 ( #18443, #16397, #28041, #11210, #30880, #6956, #23802, #9311, #20812, #18910, #28510, #16549, #4591, #30419, #14199, #2247 ),
 .UNSPECIFIED., .F., .F.,
 ( 4, 2, 2, 2, 2, 2, 2, 4 ),
 ( 0.000000000000000000, 0.1249999999999999167, 0.2499999999999998335, 0.4999999999999998890, 0.6249999999999998890, 0.7499999999999998890, 0.8750000000000000000, 1.000000000000000000 ),
 .UNSPECIFIED. ) ;
#12658=CARTESIAN_POINT ( 'NONE',  ( 9.707106781189999367, -130.0000000000000000, -43.10710678118599759 ) ) ;
#12662=ORIENTED_EDGE ( 'NONE', *, *, #4072, .T. ) ;
#12668=CARTESIAN_POINT ( 'NONE',  ( 9.999999999962223995, -25.75869229542447769, -25.66275671166319583 ) ) ;
#12669=CARTESIAN_POINT ( 'NONE',  ( 10.69999999999173390, -129.7008471317687395, -38.73679577504942273 ) ) ;
#12675=CARTESIAN_POINT ( 'NONE',  ( 10.69999999930000101, -29.30501631380000305, -26.47986985000000004 ) ) ;
#12679=FACE_OUTER_BOUND ( 'NONE', #23338, .T. ) ;
#12685=EDGE_CURVE ( 'NONE', #29610, #29523, #24952, .T. ) ;
#12701=EDGE_CURVE ( 'NONE', #3589, #11176, #4278, .T. ) ;
#12705=VECTOR ( 'NONE', #7417, 1000.000000000000000 ) ;
#12706=DIRECTION ( 'NONE',  ( -1.000000000000000000, 0.000000000000000000, 0.000000000000000000 ) ) ;
#12715=ORIENTED_EDGE ( 'NONE', *, *, #21844, .T. ) ;
#12725=VERTEX_POINT ( 'NONE', #20441 ) ;
#12752=CARTESIAN_POINT ( 'NONE',  ( 16.13219926443963814, 11.40100527538031905, -1.400000000000001910 ) ) ;
#12756=CARTESIAN_POINT ( 'NONE',  ( 10.99999999979999998, 20.99999999999999645, -58.51619795479999908 ) ) ;
#12763=DIRECTION ( 'NONE',  ( 0.000000000000000000, -1.000000000000000000, 0.000000000000000000 ) ) ;
#12764=ORIENTED_EDGE ( 'NONE', *, *, #17166, .T. ) ;
#12765=ORIENTED_EDGE ( 'NONE', *, *, #11427, .T. ) ;
#12772=LINE ( 'NONE', #12459, #22209 ) ;
#12774=LINE ( 'NONE', #20168, #22353 ) ;
#12775=AXIS2_PLACEMENT_3D ( 'NONE', #15427, #8487, #10704 ) ;
#12776=CARTESIAN_POINT ( 'NONE',  ( -10.00000000000000000, 19.99999999999999645, -42.39999999999999858 ) ) ;
#12783=DIRECTION ( 'NONE',  ( -1.000000000000000000, 0.000000000000000000, -2.253435535809999718E-12 ) ) ;
#12795=VECTOR ( 'NONE', #22402, 1000.000000000000000 ) ;
#12799=DIRECTION ( 'NONE',  ( -2.256480420250000087E-12, 0.000000000000000000, -1.000000000000000000 ) ) ;
#12801=VECTOR ( 'NONE', #28000, 1000.000000000000000 ) ;
#12805=VERTEX_POINT ( 'NONE', #760 ) ;
#12810=ORIENTED_EDGE ( 'NONE', *, *, #22230, .T. ) ;
#12837=CARTESIAN_POINT ( 'NONE',  ( -9.500000000000000000, 21.70000000000000284, -64.10000000019999788 ) ) ;
#12846=CARTESIAN_POINT ( 'NONE',  ( 10.49243769669999971, -24.66097101770000322, -1.192453590699998900 ) ) ;
#12847=CARTESIAN_POINT ( 'NONE',  ( -10.89131017139999891, -25.00000000000000000, -1.811764705899998606 ) ) ;
#12848=DIRECTION ( 'NONE',  ( 0.000000000000000000, -1.000000000000000000, 0.000000000000000000 ) ) ;
#12854=EDGE_CURVE ( 'NONE', #19996, #14172, #24362, .T. ) ;
#12856=CARTESIAN_POINT ( 'NONE',  ( 9.999999999969999109, -29.12127062269999911, -30.52127062070000107 ) ) ;
#12870=CARTESIAN_POINT ( 'NONE',  ( -8.999999998369998977, 20.99999999999999645, -60.10000000000000142 ) ) ;
#12877=DIRECTION ( 'NONE',  ( 0.000000000000000000, 1.000000000000000000, 0.000000000000000000 ) ) ;
#12881=EDGE_CURVE ( 'NONE', #24088, #29870, #19796, .T. ) ;
#12882=CARTESIAN_POINT ( 'NONE',  ( 13.92209366199456255, 21.69999999994632489, -67.88485145451890901 ) ) ;
#12885=ORIENTED_EDGE ( 'NONE', *, *, #1679, .F. ) ;
#12886=EDGE_CURVE ( 'NONE', #27858, #4970, #10351, .T. ) ;
#12891=CARTESIAN_POINT ( 'NONE',  ( 10.69999999999999929, -27.00000000000000000, -28.40000000000000213 ) ) ;
#12898=CARTESIAN_POINT ( 'NONE',  ( 10.69999999999999929, -27.00000000000000000, -31.39999999999999858 ) ) ;
#12927=CYLINDRICAL_SURFACE ( 'NONE', #23725, 2.999999999999999556 ) ;
#12929=ORIENTED_EDGE ( 'NONE', *, *, #7016, .T. ) ;
#12935=VERTEX_POINT ( 'NONE', #22621 ) ;
#12941=ADVANCED_FACE ( 'NONE', ( #1373 ), #1218, .F. ) ;
#12945=CARTESIAN_POINT ( 'NONE',  ( 10.69999999999999929, -30.49251257979999963, -21.04205368479999905 ) ) ;
#12950=ORIENTED_EDGE ( 'NONE', *, *, #25582, .F. ) ;
#12957=VERTEX_POINT ( 'NONE', #8589 ) ;
#12962=AXIS2_PLACEMENT_3D ( 'NONE', #26044, #21314, #30917 ) ;
#12965=CARTESIAN_POINT ( 'NONE',  ( -10.69999999999999929, -29.30501631370000482, -26.47986984990000181 ) ) ;
#12979=EDGE_CURVE ( 'NONE', #15367, #17295, #27634, .T. ) ;
#12995=CARTESIAN_POINT ( 'NONE',  ( -26.38304356803462625, 5.185566697915457546, -0.6999999999999992895 ) ) ;
#12999=VERTEX_POINT ( 'NONE', #6246 ) ;
#13006=CYLINDRICAL_SURFACE ( 'NONE', #9404, 10.00000000000000355 ) ;
#13007=DIRECTION ( 'NONE',  ( -0.7071067811865466846, -1.595945597898659700E-12, -0.7071067811865484609 ) ) ;
#13022=CARTESIAN_POINT ( 'NONE',  ( -10.69999999999999929, -27.00000000000000000, -25.39999999999999858 ) ) ;
#13026=ORIENTED_EDGE ( 'NONE', *, *, #25405, .F. ) ;
#13041=VECTOR ( 'NONE', #642, 1000.000000000000000 ) ;
#13051=EDGE_CURVE ( 'NONE', #26103, #25785, #3256, .T. ) ;
#13055=FACE_OUTER_BOUND ( 'NONE', #5383, .T. ) ;
#13059=ORIENTED_EDGE ( 'NONE', *, *, #20977, .T. ) ;
#13060=ORIENTED_EDGE ( 'NONE', *, *, #14494, .F. ) ;
#13064=ORIENTED_EDGE ( 'NONE', *, *, #21142, .F. ) ;
#13066=DIRECTION ( 'NONE',  ( 1.000000000000000000, 0.000000000000000000, 0.000000000000000000 ) ) ;
#13069=EDGE_LOOP ( 'NONE', ( #12307, #16701, #8251, #9335 ) ) ;
#13071=ORIENTED_EDGE ( 'NONE', *, *, #29887, .T. ) ;
#13076=ADVANCED_FACE ( 'NONE', ( #1534 ), #22463, .F. ) ;
#13079=DIRECTION ( 'NONE',  ( 0.000000000000000000, -1.000000000000000000, 0.000000000000000000 ) ) ;
#13092=EDGE_CURVE ( 'NONE', #6267, #9824, #26018, .T. ) ;
#13103=B_SPLINE_CURVE_WITH_KNOTS ( 'NONE', 3,
 ( #20679, #13749, #13274, #22886, #1329, #18621 ),
 .UNSPECIFIED., .F., .F.,
 ( 4, 2, 4 ),
 ( 0.000000000000000000, 0.5000000000000000000, 1.000000000000000000 ),
 .UNSPECIFIED. ) ;
#13132=CARTESIAN_POINT ( 'NONE',  ( -12.47330046629999956, 20.99999999999999645, -55.90292611659999977 ) ) ;
#13135=CARTESIAN_POINT ( 'NONE',  ( -10.69999999997517115, -27.39453140544401322, -31.40000000000000568 ) ) ;
#13140=CARTESIAN_POINT ( 'NONE',  ( 8.999999999770000869, 21.70000000000000284, -45.10000000000000142 ) ) ;
#13142=CARTESIAN_POINT ( 'NONE',  ( -10.99289321870000080, -24.65831413349999934, -1.692893218799999877 ) ) ;
#13151=ADVANCED_FACE ( 'NONE', ( #18974 ), #8910, .F. ) ;
#13155=CYLINDRICAL_SURFACE ( 'NONE', #6911, 3.000000000000003997 ) ;
#13159=VERTEX_POINT ( 'NONE', #11439 ) ;
#13165=LINE ( 'NONE', #10512, #5967 ) ;
#13169=CARTESIAN_POINT ( 'NONE',  ( -17.41133668179312721, 11.94697101933574324, -1.400000000000001688 ) ) ;
#13170=CARTESIAN_POINT ( 'NONE',  ( -11.69999999989999928, -25.00000000000000000, -1.399999999999998579 ) ) ;
#13177=ORIENTED_EDGE ( 'NONE', *, *, #28804, .T. ) ;
#13186=DIRECTION ( 'NONE',  ( 1.595945597898660305E-12, 0.7071067811865475727, -0.7071067811865475727 ) ) ;
#13199=EDGE_CURVE ( 'NONE', #1607, #23118, #30641, .T. ) ;
#13209=EDGE_CURVE ( 'NONE', #9398, #22920, #28582, .T. ) ;
#13215=DIRECTION ( 'NONE',  ( 0.000000000000000000, -1.000000000000000000, 2.257145581549999994E-12 ) ) ;
#13219=ORIENTED_EDGE ( 'NONE', *, *, #17643, .T. ) ;
#13224=CARTESIAN_POINT ( 'NONE',  ( -9.999999999959999997, -24.87868334570000073, -26.27868334529999927 ) ) ;
#13225=FACE_OUTER_BOUND ( 'NONE', #23589, .T. ) ;
#13237=CARTESIAN_POINT ( 'NONE',  ( -10.69999999999999929, -130.0000000000000000, -22.39999999999999858 ) ) ;
#13245=DIRECTION ( 'NONE',  ( 0.000000000000000000, 2.259525899719999991E-12, 1.000000000000000000 ) ) ;
#13264=FACE_OUTER_BOUND ( 'NONE', #24495, .T. ) ;
#13268=CARTESIAN_POINT ( 'NONE',  ( 13.67718073920000066, 20.99999999999999645, -57.16242423349999768 ) ) ;
#13273=EDGE_CURVE ( 'NONE', #27091, #17864, #26676, .T. ) ;
#13274=CARTESIAN_POINT ( 'NONE',  ( -10.00000000021355362, -24.37864083493692746, -29.91085694111383120 ) ) ;
#13275=CARTESIAN_POINT ( 'NONE',  ( 9.301654454730000410, 19.99999999999999645, -44.08327288285030221 ) ) ;
#13279=ORIENTED_EDGE ( 'NONE', *, *, #17499, .T. ) ;
#13280=ADVANCED_FACE ( 'NONE', ( #14579 ), #24019, .T. ) ;
#13285=EDGE_LOOP ( 'NONE', ( #452, #2479, #14088, #9203 ) ) ;
#13287=DIRECTION ( 'NONE',  ( 0.000000000000000000, -2.257157423930000049E-12, -1.000000000000000000 ) ) ;
#13296=CARTESIAN_POINT ( 'NONE',  ( -11.51411769270000107, -24.20066399839999960, -0.7084723282999999538 ) ) ;
#13307=CARTESIAN_POINT ( 'NONE',  ( -17.83928249680000278, 19.99999999999999645, -0.6999999999999992895 ) ) ;
#13314=ORIENTED_EDGE ( 'NONE', *, *, #8898, .F. ) ;
#13318=AXIS2_PLACEMENT_3D ( 'NONE', #3802, #1128, #1447 ) ;
#13321=CIRCLE ( 'NONE', #3275, 3.999999999669999973 ) ;
#13330=DIRECTION ( 'NONE',  ( 0.000000000000000000, 1.000000000000000000, 0.000000000000000000 ) ) ;
#13332=CARTESIAN_POINT ( 'NONE',  ( 9.999999999969999109, -24.87872937930000106, -30.52127062269999769 ) ) ;
#13335=EDGE_CURVE ( 'NONE', #11684, #25785, #19757, .T. ) ;
#13338=EDGE_CURVE ( 'NONE', #21717, #5024, #12508, .T. ) ;
#13341=LINE ( 'NONE', #22947, #28395 ) ;
#13356=FACE_OUTER_BOUND ( 'NONE', #31072, .T. ) ;
#13359=CARTESIAN_POINT ( 'NONE',  ( -10.00000000009183942, -29.39900052719528389, -30.24364015992538057 ) ) ;
#13361=ORIENTED_EDGE ( 'NONE', *, *, #503, .T. ) ;
#13383=DIRECTION ( 'NONE',  ( -5.550937487439999770E-18, 0.000000000000000000, -1.000000000000000000 ) ) ;
#13387=DIRECTION ( 'NONE',  ( 0.000000000000000000, -1.000000000000000000, 0.000000000000000000 ) ) ;
#13396=EDGE_CURVE ( 'NONE', #5518, #23628, #18138, .T. ) ;
#13405=CARTESIAN_POINT ( 'NONE',  ( 9.999999999982071230, -128.1247626104539279, -35.28103264683748819 ) ) ;
#13411=CARTESIAN_POINT ( 'NONE',  ( 0.000000000000000000, -119.7166638525666826, -43.39999999999999858 ) ) ;
#13412=ORIENTED_EDGE ( 'NONE', *, *, #14640, .T. ) ;
#13415=DIRECTION ( 'NONE',  ( 0.000000000000000000, 1.000000000000000000, 0.000000000000000000 ) ) ;
#13422=ORIENTED_EDGE ( 'NONE', *, *, #232, .F. ) ;
#13438=CARTESIAN_POINT ( 'NONE',  ( 10.69999999999999929, -27.00000000000000000, -28.40000000000000213 ) ) ;
#13446=FACE_OUTER_BOUND ( 'NONE', #9400, .T. ) ;
#13464=LINE ( 'NONE', #18016, #29553 ) ;
#13468=ORIENTED_EDGE ( 'NONE', *, *, #21414, .F. ) ;
#13469=CARTESIAN_POINT ( 'NONE',  ( -10.99999999969999998, 20.99999999999999645, -70.09999999999999432 ) ) ;
#13470=FACE_OUTER_BOUND ( 'NONE', #938, .T. ) ;
#13471=CARTESIAN_POINT ( 'NONE',  ( -12.47331730070000155, 21.70000000000000284, -55.90289625529999995 ) ) ;
#13477=DIRECTION ( 'NONE',  ( 0.000000000000000000, -2.255973186040000320E-12, -1.000000000000000000 ) ) ;
#13483=CARTESIAN_POINT ( 'NONE',  ( 0.000000000000000000, -119.7166638525666826, -44.10000000000000142 ) ) ;
#13488=CARTESIAN_POINT ( 'NONE',  ( -16.03124949821963341, 10.23368197014037406, -1.400000000000001910 ) ) ;
#13490=VECTOR ( 'NONE', #12783, 1000.000000000000000 ) ;
#13491=EDGE_CURVE ( 'NONE', #26103, #20099, #1028, .T. ) ;
#13514=DIRECTION ( 'NONE',  ( 0.000000000000000000, -1.000000000000000000, 0.000000000000000000 ) ) ;
#13524=CARTESIAN_POINT ( 'NONE',  ( 8.999999999769999093, 20.50498856619357113, -44.22672584786599970 ) ) ;
#13534=B_SPLINE_CURVE_WITH_KNOTS ( 'NONE', 3,
 ( #2311, #7022, #5540, #11894, #14852, #4512, #12469, #4657, #21496, #24443 ),
 .UNSPECIFIED., .F., .F.,
 ( 4, 2, 2, 2, 4 ),
 ( 0.000000000000000000, 0.2500000000000000000, 0.5000000000000000000, 0.7500000000000000000, 1.000000000000000000 ),
 .UNSPECIFIED. ) ;
#13535=ORIENTED_EDGE ( 'NONE', *, *, #13491, .T. ) ;
#13539=ORIENTED_EDGE ( 'NONE', *, *, #12199, .F. ) ;
#13544=VECTOR ( 'NONE', #10762, 1000.000000000000000 ) ;
#13546=FACE_OUTER_BOUND ( 'NONE', #26037, .T. ) ;
#13585=EDGE_CURVE ( 'NONE', #49, #18717, #6669, .T. ) ;
#13586=ORIENTED_EDGE ( 'NONE', *, *, #14851, .T. ) ;
#13592=CARTESIAN_POINT ( 'NONE',  ( -10.00000000057898220, -121.7869891323785083, -31.32664466904982348 ) ) ;
#13595=B_SPLINE_CURVE_WITH_KNOTS ( 'NONE', 3,
 ( #10360, #29389, #8285, #19952, #17429, #30005 ),
 .UNSPECIFIED., .F., .F.,
 ( 4, 2, 4 ),
 ( 0.000000000000000000, 0.5000000000000000000, 1.000000000000000000 ),
 .UNSPECIFIED. ) ;
#13597=DIRECTION ( 'NONE',  ( 0.7071067811870488384, 0.000000000000000000, -0.7071067811860461960 ) ) ;
#13605=CARTESIAN_POINT ( 'NONE',  ( 18.65047562642688916, 19.27644483004725728, -1.399999999999998579 ) ) ;
#13609=DIRECTION ( 'NONE',  ( 0.000000000000000000, -1.000000000000000000, 0.000000000000000000 ) ) ;
#13612=CARTESIAN_POINT ( 'NONE',  ( -4.175165894169885483, -119.7166638525666826, -44.10000000000000142 ) ) ;
#13635=CYLINDRICAL_SURFACE ( 'NONE', #21543, 3.000000000000005329 ) ;
#13646=VECTOR ( 'NONE', #16506, 1000.000000000000000 ) ;
#13650=CARTESIAN_POINT ( 'NONE',  ( -16.66189934012373897, 9.903956624658377450, -1.400000000000001910 ) ) ;
#13683=DIRECTION ( 'NONE',  ( -1.000000000000000000, 0.000000000000000000, -2.257144471330000330E-12 ) ) ;
#13690=CARTESIAN_POINT ( 'NONE',  ( -10.00000000000000000, 19.99999999999999645, -42.39999999999999858 ) ) ;
#13698=CARTESIAN_POINT ( 'NONE',  ( 9.999999999949999108, -30.49251257979999963, -21.04205368479999905 ) ) ;
#13703=ORIENTED_EDGE ( 'NONE', *, *, #26382, .T. ) ;
#13706=VERTEX_POINT ( 'NONE', #2881 ) ;
#13725=DIRECTION ( 'NONE',  ( -5.551115123049999208E-18, 3.153710283929999911E-31, -1.000000000000000000 ) ) ;
#13729=VECTOR ( 'NONE', #17608, 1000.000000000000000 ) ;
#13736=ADVANCED_FACE ( 'NONE', ( #841 ), #15304, .T. ) ;
#13741=ORIENTED_EDGE ( 'NONE', *, *, #19054, .F. ) ;
#13742=LINE ( 'NONE', #25234, #16259 ) ;
#13743=EDGE_LOOP ( 'NONE', ( #25075, #753, #12447, #2945 ) ) ;
#13749=CARTESIAN_POINT ( 'NONE',  ( -10.00000000009184120, -24.60099947280526678, -30.24364015992614085 ) ) ;
#13766=VECTOR ( 'NONE', #6375, 1000.000000000000000 ) ;
#13782=CARTESIAN_POINT ( 'NONE',  ( 0.000000000000000000, 19.99999999999999645, -43.39999999999999858 ) ) ;
#13787=VECTOR ( 'NONE', #24146, 1000.000000000000000 ) ;
#13788=PLANE ( 'NONE',  #17553 ) ;
#13790=CARTESIAN_POINT ( 'NONE',  ( 9.785465176140000665, 19.99999999999999645, -43.02073679144999829 ) ) ;
#13801=CARTESIAN_POINT ( 'NONE',  ( 11.69999999989999928, -2.500000000000002220, -2.399999999999999467 ) ) ;
#13806=CARTESIAN_POINT ( 'NONE',  ( 9.999999999969999109, -24.00000000000000000, -28.40000000000000213 ) ) ;
#13813=VECTOR ( 'NONE', #22407, 1000.000000000000000 ) ;
#13825=ORIENTED_EDGE ( 'NONE', *, *, #21502, .T. ) ;
#13839=AXIS2_PLACEMENT_3D ( 'NONE', #10562, #29441, #26937 ) ;
#13852=EDGE_CURVE ( 'NONE', #28717, #15209, #29327, .T. ) ;
#13863=( NAMED_UNIT ( * ) SI_UNIT ( $, .STERADIAN. ) SOLID_ANGLE_UNIT ( ) );
#13866=EDGE_LOOP ( 'NONE', ( #17063, #16368, #25975, #26015, #12467, #4500 ) ) ;
#13867=CARTESIAN_POINT ( 'NONE',  ( 10.69999999999999929, -29.12132034360000077, -30.52132034359999935 ) ) ;
#13873=FACE_OUTER_BOUND ( 'NONE', #15321, .T. ) ;
#13881=CARTESIAN_POINT ( 'NONE',  ( 17.16657240490000191, -8.999999999699998199, -0.6999999999999992895 ) ) ;
#13887=CARTESIAN_POINT ( 'NONE',  ( -10.00000000038429704, -25.59790977654974142, -12.29094066695284226 ) ) ;
#13891=ORIENTED_EDGE ( 'NONE', *, *, #10403, .T. ) ;
#13893=DIRECTION ( 'NONE',  ( -0.000000000000000000, -0.000000000000000000, 1.000000000000000000 ) ) ;
#13902=ORIENTED_EDGE ( 'NONE', *, *, #13273, .F. ) ;
#13918=B_SPLINE_CURVE_WITH_KNOTS ( 'NONE', 3,
 ( #18672, #30333, #11601, #11293 ),
 .UNSPECIFIED., .F., .F.,
 ( 4, 4 ),
 ( 0.000000000000000000, 1.000000000000000000 ),
 .UNSPECIFIED. ) ;
#13920=ORIENTED_EDGE ( 'NONE', *, *, #25159, .F. ) ;
#13922=PLANE ( 'NONE',  #25757 ) ;
#13926=CARTESIAN_POINT ( 'NONE',  ( 11.69999999989999928, -24.11120071670000087, -1.399999999299995856 ) ) ;
#13928=CARTESIAN_POINT ( 'NONE',  ( 10.69999999999999929, -24.87867965640000278, -26.27867965640000136 ) ) ;
#13940=CARTESIAN_POINT ( 'NONE',  ( 10.46457122910000059, 21.70000000000000284, -54.63542873130000288 ) ) ;
#13945=EDGE_CURVE ( 'NONE', #11888, #1366, #10948, .T. ) ;
#13949=CARTESIAN_POINT ( 'NONE',  ( -12.57879864068154774, 21.69999999999986784, -55.96236416640539346 ) ) ;
#13950=CARTESIAN_POINT ( 'NONE',  ( 10.69999999993204653, -25.59803261866920465, -12.29454957252203151 ) ) ;
#13958=ORIENTED_EDGE ( 'NONE', *, *, #13585, .T. ) ;
#13967=CARTESIAN_POINT ( 'NONE',  ( -15.93711909997440301, 10.34626908942863466, -1.400000000000002132 ) ) ;
#13970=LINE ( 'NONE', #18203, #27372 ) ;
#13973=CARTESIAN_POINT ( 'NONE',  ( 11.69999999989999928, -2.055600358200002198, -1.399999999999998579 ) ) ;
#13988=FACE_OUTER_BOUND ( 'NONE', #1084, .T. ) ;
#13997=CARTESIAN_POINT ( 'NONE',  ( 12.77819780750000156, 20.99999999999999645, -56.09999999999999432 ) ) ;
#14004=LINE ( 'NONE', #25336, #12801 ) ;
#14007=CARTESIAN_POINT ( 'NONE',  ( -9.999999999879573664, 20.00000000000001066, -42.66179938841035124 ) ) ;
#14008=VECTOR ( 'NONE', #14224, 1000.000000000000000 ) ;
#14009=EDGE_CURVE ( 'NONE', #27171, #21717, #17289, .T. ) ;
#14011=CARTESIAN_POINT ( 'NONE',  ( -12.84240556079365270, 21.69999999994267270, -69.50012576675229070 ) ) ;
#14015=DIRECTION ( 'NONE',  ( 0.000000000000000000, 0.000000000000000000, 1.000000000000000000 ) ) ;
#14019=ORIENTED_EDGE ( 'NONE', *, *, #18210, .T. ) ;
#14022=VECTOR ( 'NONE', #10471, 1000.000000000000000 ) ;
#14026=CARTESIAN_POINT ( 'NONE',  ( 10.69999999996929141, -30.00000000000000355, -28.79453140544987377 ) ) ;
#14033=CYLINDRICAL_SURFACE ( 'NONE', #30191, 1.099999999999999201 ) ;
#14041=DIRECTION ( 'NONE',  ( 0.000000000000000000, 0.000000000000000000, -1.000000000000000000 ) ) ;
#14047=DIRECTION ( 'NONE',  ( -1.000000000000000000, -1.750660885084214717E-48, 4.045530494348897360E-18 ) ) ;
#14048=EDGE_LOOP ( 'NONE', ( #30545, #9052, #18056, #26099 ) ) ;
#14056=DIRECTION ( 'NONE',  ( 1.000000000000000000, 0.000000000000000000, 0.000000000000000000 ) ) ;
#14058=ORIENTED_EDGE ( 'NONE', *, *, #30478, .F. ) ;
#14062=ORIENTED_EDGE ( 'NONE', *, *, #30416, .F. ) ;
#14066=SURFACE_STYLE_USAGE ( .BOTH. , #4467 ) ;
#14069=ADVANCED_FACE ( 'NONE', ( #618 ), #26572, .T. ) ;
#14086=CARTESIAN_POINT ( 'NONE',  ( 9.999999999959999997, -24.97510463849999951, -26.18619911149999879 ) ) ;
#14088=ORIENTED_EDGE ( 'NONE', *, *, #15585, .T. ) ;
#14089=CARTESIAN_POINT ( 'NONE',  ( -10.69999999999999929, -24.09288384250000092, -29.20409973919999658 ) ) ;
#14108=CARTESIAN_POINT ( 'NONE',  ( -10.69999999999999929, -24.00000000000000000, -28.06060480569999882 ) ) ;
#14122=VECTOR ( 'NONE', #2929, 1000.000000000000000 ) ;
#14128=DIRECTION ( 'NONE',  ( -0.000000000000000000, -0.000000000000000000, 1.000000000000000000 ) ) ;
#14134=VERTEX_POINT ( 'NONE', #10359 ) ;
#14159=DIRECTION ( 'NONE',  ( -0.8775825618903718706, 0.4794255386042047262, 0.000000000000000000 ) ) ;
#14172=VERTEX_POINT ( 'NONE', #19950 ) ;
#14174=ORIENTED_EDGE ( 'NONE', *, *, #12266, .F. ) ;
#14176=ORIENTED_EDGE ( 'NONE', *, *, #27627, .F. ) ;
#14177=CARTESIAN_POINT ( 'NONE',  ( 9.000000000029999114, 21.00000000060000360, -70.09999999999999432 ) ) ;
#14182=DIRECTION ( 'NONE',  ( 1.595945597898660305E-12, -0.7071067811865475727, -0.7071067811865475727 ) ) ;
#14197=CARTESIAN_POINT ( 'NONE',  ( 17.74448149004798481, 10.05302898057284899, -1.400000000000001688 ) ) ;
#14199=CARTESIAN_POINT ( 'NONE',  ( -26.43116876448085861, -4.566970306898999965, -1.399999999999998579 ) ) ;
#14212=ORIENTED_EDGE ( 'NONE', *, *, #24664, .T. ) ;
#14224=DIRECTION ( 'NONE',  ( -1.000000000000000000, 0.000000000000000000, 0.000000000000000000 ) ) ;
#14227=B_SPLINE_CURVE_WITH_KNOTS ( 'NONE', 3,
 ( #17761, #25491, #5817, #3931 ),
 .UNSPECIFIED., .F., .F.,
 ( 4, 4 ),
 ( 0.000000000000000000, 1.000000000000000000 ),
 .UNSPECIFIED. ) ;
#14245=CIRCLE ( 'NONE', #7205, 1.000000000000000888 ) ;
#14253=AXIS2_PLACEMENT_3D ( 'NONE', #953, #17457, #19978 ) ;
#14265=CARTESIAN_POINT ( 'NONE',  ( 12.51085694015827521, 20.99999999989886845, -69.72135916545833823 ) ) ;
#14267=ORIENTED_EDGE ( 'NONE', *, *, #12638, .F. ) ;
#14279=PLANE ( 'NONE',  #11605 ) ;
#14280=EDGE_CURVE ( 'NONE', #9281, #29912, #13165, .T. ) ;
#14282=CARTESIAN_POINT ( 'NONE',  ( 10.46457122910000059, 21.70000000000000284, -54.63542873130000288 ) ) ;
#14285=ORIENTED_EDGE ( 'NONE', *, *, #2083, .T. ) ;
#14295=ORIENTED_EDGE ( 'NONE', *, *, #9589, .T. ) ;
#14302=CARTESIAN_POINT ( 'NONE',  ( -10.69999999999999929, -120.5233595621999996, -31.26042064940000387 ) ) ;
#14311=ADVANCED_FACE ( 'NONE', ( #1224 ), #8761, .F. ) ;
#14320=FACE_OUTER_BOUND ( 'NONE', #2215, .T. ) ;
#14322=VECTOR ( 'NONE', #18439, 1000.000000000000000 ) ;
#14326=CARTESIAN_POINT ( 'NONE',  ( 8.999999999770000869, 20.19161784319999953, -43.40000000028999949 ) ) ;
#14334=CYLINDRICAL_SURFACE ( 'NONE', #16771, 10.00000000000000355 ) ;
#14341=VERTEX_POINT ( 'NONE', #8598 ) ;
#14356=AXIS2_PLACEMENT_3D ( 'NONE', #13237, #8511, #7103 ) ;
#14357=STYLED_ITEM ( 'NONE', ( #16063 ), #4675 ) ;
#14358=LINE ( 'NONE', #25847, #21232 ) ;
#14362=CARTESIAN_POINT ( 'NONE',  ( 17.61443111645372639, 9.985034189246265512, -1.400000000000002132 ) ) ;
#14366=DIRECTION ( 'NONE',  ( -1.000000000000000000, 0.000000000000000000, 0.000000000000000000 ) ) ;
#14372=ORIENTED_EDGE ( 'NONE', *, *, #14640, .F. ) ;
#14393=CARTESIAN_POINT ( 'NONE',  ( -8.999999999699999975, 20.99999999990000887, -70.09999999999999432 ) ) ;
#14397=CARTESIAN_POINT ( 'NONE',  ( -13.39962415728801304, 21.69999999994393036, -68.94292916387466619 ) ) ;
#14399=CARTESIAN_POINT ( 'NONE',  ( -10.69999999999999929, -24.00010364340000280, -28.42731455210000036 ) ) ;
#14405=CARTESIAN_POINT ( 'NONE',  ( 10.00000000000000000, -55.00000000000000000, -42.39999999999999858 ) ) ;
#14410=EDGE_LOOP ( 'NONE', ( #5526, #24728, #21753, #13059 ) ) ;
#14412=EDGE_CURVE ( 'NONE', #18576, #22920, #12506, .T. ) ;
#14428=LINE ( 'NONE', #9377, #26226 ) ;
#14430=CARTESIAN_POINT ( 'NONE',  ( 8.999999999770000869, 20.26086086378412432, -44.12622114747841096 ) ) ;
#14432=CARTESIAN_POINT ( 'NONE',  ( -10.69999999930000101, -27.00000000000000000, -31.39999999999999858 ) ) ;
#14435=CARTESIAN_POINT ( 'NONE',  ( 4.175165894169885483, -50.49316738903675628, -63.39999999999999858 ) ) ;
#14452=CARTESIAN_POINT ( 'NONE',  ( -10.46447140189999914, 20.99999999999999645, -54.63552859760000047 ) ) ;
#14456=CARTESIAN_POINT ( 'NONE',  ( 16.71871369222880688, 12.01496581087208249, -1.400000000000002132 ) ) ;
#14462=LINE ( 'NONE', #2040, #17998 ) ;
#14463=EDGE_CURVE ( 'NONE', #3949, #6922, #11292, .T. ) ;
#14469=DIRECTION ( 'NONE',  ( -1.000000000000000000, 0.000000000000000000, 0.000000000000000000 ) ) ;
#14472=CARTESIAN_POINT ( 'NONE',  ( -10.69999999999999929, -125.6542114415999976, -32.94738679099999956 ) ) ;
#14482=PLANE ( 'NONE',  #1195 ) ;
#14484=ORIENTED_EDGE ( 'NONE', *, *, #2406, .T. ) ;
#14485=EDGE_LOOP ( 'NONE', ( #25669, #21486, #2598, #12929 ) ) ;
#14494=EDGE_CURVE ( 'NONE', #20670, #28644, #25208, .T. ) ;
#14501=EDGE_LOOP ( 'NONE', ( #10941, #629, #23539, #17716 ) ) ;
#14509=DIRECTION ( 'NONE',  ( -1.000000000000000000, 0.000000000000000000, 0.000000000000000000 ) ) ;
#14513=CARTESIAN_POINT ( 'NONE',  ( -12.47330046629999956, 20.99999999999999645, -55.90292611659999977 ) ) ;
#14514=ORIENTED_EDGE ( 'NONE', *, *, #21227, .F. ) ;
#14515=VECTOR ( 'NONE', #8011, 1000.000000000000000 ) ;
#14521=EDGE_CURVE ( 'NONE', #145, #15176, #6427, .T. ) ;
#14526=DIRECTION ( 'NONE',  ( -2.966217977826874882E-25, -1.000000000000000000, 2.257145581549900232E-12 ) ) ;
#14539=DIRECTION ( 'NONE',  ( -0.000000000000000000, 1.000000000000000000, -2.258510841069999963E-12 ) ) ;
#14545=LINE ( 'NONE', #29154, #6148 ) ;
#14550=CARTESIAN_POINT ( 'NONE',  ( 10.00000000000000000, 21.69999999990000106, -70.10000000019999788 ) ) ;
#14553=ORIENTED_EDGE ( 'NONE', *, *, #24892, .F. ) ;
#14576=CARTESIAN_POINT ( 'NONE',  ( -10.70000000000015206, -26.27037943353427707, -25.46729144951078183 ) ) ;
#14577=DIRECTION ( 'NONE',  ( 0.000000000000000000, 0.000000000000000000, 1.000000000000000000 ) ) ;
#14579=FACE_OUTER_BOUND ( 'NONE', #29782, .T. ) ;
#14583=CYLINDRICAL_SURFACE ( 'NONE', #18797, 3.000000000000001776 ) ;
#14592=FACE_OUTER_BOUND ( 'NONE', #9601, .T. ) ;
#14595=PLANE ( 'NONE',  #22865 ) ;
#14597=EDGE_LOOP ( 'NONE', ( #21225, #3013, #23156, #8897 ) ) ;
#14603=ORIENTED_EDGE ( 'NONE', *, *, #12881, .F. ) ;
#14610=CARTESIAN_POINT ( 'NONE',  ( 9.707106781189999367, 19.99999999999999645, -43.10710678118599759 ) ) ;
#14622=DIRECTION ( 'NONE',  ( 0.000000000000000000, 0.000000000000000000, -1.000000000000000000 ) ) ;
#14630=DIRECTION ( 'NONE',  ( -1.000000000000000000, 0.000000000000000000, 0.000000000000000000 ) ) ;
#14631=ORIENTED_EDGE ( 'NONE', *, *, #2021, .T. ) ;
#14636=CARTESIAN_POINT ( 'NONE',  ( 7.797918471980000099, -130.0000000000000000, -43.60208152801600079 ) ) ;
#14638=ORIENTED_EDGE ( 'NONE', *, *, #2925, .T. ) ;
#14640=EDGE_CURVE ( 'NONE', #10748, #1470, #20074, .T. ) ;
#14645=VERTEX_POINT ( 'NONE', #1185 ) ;
#14648=CARTESIAN_POINT ( 'NONE',  ( 8.999999999770000869, 20.70710678120000381, -44.39289321881399530 ) ) ;
#14666=CARTESIAN_POINT ( 'NONE',  ( -10.69999999999999929, -29.12132034360000077, -30.52132034359999935 ) ) ;
#14689=PLANE ( 'NONE',  #9448 ) ;
#14690=ORIENTED_EDGE ( 'NONE', *, *, #7540, .F. ) ;
#14693=EDGE_CURVE ( 'NONE', #28151, #6267, #30289, .T. ) ;
#14701=CYLINDRICAL_SURFACE ( 'NONE', #25780, 4.175165894169885483 ) ;
#14703=CARTESIAN_POINT ( 'NONE',  ( -13.12132034329999897, 21.69999999990000106, -69.22132034359999864 ) ) ;
#14707=CARTESIAN_POINT ( 'NONE',  ( -2.299991308520000465E-10, 21.70000000000000284, -64.10000000000000853 ) ) ;
#14709=CARTESIAN_POINT ( 'NONE',  ( 9.999999999930961891, -25.59790977665528189, -12.29094066744903557 ) ) ;
#14714=CARTESIAN_POINT ( 'NONE',  ( 10.69999999999999929, -27.00000000000000000, -28.40000000000000213 ) ) ;
#14731=CARTESIAN_POINT ( 'NONE',  ( 9.999999999959999997, -29.06670649020000141, -26.22546295170000263 ) ) ;
#14755=CARTESIAN_POINT ( 'NONE',  ( -15.86808677770000209, 10.47263190749999495, -0.7999999992999995424 ) ) ;
#14756=EDGE_CURVE ( 'NONE', #26453, #27866, #25147, .T. ) ;
#14759=AXIS2_PLACEMENT_3D ( 'NONE', #16445, #7465, #26054 ) ;
#14760=CARTESIAN_POINT ( 'NONE',  ( 16.27026390832094549, 11.65373091049968579, -1.400000000000002132 ) ) ;
#14764=ORIENTED_EDGE ( 'NONE', *, *, #14463, .F. ) ;
#14768=CARTESIAN_POINT ( 'NONE',  ( 12.70701705218868760, 21.70000000000012363, -56.04761461377552223 ) ) ;
#14771=FACE_OUTER_BOUND ( 'NONE', #2268, .T. ) ;
#14773=FACE_OUTER_BOUND ( 'NONE', #14794, .T. ) ;
#14778=EDGE_CURVE ( 'NONE', #26791, #12935, #12419, .T. ) ;
#14782=VERTEX_POINT ( 'NONE', #23383 ) ;
#14783=VECTOR ( 'NONE', #13287, 1000.000000000000000 ) ;
#14786=CARTESIAN_POINT ( 'NONE',  ( -10.00000000063852035, -42.68965130439637790, -27.18132884625137535 ) ) ;
#14788=VERTEX_POINT ( 'NONE', #18481 ) ;
#14794=EDGE_LOOP ( 'NONE', ( #4341, #5581, #2795, #2637 ) ) ;
#14799=CARTESIAN_POINT ( 'NONE',  ( 9.999999999959999997, -29.30501631460000311, -26.47986984960000001 ) ) ;
#14803=CARTESIAN_POINT ( 'NONE',  ( -10.00000000070000183, -27.00000000000000000, -25.39999999999999858 ) ) ;
#14805=CARTESIAN_POINT ( 'NONE',  ( -10.69999999999999929, -27.00000000000000000, -28.40000000000000213 ) ) ;
#14807=ORIENTED_EDGE ( 'NONE', *, *, #8533, .T. ) ;
#14811=CIRCLE ( 'NONE', #23798, 1.700000000000000178 ) ;
#14815=CARTESIAN_POINT ( 'NONE',  ( -2.299991308520000465E-10, 21.70000000000000284, -60.10000000000000142 ) ) ;
#14818=CARTESIAN_POINT ( 'NONE',  ( 9.999999999964986230, -24.37875421243714058, -26.88867997429543166 ) ) ;
#14821=CARTESIAN_POINT ( 'NONE',  ( 10.69999999930000101, -25.00000000000000000, -26.16393202249999916 ) ) ;
#14827=CARTESIAN_POINT ( 'NONE',  ( 13.99999999977382359, 20.99999999989910293, -67.49269908208931668 ) ) ;
#14828=ORIENTED_EDGE ( 'NONE', *, *, #26734, .T. ) ;
#14834=CARTESIAN_POINT ( 'NONE',  ( -11.69999999989999928, -2.500000000000002220, -0.6999999999999992895 ) ) ;
#14839=ORIENTED_EDGE ( 'NONE', *, *, #7528, .T. ) ;
#14840=CARTESIAN_POINT ( 'NONE',  ( 13.99999999979999821, 20.99999999999999645, -51.10000000000000142 ) ) ;
#14846=DIRECTION ( 'NONE',  ( -1.000000000000000000, 0.000000000000000000, 0.000000000000000000 ) ) ;
#14851=EDGE_CURVE ( 'NONE', #30214, #23190, #17474, .T. ) ;
#14852=CARTESIAN_POINT ( 'NONE',  ( -10.69999999994010587, -26.89373798101190616, -15.86471592097247019 ) ) ;
#14857=LINE ( 'NONE', #5087, #26306 ) ;
#14860=LINE ( 'NONE', #19888, #11708 ) ;
#14861=ADVANCED_FACE ( 'NONE', ( #11564, #2121, #21161 ), #9187, .F. ) ;
#14866=CARTESIAN_POINT ( 'NONE',  ( -10.69999999999999929, -130.0000000000000000, -41.82335799894999440 ) ) ;
#14869=PRODUCT_DEFINITION_FORMATION_WITH_SPECIFIED_SOURCE ( 'ANY', '', #9142, .NOT_KNOWN. ) ;
#14876=DIRECTION ( 'NONE',  ( 1.000000000000000000, 0.000000000000000000, -2.257150022439999944E-12 ) ) ;
#14891=DIRECTION ( 'NONE',  ( 0.000000000000000000, 0.000000000000000000, -1.000000000000000000 ) ) ;
#14899=DIRECTION ( 'NONE',  ( -1.553705081258627072E-12, -0.7253743710120287291, 0.6883545756940268046 ) ) ;
#14901=ORIENTED_EDGE ( 'NONE', *, *, #14463, .T. ) ;
#14902=CARTESIAN_POINT ( 'NONE',  ( 10.40384844070000092, -24.69832375569999883, -1.291913789700005477 ) ) ;
#14910=DIRECTION ( 'NONE',  ( 0.000000000000000000, -2.259525899719999991E-12, -1.000000000000000000 ) ) ;
#14911=ADVANCED_FACE ( 'NONE', ( #29157 ), #19107, .T. ) ;
#14912=ORIENTED_EDGE ( 'NONE', *, *, #19856, .T. ) ;
#14917=CARTESIAN_POINT ( 'NONE',  ( 17.82030331447854010, 11.89630849604035845, -1.400000000000001910 ) ) ;
#14942=ORIENTED_EDGE ( 'NONE', *, *, #21502, .F. ) ;
#14950=CARTESIAN_POINT ( 'NONE',  ( -11.78524365341753466, 20.99999999990017585, -70.02191802985640834 ) ) ;
#14957=CARTESIAN_POINT ( 'NONE',  ( -10.69999999995573958, -32.31934595230423923, -22.79266741176987310 ) ) ;
#14965=DIRECTION ( 'NONE',  ( 0.000000000000000000, -1.000000000000000000, 2.257145581549999994E-12 ) ) ;
#14971=CARTESIAN_POINT ( 'NONE',  ( 16.40025437452154478, 10.19782190223724072, -1.400000000000001910 ) ) ;
#14975=ORIENTED_EDGE ( 'NONE', *, *, #2577, .F. ) ;
#14985=CIRCLE ( 'NONE', #20007, 4.175165894169885483 ) ;
#14990=CARTESIAN_POINT ( 'NONE',  ( -10.69999999999999929, -24.92624642180000194, -26.23177034519999751 ) ) ;
#15002=DIRECTION ( 'NONE',  ( 0.5193310806158223381, 1.929012505286207873E-12, 0.8545731265997089654 ) ) ;
#15003=CYLINDRICAL_SURFACE ( 'NONE', #3177, 5.000000000000003553 ) ;
#15007=CARTESIAN_POINT ( 'NONE',  ( 11.69999999989999928, -25.00000000000000000, -2.399999999999999467 ) ) ;
#15012=VECTOR ( 'NONE', #13383, 1000.000000000000000 ) ;
#15021=VERTEX_POINT ( 'NONE', #2736 ) ;
#15027=CYLINDRICAL_SURFACE ( 'NONE', #866, 3.000000000000000444 ) ;
#15028=ADVANCED_FACE ( 'NONE', ( #12333 ), #549, .F. ) ;
#15032=CARTESIAN_POINT ( 'NONE',  ( -15.86808677770000209, -9.527368092500001495, -1.399999999599998990 ) ) ;
#15041=LINE ( 'NONE', #5430, #1737 ) ;
#15047=EDGE_CURVE ( 'NONE', #10599, #5374, #21108, .T. ) ;
#15049=CARTESIAN_POINT ( 'NONE',  ( 10.69999999999999929, -30.00000000000000000, -28.40000000000000213 ) ) ;
#15050=DIRECTION ( 'NONE',  ( 0.000000000000000000, 1.000000000000000000, 0.000000000000000000 ) ) ;
#15051=LINE ( 'NONE', #12675, #14122 ) ;
#15056=CARTESIAN_POINT ( 'NONE',  ( 10.79767714369999965, -24.52928866599999935, -0.9448357716000042039 ) ) ;
#15059=ORIENTED_EDGE ( 'NONE', *, *, #13051, .F. ) ;
#15066=CARTESIAN_POINT ( 'NONE',  ( 18.13191322229999969, -9.527368092500001495, -1.399999999599998990 ) ) ;
#15067=UNCERTAINTY_MEASURE_WITH_UNIT (LENGTH_MEASURE( 1.000000000000000082E-05 ), #19091, 'distance_accuracy_value', 'NONE');
#15069=CARTESIAN_POINT ( 'NONE',  ( 10.69999999996760742, -29.99999999999999645, -28.04933239862057803 ) ) ;
#15085=PLANE ( 'NONE',  #6751 ) ;
#15090=AXIS2_PLACEMENT_3D ( 'NONE', #1093, #8311, #17906 ) ;
#15093=CARTESIAN_POINT ( 'NONE',  ( -10.00000000007662138, -32.32189936806710762, -22.79484972449596469 ) ) ;
#15100=ORIENTED_EDGE ( 'NONE', *, *, #30446, .F. ) ;
#15101=VECTOR ( 'NONE', #24505, 1000.000000000000000 ) ;
#15104=CARTESIAN_POINT ( 'NONE',  ( 9.999999999966957986, -29.70271642751552221, -27.05243720740120139 ) ) ;
#15121=EDGE_CURVE ( 'NONE', #7509, #27320, #21422, .T. ) ;
#15123=DIRECTION ( 'NONE',  ( 0.000000000000000000, -1.000000000000000000, 2.257145581549999994E-12 ) ) ;
#15130=ORIENTED_EDGE ( 'NONE', *, *, #5558, .F. ) ;
#15135=EDGE_CURVE ( 'NONE', #18136, #11286, #20948, .T. ) ;
#15137=EDGE_LOOP ( 'NONE', ( #10379, #1314, #6303, #26214 ) ) ;
#15141=LINE ( 'NONE', #22392, #13490 ) ;
#15142=ORIENTED_EDGE ( 'NONE', *, *, #10080, .T. ) ;
#15143=EDGE_CURVE ( 'NONE', #27949, #12805, #9963, .T. ) ;
#15166=CARTESIAN_POINT ( 'NONE',  ( -10.69999999999999929, -25.00000000000000000, -26.16393202249999916 ) ) ;
#15173=DIRECTION ( 'NONE',  ( 0.000000000000000000, 1.000000000000000000, 0.000000000000000000 ) ) ;
#15175=LINE ( 'NONE', #24780, #10227 ) ;
#15176=VERTEX_POINT ( 'NONE', #30552 ) ;
#15198=EDGE_LOOP ( 'NONE', ( #19102, #9412, #6101, #19016 ) ) ;
#15199=LINE ( 'NONE', #8410, #9743 ) ;
#15201=CARTESIAN_POINT ( 'NONE',  ( 9.999999999979998222, -127.2537437101000108, -34.36317024011000143 ) ) ;
#15202=CARTESIAN_POINT ( 'NONE',  ( 16.20123158649999695, 11.52736809289999620, -0.6999999999999992895 ) ) ;
#15206=ORIENTED_EDGE ( 'NONE', *, *, #16603, .F. ) ;
#15208=EDGE_CURVE ( 'NONE', #30391, #5518, #8248, .T. ) ;
#15209=VERTEX_POINT ( 'NONE', #24698 ) ;
#15210=EDGE_LOOP ( 'NONE', ( #7165, #25752, #14285, #13703 ) ) ;
#15211=CARTESIAN_POINT ( 'NONE',  ( 9.999999999979998222, -27.00000000000000000, -31.39999999999999858 ) ) ;
#15229=CARTESIAN_POINT ( 'NONE',  ( -16.43242232095159139, 12.03437313996399105, -1.400000000000002132 ) ) ;
#15237=DIRECTION ( 'NONE',  ( 1.553791817432423893E-12, -0.7253743710120292842, 0.6883545756940262494 ) ) ;
#15243=VECTOR ( 'NONE', #13066, 1000.000000000000000 ) ;
#15245=ADVANCED_FACE ( 'NONE', ( #7553 ), #19673, .F. ) ;
#15248=DIRECTION ( 'NONE',  ( 0.7071067811865466846, 1.595945597898659700E-12, 0.7071067811865484609 ) ) ;
#15265=AXIS2_PLACEMENT_3D ( 'NONE', #2051, #8966, #11797 ) ;
#15267=CARTESIAN_POINT ( 'NONE',  ( 9.499999999770000869, 21.70000000000000284, -60.10000000000000142 ) ) ;
#15282=ORIENTED_EDGE ( 'NONE', *, *, #2021, .F. ) ;
#15283=ORIENTED_EDGE ( 'NONE', *, *, #21680, .F. ) ;
#15288=CIRCLE ( 'NONE', #19318, 1.100000000390000787 ) ;
#15290=AXIS2_PLACEMENT_3D ( 'NONE', #24424, #2859, #29598 ) ;
#15293=AXIS2_PLACEMENT_3D ( 'NONE', #13801, #28268, #27962 ) ;
#15304=PLANE ( 'NONE',  #5455 ) ;
#15321=EDGE_LOOP ( 'NONE', ( #26851, #17520, #7321, #5027, #15935 ) ) ;
#15322=EDGE_CURVE ( 'NONE', #9489, #22831, #644, .T. ) ;
#15327=CARTESIAN_POINT ( 'NONE',  ( -12.12499970569999874, 20.99999999999999645, -55.73512393480000071 ) ) ;
#15337=ORIENTED_EDGE ( 'NONE', *, *, #23865, .T. ) ;
#15338=UNCERTAINTY_MEASURE_WITH_UNIT (LENGTH_MEASURE( 1.000000000000000082E-05 ), #16215, 'distance_accuracy_value', 'NONE');
#15341=VERTEX_POINT ( 'NONE', #14648 ) ;
#15354=EDGE_CURVE ( 'NONE', #6694, #22920, #9775, .T. ) ;
#15360=CARTESIAN_POINT ( 'NONE',  ( -9.000000000229999131, 20.99999999999999645, -53.60000000000000142 ) ) ;
#15367=VERTEX_POINT ( 'NONE', #8709 ) ;
#15374=DIRECTION ( 'NONE',  ( -1.000000000000000000, -6.565028073413479156E-24, -2.257144471327815248E-12 ) ) ;
#15394=CARTESIAN_POINT ( 'NONE',  ( 13.99999999979999821, 21.69999999929999390, -67.09999999999999432 ) ) ;
#15404=DIRECTION ( 'NONE',  ( -1.595945597898660305E-12, -0.7071067811865475727, -0.7071067811865475727 ) ) ;
#15426=EDGE_CURVE ( 'NONE', #15866, #30881, #6361, .T. ) ;
#15427=CARTESIAN_POINT ( 'NONE',  ( -8.999999999970000886, 19.99999999999999645, -45.10000000000000142 ) ) ;
#15428=CARTESIAN_POINT ( 'NONE',  ( 11.69999999989999928, 19.99999999999999645, -0.6999999999999992895 ) ) ;
#15433=VECTOR ( 'NONE', #29334, 1000.000000000000000 ) ;
#15437=EDGE_CURVE ( 'NONE', #20967, #16094, #18407, .T. ) ;
#15457=CARTESIAN_POINT ( 'NONE',  ( -12.12499970569999874, 20.99999999999999645, -55.73512393480000071 ) ) ;
#15465=EDGE_CURVE ( 'NONE', #7630, #16094, #31059, .T. ) ;
#15468=EDGE_CURVE ( 'NONE', #14645, #9943, #10882, .T. ) ;
#15478=ORIENTED_EDGE ( 'NONE', *, *, #24567, .T. ) ;
#15479=DIRECTION ( 'NONE',  ( 0.000000000000000000, 1.000000000000000000, 0.000000000000000000 ) ) ;
#15485=CARTESIAN_POINT ( 'NONE',  ( 10.46446609389999871, 20.99999999999999645, -54.63553390589999736 ) ) ;
#15486=CARTESIAN_POINT ( 'NONE',  ( -26.85688130224987091, -1.306556711637668622, -1.399999999999998579 ) ) ;
#15500=PLANE ( 'NONE',  #6234 ) ;
#15501=VERTEX_POINT ( 'NONE', #22654 ) ;
#15505=PLANE ( 'NONE',  #8199 ) ;
#15523=ORIENTED_EDGE ( 'NONE', *, *, #7842, .T. ) ;
#15524=CARTESIAN_POINT ( 'NONE',  ( 10.99999999979999998, 20.99999999999999645, -58.51619795479999908 ) ) ;
#15538=CARTESIAN_POINT ( 'NONE',  ( -12.12499970530000049, 21.69999999919999212, -55.73512393530000253 ) ) ;
#15542=ORIENTED_EDGE ( 'NONE', *, *, #16313, .F. ) ;
#15544=CARTESIAN_POINT ( 'NONE',  ( 13.40012576665181321, 21.69999999994393391, -68.94240556069520665 ) ) ;
#15548=ORIENTED_EDGE ( 'NONE', *, *, #5839, .F. ) ;
#15549=ORIENTED_EDGE ( 'NONE', *, *, #24315, .T. ) ;
#15577=B_SPLINE_CURVE_WITH_KNOTS ( 'NONE', 3,
 ( #537, #21931, #29147, #13950, #17188, #23563, #26790, #5234, #12009, #19720 ),
 .UNSPECIFIED., .F., .F.,
 ( 4, 2, 2, 2, 4 ),
 ( 0.000000000000000000, 0.2500000000000000000, 0.5000000000000000000, 0.7500000000000000000, 1.000000000000000000 ),
 .UNSPECIFIED. ) ;
#15585=EDGE_CURVE ( 'NONE', #27858, #5618, #5963, .T. ) ;
#15590=CARTESIAN_POINT ( 'NONE',  ( 10.69999999930000101, -24.00000000000000000, -28.40000000000000213 ) ) ;
#15592=ORIENTED_EDGE ( 'NONE', *, *, #4950, .F. ) ;
#15598=ADVANCED_FACE ( 'NONE', ( #10389 ), #3295, .F. ) ;
#15604=CARTESIAN_POINT ( 'NONE',  ( -9.999999999919999993, -25.00000000000000000, -7.274962171499997687 ) ) ;
#15618=VERTEX_POINT ( 'NONE', #27374 ) ;
#15637=ORIENTED_EDGE ( 'NONE', *, *, #11548, .F. ) ;
#15642=CARTESIAN_POINT ( 'NONE',  ( 9.999999999959999997, -29.06670649020000141, -26.22546295170000263 ) ) ;
#15655=CIRCLE ( 'NONE', #11644, 4.175165894169885483 ) ;
#15665=ORIENTED_EDGE ( 'NONE', *, *, #1965, .F. ) ;
#15690=DIRECTION ( 'NONE',  ( 0.000000000000000000, -2.256683728769999802E-12, -1.000000000000000000 ) ) ;
#15692=DIRECTION ( 'NONE',  ( 0.000000000000000000, 1.000000000000000000, 0.000000000000000000 ) ) ;
#15695=ORIENTED_EDGE ( 'NONE', *, *, #14009, .T. ) ;
#15696=CARTESIAN_POINT ( 'NONE',  ( -10.69999999999999929, -120.0000000000000000, -41.24671599700000257 ) ) ;
#15726=ORIENTED_EDGE ( 'NONE', *, *, #15354, .F. ) ;
#15735=FACE_OUTER_BOUND ( 'NONE', #18421, .T. ) ;
#15738=VERTEX_POINT ( 'NONE', #27833 ) ;
#15755=ADVANCED_FACE ( 'NONE', ( #18225 ), #18068, .F. ) ;
#15758=VECTOR ( 'NONE', #23961, 1000.000000000000000 ) ;
#15767=CARTESIAN_POINT ( 'NONE',  ( 8.999999999769999093, 20.97450841549535028, -44.83935997348105928 ) ) ;
#15781=FACE_OUTER_BOUND ( 'NONE', #2137, .T. ) ;
#15784=CARTESIAN_POINT ( 'NONE',  ( 10.69999999949999925, 19.99999999999999645, -2.302021179699999198 ) ) ;
#15805=ADVANCED_FACE ( 'NONE', ( #1415 ), #10855, .F. ) ;
#15806=VECTOR ( 'NONE', #16202, 1000.000000000000000 ) ;
#15809=ORIENTED_EDGE ( 'NONE', *, *, #6584, .F. ) ;
#15817=VECTOR ( 'NONE', #6596, 1000.000000000000000 ) ;
#15820=CARTESIAN_POINT ( 'NONE',  ( -11.59065746630000149, -24.20066399839999960, -1.404983722500002807 ) ) ;
#15827=EDGE_CURVE ( 'NONE', #24348, #27161, #29656, .T. ) ;
#15829=CARTESIAN_POINT ( 'NONE',  ( -16.83342759559999635, -9.000000000000001776, -1.399999999999998579 ) ) ;
#15832=DIRECTION ( 'NONE',  ( 0.000000000000000000, -1.000000000000000000, 0.000000000000000000 ) ) ;
#15848=VECTOR ( 'NONE', #20329, 1000.000000000000000 ) ;
#15849=CARTESIAN_POINT ( 'NONE',  ( 8.999999999770000869, 21.70000000000000284, -58.10000000000000142 ) ) ;
#15858=CARTESIAN_POINT ( 'NONE',  ( -15.86808677770000209, 10.47263190749999495, -1.399999999599998990 ) ) ;
#15863=EDGE_CURVE ( 'NONE', #23914, #11684, #7217, .T. ) ;
#15866=VERTEX_POINT ( 'NONE', #9578 ) ;
#15869=EDGE_CURVE ( 'NONE', #7509, #12603, #21542, .T. ) ;
#15874=ORIENTED_EDGE ( 'NONE', *, *, #22076, .F. ) ;
#15882=DIRECTION ( 'NONE',  ( 0.9915824307782121760, -0.1294769592320275942, 0.000000000000000000 ) ) ;
#15888=FACE_OUTER_BOUND ( 'NONE', #3977, .T. ) ;
#15889=CARTESIAN_POINT ( 'NONE',  ( 10.00000000000000000, -130.0000000000000000, -42.39999999999999858 ) ) ;
#15903=VERTEX_POINT ( 'NONE', #19334 ) ;
#15914=CARTESIAN_POINT ( 'NONE',  ( -10.69999999999999929, -30.00000000000000000, -28.40000000000000213 ) ) ;
#15916=ADVANCED_FACE ( 'NONE', ( #16805 ), #12240, .T. ) ;
#15918=EDGE_CURVE ( 'NONE', #13159, #15501, #14462, .T. ) ;
#15931=CARTESIAN_POINT ( 'NONE',  ( -10.00000000049220006, -25.12044511663835422, -9.805662262113871819 ) ) ;
#15935=ORIENTED_EDGE ( 'NONE', *, *, #10016, .T. ) ;
#15942=ORIENTED_EDGE ( 'NONE', *, *, #14693, .T. ) ;
#15949=ADVANCED_FACE ( 'NONE', ( #21043 ), #6554, .T. ) ;
#15965=DIRECTION ( 'NONE',  ( 0.000000000000000000, -2.257145581549999994E-12, -1.000000000000000000 ) ) ;
#15970=CARTESIAN_POINT ( 'NONE',  ( -4.175165894169885483, -50.49316738903675628, -63.39999999999999858 ) ) ;
#15973=ORIENTED_EDGE ( 'NONE', *, *, #12854, .T. ) ;
#15975=CARTESIAN_POINT ( 'NONE',  ( 9.000000000029999114, 21.70000000000000284, -64.10000000000000853 ) ) ;
#15983=CARTESIAN_POINT ( 'NONE',  ( 0.000000000000000000, -55.00000000000000000, -43.39999999999999858 ) ) ;
#15985=ORIENTED_EDGE ( 'NONE', *, *, #28751, .T. ) ;
#15992=CARTESIAN_POINT ( 'NONE',  ( 10.69999999999999929, -27.00000000000000000, -28.40000000000000213 ) ) ;
#15993=CYLINDRICAL_SURFACE ( 'NONE', #7474, 2.999999999999998668 ) ;
#16009=CARTESIAN_POINT ( 'NONE',  ( -17.48715850607838007, 10.10369150396071625, -1.400000000000001910 ) ) ;
#16017=CARTESIAN_POINT ( 'NONE',  ( 10.69999999999999929, -27.00000000000000000, -31.39999999999999858 ) ) ;
#16023=EDGE_LOOP ( 'NONE', ( #28172, #28951, #16364, #18530 ) ) ;
#16024=ORIENTED_EDGE ( 'NONE', *, *, #1150, .F. ) ;
#16035=CARTESIAN_POINT ( 'NONE',  ( -10.69999999999999929, -27.00000000000000000, -28.40000000000000213 ) ) ;
#16039=AXIS2_PLACEMENT_3D ( 'NONE', #414, #22112, #17220 ) ;
#16047=LINE ( 'NONE', #18711, #30402 ) ;
#16051=CARTESIAN_POINT ( 'NONE',  ( -8.999999999710000864, 21.35000000040000145, -51.10000000000000142 ) ) ;
#16052=DIRECTION ( 'NONE',  ( -2.254056676789046554E-12, 0.05233595624287792208, -0.9986295347545773859 ) ) ;
#16055=DIRECTION ( 'NONE',  ( -1.000000000000000000, 0.000000000000000000, 0.000000000000000000 ) ) ;
#16058=ORIENTED_EDGE ( 'NONE', *, *, #10913, .T. ) ;
#16062=AXIS2_PLACEMENT_3D ( 'NONE', #15992, #21034, #6699 ) ;
#16063=PRESENTATION_STYLE_ASSIGNMENT (( #4263 ) ) ;
#16082=CARTESIAN_POINT ( 'NONE',  ( -11.69999999989999928, -24.11120071630000083, -1.399999999999998579 ) ) ;
#16083=CARTESIAN_POINT ( 'NONE',  ( 9.000000000029999114, 20.99999999999999645, -45.10000000000000142 ) ) ;
#16091=EDGE_LOOP ( 'NONE', ( #11593, #23123, #8035, #11087 ) ) ;
#16094=VERTEX_POINT ( 'NONE', #4826 ) ;
#16098=ADVANCED_FACE ( 'NONE', ( #7177 ), #9541, .T. ) ;
#16103=CARTESIAN_POINT ( 'NONE',  ( -9.999999999949999108, -30.49286765380000119, -21.04171673159999756 ) ) ;
#16116=B_SPLINE_CURVE_WITH_KNOTS ( 'NONE', 5,
 ( #9428, #30996, #28475, #2212, #28633, #11799, #16206, #11493, #6916, #25971, #6765, #4719 ),
 .UNSPECIFIED., .F., .F.,
 ( 6, 3, 3, 6 ),
 ( 0.000000000000000000, 1.357884647199999906, 2.715789078020000247, 3.784579751639999934 ),
 .UNSPECIFIED. ) ;
#16120=CARTESIAN_POINT ( 'NONE',  ( -10.69999999999999929, -128.3726541643999894, -35.73121451845000252 ) ) ;
#16121=CARTESIAN_POINT ( 'NONE',  ( 10.99999999979999998, 20.99999999990000887, -70.09999999999999432 ) ) ;
#16125=CARTESIAN_POINT ( 'NONE',  ( 9.999999999959999997, -24.87868334570000073, -26.27868334529999927 ) ) ;
#16138=EDGE_CURVE ( 'NONE', #20193, #23914, #18976, .T. ) ;
#16143=DIRECTION ( 'NONE',  ( 0.000000000000000000, 1.000000000000000000, 0.000000000000000000 ) ) ;
#16146=B_SPLINE_CURVE_WITH_KNOTS ( 'NONE', 3,
 ( #2517, #2665, #24223, #9905, #17556, #15201 ),
 .UNSPECIFIED., .F., .F.,
 ( 4, 2, 4 ),
 ( 0.000000000000000000, 0.5000000000000000000, 1.000000000000000000 ),
 .UNSPECIFIED. ) ;
#16154=LINE ( 'NONE', #25616, #24841 ) ;
#16156=DIRECTION ( 'NONE',  ( 1.000000000000000000, 0.000000000000000000, 0.000000000000000000 ) ) ;
#16164=CARTESIAN_POINT ( 'NONE',  ( 0.000000000000000000, 20.99999999999999645, -44.10000000017154065 ) ) ;
#16172=ORIENTED_EDGE ( 'NONE', *, *, #6842, .F. ) ;
#16174=VERTEX_POINT ( 'NONE', #29038 ) ;
#16178=CARTESIAN_POINT ( 'NONE',  ( -10.69999999999999929, -27.00000000000000000, -28.40000000000000213 ) ) ;
#16202=DIRECTION ( 'NONE',  ( 0.000000000000000000, 0.000000000000000000, -1.000000000000000000 ) ) ;
#16206=CARTESIAN_POINT ( 'NONE',  ( -10.63581336909999919, 19.99999999999999645, -1.053405123100002783 ) ) ;
#16207=LINE ( 'NONE', #25822, #15243 ) ;
#16215=( LENGTH_UNIT ( ) NAMED_UNIT ( * ) SI_UNIT ( .MILLI., .METRE. ) );
#16218=ORIENTED_EDGE ( 'NONE', *, *, #26802, .F. ) ;
#16224=CARTESIAN_POINT ( 'NONE',  ( 12.69530690868993617, -23.62822639411161418, -1.399999999999998801 ) ) ;
#16250=ORIENTED_EDGE ( 'NONE', *, *, #12590, .T. ) ;
#16259=VECTOR ( 'NONE', #8855, 1000.000000000000000 ) ;
#16278=CIRCLE ( 'NONE', #1209, 3.999999999669999973 ) ;
#16279=ORIENTED_EDGE ( 'NONE', *, *, #6748, .F. ) ;
#16280=CARTESIAN_POINT ( 'NONE',  ( -9.999999999969999109, -29.12127062080000073, -30.52127062269999769 ) ) ;
#16282=VECTOR ( 'NONE', #6, 1000.000000000000000 ) ;
#16285=AXIS2_PLACEMENT_3D ( 'NONE', #1969, #16581, #9034 ) ;
#16286=AXIS2_PLACEMENT_3D ( 'NONE', #3435, #6109, #15248 ) ;
#16290=ORIENTED_EDGE ( 'NONE', *, *, #16783, .F. ) ;
#16291=CARTESIAN_POINT ( 'NONE',  ( -10.69999999930000101, -29.12132034360000077, -30.52132034359999935 ) ) ;
#16298=VECTOR ( 'NONE', #21706, 1000.000000000000000 ) ;
#16306=DIRECTION ( 'NONE',  ( 1.595945597898660305E-12, -0.7071067811865475727, 0.7071067811865475727 ) ) ;
#16313=EDGE_CURVE ( 'NONE', #28151, #20047, #19910, .T. ) ;
#16327=CARTESIAN_POINT ( 'NONE',  ( 14.00000000000000000, 21.70000000000000284, -62.80809897700000022 ) ) ;
#16330=ADVANCED_FACE ( 'NONE', ( #28075 ), #27761, .F. ) ;
#16359=CARTESIAN_POINT ( 'NONE',  ( -12.51132621223302799, 21.69999999994217177, -69.72125039903896493 ) ) ;
#16364=ORIENTED_EDGE ( 'NONE', *, *, #30476, .F. ) ;
#16368=ORIENTED_EDGE ( 'NONE', *, *, #13945, .F. ) ;
#16373=EDGE_CURVE ( 'NONE', #28074, #5070, #26651, .T. ) ;
#16381=DIRECTION ( 'NONE',  ( 0.000000000000000000, 1.000000000000000000, 0.000000000000000000 ) ) ;
#16384=ORIENTED_EDGE ( 'NONE', *, *, #26178, .T. ) ;
#16388=B_SPLINE_CURVE_WITH_KNOTS ( 'NONE', 3,
 ( #12248, #19499, #2966, #24070, #9734, #4869 ),
 .UNSPECIFIED., .F., .F.,
 ( 4, 2, 4 ),
 ( 0.000000000000000000, 0.5000000000000000000, 1.000000000000000000 ),
 .UNSPECIFIED. ) ;
#16389=EDGE_CURVE ( 'NONE', #15903, #25954, #24733, .T. ) ;
#16397=CARTESIAN_POINT ( 'NONE',  ( -12.69498943403903546, -23.62838044921069169, -1.399999999999998579 ) ) ;
#16407=CARTESIAN_POINT ( 'NONE',  ( 13.46591332798936236, 21.70000000000094786, -56.74462838232277306 ) ) ;
#16409=EDGE_LOOP ( 'NONE', ( #21567, #16058, #23998, #19117 ) ) ;
#16410=ORIENTED_EDGE ( 'NONE', *, *, #21521, .F. ) ;
#16441=CARTESIAN_POINT ( 'NONE',  ( 10.69999999989999928, -25.00000000000000000, -14.32712675259999813 ) ) ;
#16442=DIRECTION ( 'NONE',  ( 0.000000000000000000, -1.000000000000000000, 0.000000000000000000 ) ) ;
#16445=CARTESIAN_POINT ( 'NONE',  ( -11.69999999989999928, -2.500000000000002220, -2.399999999999999467 ) ) ;
#16453=ORIENTED_EDGE ( 'NONE', *, *, #5154, .F. ) ;
#16457=DIRECTION ( 'NONE',  ( 1.000000000000000000, 6.668066630619518976E-24, -2.257150022442225012E-12 ) ) ;
#16459=CARTESIAN_POINT ( 'NONE',  ( 10.00000000000000000, -130.0000000000000000, -41.82335799894999440 ) ) ;
#16460=DIRECTION ( 'NONE',  ( 0.000000000000000000, 0.000000000000000000, -1.000000000000000000 ) ) ;
#16464=LINE ( 'NONE', #18366, #25871 ) ;
#16477=CARTESIAN_POINT ( 'NONE',  ( -12.24455124192851407, 21.69999999999989626, -55.78348256257161353 ) ) ;
#16478=CARTESIAN_POINT ( 'NONE',  ( 10.69999999997499351, -26.21515828619547861, -31.32227941849448882 ) ) ;
#16490=LINE ( 'NONE', #6884, #8915 ) ;
#16497=ORIENTED_EDGE ( 'NONE', *, *, #14009, .F. ) ;
#16503=CARTESIAN_POINT ( 'NONE',  ( -10.00404318770000067, -25.00000000000000000, -2.271680403899995149 ) ) ;
#16506=DIRECTION ( 'NONE',  ( 0.000000000000000000, -1.000000000000000000, 2.257145581549999994E-12 ) ) ;
#16513=ADVANCED_FACE ( 'NONE', ( #4324 ), #13922, .F. ) ;
#16517=CARTESIAN_POINT ( 'NONE',  ( 10.79293894529999953, 19.99999999999999645, -1.960370163500001262 ) ) ;
#16525=VERTEX_POINT ( 'NONE', #8054 ) ;
#16535=PLANE ( 'NONE',  #28102 ) ;
#16536=FACE_OUTER_BOUND ( 'NONE', #12387, .T. ) ;
#16537=FACE_OUTER_BOUND ( 'NONE', #16945, .T. ) ;
#16546=EDGE_CURVE ( 'NONE', #22644, #9824, #14545, .T. ) ;
#16547=CARTESIAN_POINT ( 'NONE',  ( 18.06288090037109839, 10.34626908989090133, -1.400000000000002132 ) ) ;
#16549=CARTESIAN_POINT ( 'NONE',  ( -25.32382120361955913, -8.841433100612317020, -1.399999999999998579 ) ) ;
#16550=ORIENTED_EDGE ( 'NONE', *, *, #15585, .F. ) ;
#16558=ORIENTED_EDGE ( 'NONE', *, *, #12253, .T. ) ;
#16575=CARTESIAN_POINT ( 'NONE',  ( 11.57608395239999943, -24.17108566339999953, -0.7028182531999965788 ) ) ;
#16581=DIRECTION ( 'NONE',  ( 0.000000000000000000, -2.257145581549999994E-12, -1.000000000000000000 ) ) ;
#16586=CARTESIAN_POINT ( 'NONE',  ( 10.69999999997821583, -125.3091097352362056, -32.74879024719411547 ) ) ;
#16588=CARTESIAN_POINT ( 'NONE',  ( -10.69999999999999929, -24.00003454060000152, -28.41820959990000262 ) ) ;
#16594=CARTESIAN_POINT ( 'NONE',  ( 10.69999999999999929, -24.00000000000000000, -28.40000000000000213 ) ) ;
#16603=EDGE_CURVE ( 'NONE', #17295, #5944, #5086, .T. ) ;
#16617=DIRECTION ( 'NONE',  ( 0.000000000000000000, 0.000000000000000000, 1.000000000000000000 ) ) ;
#16625=AXIS2_PLACEMENT_3D ( 'NONE', #27455, #17397, #26846 ) ;
#16626=CARTESIAN_POINT ( 'NONE',  ( 9.000000000000000000, 21.70000000000000284, -51.10000000017000588 ) ) ;
#16630=CARTESIAN_POINT ( 'NONE',  ( 10.89131017139999891, -24.73114799960000099, -1.811764705899998606 ) ) ;
#16631=EDGE_LOOP ( 'NONE', ( #13026, #22949, #18017, #2663 ) ) ;
#16636=ORIENTED_EDGE ( 'NONE', *, *, #1150, .T. ) ;
#16659=LINE ( 'NONE', #5165, #11789 ) ;
#16697=ORIENTED_EDGE ( 'NONE', *, *, #17883, .F. ) ;
#16701=ORIENTED_EDGE ( 'NONE', *, *, #30200, .T. ) ;
#16706=ORIENTED_EDGE ( 'NONE', *, *, #8864, .T. ) ;
#16725=ORIENTED_EDGE ( 'NONE', *, *, #14494, .T. ) ;
#16729=DIRECTION ( 'NONE',  ( 1.553705081258627072E-12, -0.7253743710120287291, 0.6883545756940268046 ) ) ;
#16730=LINE ( 'NONE', #14550, #10688 ) ;
#16731=ADVANCED_FACE ( 'NONE', ( #6633 ), #28658, .T. ) ;
#16733=CARTESIAN_POINT ( 'NONE',  ( 10.69999999999999929, -120.5233595624000174, -31.26042064949999855 ) ) ;
#16739=CARTESIAN_POINT ( 'NONE',  ( 9.999999999945847762, -28.83786139299247608, -19.12343975076440827 ) ) ;
#16740=VECTOR ( 'NONE', #5853, 1000.000000000000000 ) ;
#16743=VECTOR ( 'NONE', #7149, 1000.000000000000114 ) ;
#16754=CYLINDRICAL_SURFACE ( 'NONE', #19947, 1.099999999999999201 ) ;
#16763=DIRECTION ( 'NONE',  ( 0.000000000000000000, -2.257145581549999994E-12, -1.000000000000000000 ) ) ;
#16768=DIRECTION ( 'NONE',  ( 1.000000000000000000, -0.000000000000000000, -2.257150022439999944E-12 ) ) ;
#16770=PLANE ( 'NONE',  #6104 ) ;
#16771=AXIS2_PLACEMENT_3D ( 'NONE', #25399, #23932, #28057 ) ;
#16783=EDGE_CURVE ( 'NONE', #29610, #28095, #14358, .T. ) ;
#16791=VECTOR ( 'NONE', #5826, 1000.000000000000000 ) ;
#16799=CARTESIAN_POINT ( 'NONE',  ( 16.20123158649999695, 11.52736809289999620, -1.399999999999998579 ) ) ;
#16805=FACE_OUTER_BOUND ( 'NONE', #7807, .T. ) ;
#16814=AXIS2_PLACEMENT_3D ( 'NONE', #7714, #19989, #8322 ) ;
#16821=CARTESIAN_POINT ( 'NONE',  ( -10.00000000000000000, 21.70000000000000284, -62.10000000000000142 ) ) ;
#16832=ORIENTED_EDGE ( 'NONE', *, *, #3445, .F. ) ;
#16842=DIRECTION ( 'NONE',  ( -1.595945597898660305E-12, 0.7071067811865475727, 0.7071067811865475727 ) ) ;
#16848=EDGE_CURVE ( 'NONE', #28074, #27949, #12591, .T. ) ;
#16857=CARTESIAN_POINT ( 'NONE',  ( 16.76556712906763735, 9.965626860143510513, -1.400000000000002132 ) ) ;
#16860=ORIENTED_EDGE ( 'NONE', *, *, #6098, .F. ) ;
#16862=CARTESIAN_POINT ( 'NONE',  ( 10.32522729140000095, -25.00000000000000000, -1.399999999999998579 ) ) ;
#16863=CARTESIAN_POINT ( 'NONE',  ( 10.69999999999910933, -23.99999999999999645, -28.00730091825414902 ) ) ;
#16876=DIRECTION ( 'NONE',  ( 2.257144471330000330E-12, -0.000000000000000000, -1.000000000000000000 ) ) ;
#16897=DIRECTION ( 'NONE',  ( 0.000000000000000000, 0.000000000000000000, -1.000000000000000000 ) ) ;
#16898=CARTESIAN_POINT ( 'NONE',  ( 9.000000000000000000, -55.00000000000001421, -42.39999999999999858 ) ) ;
#16906=CARTESIAN_POINT ( 'NONE',  ( -11.69999999989999928, 19.99999999999999645, -1.399999999999998579 ) ) ;
#16925=CARTESIAN_POINT ( 'NONE',  ( 1.110223024630000146E-16, 0.000000000000000000, -44.10000000000000142 ) ) ;
#16928=CARTESIAN_POINT ( 'NONE',  ( -9.999999999979998222, -27.00000000000000000, -31.39999999999999858 ) ) ;
#16930=EDGE_CURVE ( 'NONE', #30015, #20876, #187, .T. ) ;
#16932=DIRECTION ( 'NONE',  ( 0.000000000000000000, -1.000000000000000000, 2.257145581549999994E-12 ) ) ;
#16933=VECTOR ( 'NONE', #25083, 1000.000000000000000 ) ;
#16935=DIRECTION ( 'NONE',  ( -5.551115123049999208E-18, 0.000000000000000000, -1.000000000000000000 ) ) ;
#16940=CARTESIAN_POINT ( 'NONE',  ( -12.47331730070000155, 21.70000000000000284, -55.90289625529999995 ) ) ;
#16941=ADVANCED_FACE ( 'NONE', ( #15888 ), #8477, .F. ) ;
#16942=ORIENTED_EDGE ( 'NONE', *, *, #12325, .T. ) ;
#16945=EDGE_LOOP ( 'NONE', ( #29710, #19602, #4722, #29021 ) ) ;
#16948=LINE ( 'NONE', #2943, #28737 ) ;
#16949=EDGE_CURVE ( 'NONE', #4684, #17295, #14227, .T. ) ;
#16954=CARTESIAN_POINT ( 'NONE',  ( 9.572761946760001806, 19.99999999999999645, -43.22291707689799978 ) ) ;
#16956=VECTOR ( 'NONE', #30404, 1000.000000000000000 ) ;
#16962=CARTESIAN_POINT ( 'NONE',  ( -10.00000000070000183, -130.0000000000000000, -41.82335799894999440 ) ) ;
#16968=FACE_BOUND ( 'NONE', #4600, .T. ) ;
#16972=CARTESIAN_POINT ( 'NONE',  ( -10.69999999999999929, -120.6167089059000119, -31.26531288160000344 ) ) ;
#16989=ORIENTED_EDGE ( 'NONE', *, *, #28092, .F. ) ;
#16998=EDGE_CURVE ( 'NONE', #22920, #5024, #10862, .T. ) ;
#17007=CARTESIAN_POINT ( 'NONE',  ( 8.999999999770000869, 20.99999999999999645, -45.10000000000000142 ) ) ;
#17014=FACE_OUTER_BOUND ( 'NONE', #17297, .T. ) ;
#17016=CARTESIAN_POINT ( 'NONE',  ( 10.99999999979999998, 21.34999999950001026, -70.09999999999999432 ) ) ;
#17022=ORIENTED_EDGE ( 'NONE', *, *, #19640, .F. ) ;
#17026=ORIENTED_EDGE ( 'NONE', *, *, #28444, .F. ) ;
#17035=B_SPLINE_CURVE_WITH_KNOTS ( 'NONE', 3,
 ( #23864, #29458, #14576, #24593, #28724, #31093 ),
 .UNSPECIFIED., .F., .F.,
 ( 4, 2, 4 ),
 ( 0.000000000000000000, 0.5000000000000000000, 1.000000000000000000 ),
 .UNSPECIFIED. ) ;
#17036=DIRECTION ( 'NONE',  ( 0.000000000000000000, 0.000000000000000000, 1.000000000000000000 ) ) ;
#17055=ORIENTED_EDGE ( 'NONE', *, *, #7133, .F. ) ;
#17058=CARTESIAN_POINT ( 'NONE',  ( 9.999999999933628203, -25.95491900963585152, -13.51082902187790857 ) ) ;
#17059=ORIENTED_EDGE ( 'NONE', *, *, #7016, .F. ) ;
#17061=CARTESIAN_POINT ( 'NONE',  ( 17.16657240410000185, -9.000000001100003644, -0.6999999999999992895 ) ) ;
#17063=ORIENTED_EDGE ( 'NONE', *, *, #26599, .F. ) ;
#17064=CARTESIAN_POINT ( 'NONE',  ( -11.43935997342166822, 19.99999999999998934, -1.425491584528367772 ) ) ;
#17074=CARTESIAN_POINT ( 'NONE',  ( -15.81846178510917156, 11.44785871239032105, -1.400000000000001910 ) ) ;
#17093=CARTESIAN_POINT ( 'NONE',  ( 13.99999999979999821, 20.99999999999999645, -58.51619795559999915 ) ) ;
#17094=FACE_OUTER_BOUND ( 'NONE', #20130, .T. ) ;
#17102=VERTEX_POINT ( 'NONE', #31106 ) ;
#17104=VERTEX_POINT ( 'NONE', #27995 ) ;
#17105=VERTEX_POINT ( 'NONE', #16928 ) ;
#17109=EDGE_CURVE ( 'NONE', #26791, #17104, #274, .T. ) ;
#17117=EDGE_CURVE ( 'NONE', #145, #9481, #7032, .T. ) ;
#17136=ADVANCED_FACE ( 'NONE', ( #6440 ), #30953, .F. ) ;
#17150=EDGE_LOOP ( 'NONE', ( #26314, #13064, #23587, #16497 ) ) ;
#17155=DIRECTION ( 'NONE',  ( -1.000000000000000000, 0.000000000000000000, 0.000000000000000000 ) ) ;
#17161=B_SPLINE_CURVE_WITH_KNOTS ( 'NONE', 3,
 ( #6953, #16547, #26155, #14197, #14362, #23960, #42, #7268, #16857, #2547, #14971, #19540, #12441, #19690, #26614, #17163, #12752, #12134 ),
 .UNSPECIFIED., .F., .F.,
 ( 4, 2, 2, 2, 2, 2, 2, 2, 4 ),
 ( 0.000000000000000000, 0.1250000000000000000, 0.2500000000000000000, 0.3750000000000000000, 0.5000000000000000000, 0.6250000000000000000, 0.7500000000000000000, 0.8750000000000000000, 1.000000000000000000 ),
 .UNSPECIFIED. ) ;
#17162=B_SPLINE_CURVE_WITH_KNOTS ( 'NONE', 3,
 ( #1932, #28197, #18283, #25853, #21276, #4292, #13887, #15931, #11525, #25539 ),
 .UNSPECIFIED., .F., .F.,
 ( 4, 2, 2, 2, 4 ),
 ( 0.000000000000000000, 0.2500000000000000000, 0.5000000000000000000, 0.7500000000000000000, 1.000000000000000000 ),
 .UNSPECIFIED. ) ;
#17163=CARTESIAN_POINT ( 'NONE',  ( 16.08831934135733022, 11.26096619629935702, -1.400000000000001910 ) ) ;
#17166=EDGE_CURVE ( 'NONE', #23803, #15341, #11207, .T. ) ;
#17171=CARTESIAN_POINT ( 'NONE',  ( 13.99999999979999821, 20.99999999999999645, -67.09999999999999432 ) ) ;
#17174=CARTESIAN_POINT ( 'NONE',  ( -11.69999999989999928, 19.99999999999999645, -0.6999999999999992895 ) ) ;
#17188=CARTESIAN_POINT ( 'NONE',  ( 10.69999999993478568, -25.95326775694153199, -13.50807451238996570 ) ) ;
#17189=ORIENTED_EDGE ( 'NONE', *, *, #13852, .F. ) ;
#17213=CYLINDRICAL_SURFACE ( 'NONE', #7439, 3.000000000000003997 ) ;
#17214=CARTESIAN_POINT ( 'NONE',  ( -9.500000000000000000, 21.70000000000000284, -60.10000000019999788 ) ) ;
#17220=DIRECTION ( 'NONE',  ( -1.000000000000000000, 0.000000000000000000, 0.000000000000000000 ) ) ;
#17224=PLANE ( 'NONE',  #19776 ) ;
#17227=DIRECTION ( 'NONE',  ( 1.000000000000000000, 0.000000000000000000, 0.000000000000000000 ) ) ;
#17230=DIRECTION ( 'NONE',  ( -0.8923935798119907448, -1.018860921557044162E-12, -0.4512579070889951582 ) ) ;
#17236=CARTESIAN_POINT ( 'NONE',  ( -11.69999999989999928, -2.500000000000002220, -2.399999999999999467 ) ) ;
#17242=FACE_OUTER_BOUND ( 'NONE', #27126, .T. ) ;
#17252=LINE ( 'NONE', #5306, #7134 ) ;
#17259=DIRECTION ( 'NONE',  ( -1.000000000000000000, -2.587524353642439916E-24, -2.257144471329210308E-12 ) ) ;
#17260=ADVANCED_FACE ( 'NONE', ( #3228 ), #20075, .F. ) ;
#17263=CARTESIAN_POINT ( 'NONE',  ( 16.99504414847917744, 12.09604337533561669, -1.400000000000001910 ) ) ;
#17267=ORIENTED_EDGE ( 'NONE', *, *, #2366, .F. ) ;
#17282=ADVANCED_FACE ( 'NONE', ( #13446 ), #20532, .F. ) ;
#17287=AXIS2_PLACEMENT_3D ( 'NONE', #9070, #1845, #7178 ) ;
#17289=B_SPLINE_CURVE_WITH_KNOTS ( 'NONE', 5,
 ( #23919, #2199, #28464, #19179, #6900, #16503, #9582, #6257, #7063 ),
 .UNSPECIFIED., .F., .F.,
 ( 6, 3, 6 ),
 ( 0.000000000000000000, 1.211913930199999934, 1.514808573670000102 ),
 .UNSPECIFIED. ) ;
#17291=CARTESIAN_POINT ( 'NONE',  ( -9.999999999969999109, -43.95328087550000618, -27.24755286569999768 ) ) ;
#17295=VERTEX_POINT ( 'NONE', #10938 ) ;
#17297=EDGE_LOOP ( 'NONE', ( #12885, #10067, #30963, #6671 ) ) ;
#17307=CARTESIAN_POINT ( 'NONE',  ( -10.69999999996291251, -37.77860098318037529, -25.96937563633603574 ) ) ;
#17308=AXIS2_PLACEMENT_3D ( 'NONE', #21515, #21674, #19308 ) ;
#17310=VECTOR ( 'NONE', #22052, 1000.000000000000000 ) ;
#17320=CARTESIAN_POINT ( 'NONE',  ( -1.598721155459999804E-14, 0.000000000000000000, -0.6999999999999992895 ) ) ;
#17327=FACE_OUTER_BOUND ( 'NONE', #20400, .T. ) ;
#17330=EDGE_CURVE ( 'NONE', #25188, #4001, #16730, .T. ) ;
#17344=DIRECTION ( 'NONE',  ( 2.965499939100700266E-25, -1.000000000000000000, 2.257145581549900232E-12 ) ) ;
#17349=CARTESIAN_POINT ( 'NONE',  ( 11.39269908143662491, 20.99999999989801225, -70.09999999997381792 ) ) ;
#17354=CARTESIAN_POINT ( 'NONE',  ( 9.500000000000000000, 20.99999999999999645, -64.10000000019999788 ) ) ;
#17357=CARTESIAN_POINT ( 'NONE',  ( -10.69999999999999929, -25.07023973440000120, -30.70263567090000123 ) ) ;
#17368=VERTEX_POINT ( 'NONE', #2434 ) ;
#17386=DIRECTION ( 'NONE',  ( -1.000000000000000000, 0.000000000000000000, 0.000000000000000000 ) ) ;
#17390=CARTESIAN_POINT ( 'NONE',  ( -8.999999999559999964, 21.70000000000000284, -64.10000000000000853 ) ) ;
#17397=DIRECTION ( 'NONE',  ( 0.000000000000000000, 1.000000000000000000, 0.000000000000000000 ) ) ;
#17401=CARTESIAN_POINT ( 'NONE',  ( -8.999999999699999975, 21.69999999929999390, -51.10000000000999876 ) ) ;
#17406=ORIENTED_EDGE ( 'NONE', *, *, #21512, .T. ) ;
#17414=B_SPLINE_CURVE_WITH_KNOTS ( 'NONE', 3,
 ( #7704, #17609, #7855, #19979, #17307, #181, #7558, #14957, #2994, #24703 ),
 .UNSPECIFIED., .F., .F.,
 ( 4, 2, 2, 2, 4 ),
 ( 0.000000000000000000, 0.2500000000000000000, 0.5000000000000000000, 0.7500000000000000000, 1.000000000000000000 ),
 .UNSPECIFIED. ) ;
#17424=AXIS2_PLACEMENT_3D ( 'NONE', #31051, #28992, #19561 ) ;
#17429=CARTESIAN_POINT ( 'NONE',  ( 9.999999999966100006, -30.00000000000020606, -28.79269908146310186 ) ) ;
#17432=CARTESIAN_POINT ( 'NONE',  ( -10.69999999999999929, -124.6960077043000013, -32.36679061319999562 ) ) ;
#17434=CARTESIAN_POINT ( 'NONE',  ( 10.69999999999999929, -130.0000000000000000, -42.39999999999999858 ) ) ;
#17445=ORIENTED_EDGE ( 'NONE', *, *, #26724, .T. ) ;
#17454=PLANE ( 'NONE',  #10944 ) ;
#17457=DIRECTION ( 'NONE',  ( 0.000000000000000000, 2.257145581549999994E-12, 1.000000000000000000 ) ) ;
#17459=B_SPLINE_CURVE_WITH_KNOTS ( 'NONE', 3,
 ( #15457, #17507, #17651, #22553 ),
 .UNSPECIFIED., .F., .F.,
 ( 4, 4 ),
 ( 0.000000000000000000, 1.000000000000000000 ),
 .UNSPECIFIED. ) ;
#17463=EDGE_CURVE ( 'NONE', #26986, #26129, #14860, .T. ) ;
#17470=VECTOR ( 'NONE', #11267, 1000.000000000000000 ) ;
#17471=CYLINDRICAL_SURFACE ( 'NONE', #26287, 26.80000000000000071 ) ;
#17474=CIRCLE ( 'NONE', #913, 1.700000000000000178 ) ;
#17477=CARTESIAN_POINT ( 'NONE',  ( 13.92191802967587577, 20.99999999989822186, -67.88524365365343272 ) ) ;
#17491=CARTESIAN_POINT ( 'NONE',  ( -10.69999999999999929, -24.97510340920000260, -26.18620021100000272 ) ) ;
#17499=EDGE_CURVE ( 'NONE', #19704, #30881, #29008, .T. ) ;
#17506=CYLINDRICAL_SURFACE ( 'NONE', #18240, 3.000000000000002220 ) ;
#17507=CARTESIAN_POINT ( 'NONE',  ( -12.24453640261407905, 20.99999999997362821, -55.78347656086990725 ) ) ;
#17508=EDGE_CURVE ( 'NONE', #30054, #22831, #4164, .T. ) ;
#17512=ORIENTED_EDGE ( 'NONE', *, *, #29311, .F. ) ;
#17518=ADVANCED_FACE ( 'NONE', ( #26805 ), #14701, .F. ) ;
#17520=ORIENTED_EDGE ( 'NONE', *, *, #4072, .F. ) ;
#17524=DIRECTION ( 'NONE',  ( 2.257150022439999944E-12, 0.000000000000000000, 1.000000000000000000 ) ) ;
#17527=EDGE_CURVE ( 'NONE', #27200, #6537, #5514, .T. ) ;
#17541=CARTESIAN_POINT ( 'NONE',  ( 9.999999999962829733, -25.28360478509039311, -25.93233155165111370 ) ) ;
#17553=AXIS2_PLACEMENT_3D ( 'NONE', #30315, #16143, #30636 ) ;
#17556=CARTESIAN_POINT ( 'NONE',  ( 9.999999999977427834, -126.3827248121017419, -33.44530783663593354 ) ) ;
#17558=CARTESIAN_POINT ( 'NONE',  ( -10.92933975387415302, -24.70409753101286654, -1.761594195916170946 ) ) ;
#17570=CARTESIAN_POINT ( 'NONE',  ( 18.20094554413687504, 10.59899472509098040, -1.400000000000001910 ) ) ;
#17579=CARTESIAN_POINT ( 'NONE',  ( 8.999999999770000869, 21.35000000010000321, -45.09999999954499827 ) ) ;
#17588=VERTEX_POINT ( 'NONE', #18280 ) ;
#17595=EDGE_LOOP ( 'NONE', ( #22226, #16832, #16279, #11804 ) ) ;
#17608=DIRECTION ( 'NONE',  ( -0.000000000000000000, 1.000000000000000000, -2.255973188440000244E-12 ) ) ;
#17609=CARTESIAN_POINT ( 'NONE',  ( -10.69999999996564632, -42.68530818349433531, -27.18110123272096601 ) ) ;
#17614=DIRECTION ( 'NONE',  ( 0.000000000000000000, -1.000000000000000000, 0.000000000000000000 ) ) ;
#17620=CARTESIAN_POINT ( 'NONE',  ( 16.20123158649999695, -8.472631907100000248, -0.6999999999999992895 ) ) ;
#17628=EDGE_LOOP ( 'NONE', ( #23228, #26501 ) ) ;
#17630=ORIENTED_EDGE ( 'NONE', *, *, #7365, .T. ) ;
#17643=EDGE_CURVE ( 'NONE', #12999, #19402, #3648, .T. ) ;
#17651=CARTESIAN_POINT ( 'NONE',  ( -12.36063638108074692, 20.99999999997349676, -55.83941130196991054 ) ) ;
#17666=AXIS2_PLACEMENT_3D ( 'NONE', #19343, #14622, #28932 ) ;
#17671=CARTESIAN_POINT ( 'NONE',  ( -10.69999999999999929, -29.06671945329999929, -26.22544931050000017 ) ) ;
#17674=ORIENTED_EDGE ( 'NONE', *, *, #19640, .T. ) ;
#17678=VECTOR ( 'NONE', #24562, 1000.000000000000000 ) ;
#17700=LINE ( 'NONE', #6384, #4157 ) ;
#17703=AXIS2_PLACEMENT_3D ( 'NONE', #15970, #17997, #23216 ) ;
#17716=ORIENTED_EDGE ( 'NONE', *, *, #15827, .F. ) ;
#17722=AXIS2_PLACEMENT_3D ( 'NONE', #2627, #14015, #29203 ) ;
#17734=VERTEX_POINT ( 'NONE', #23800 ) ;
#17740=AXIS2_PLACEMENT_3D ( 'NONE', #29898, #8169, #3455 ) ;
#17761=CARTESIAN_POINT ( 'NONE',  ( -13.67718144140000014, 21.70000000000000284, -57.16242377749999548 ) ) ;
#17773=ORIENTED_EDGE ( 'NONE', *, *, #28126, .F. ) ;
#17775=CARTESIAN_POINT ( 'NONE',  ( 10.24010329470000080, 19.99999999999999645, -1.477379946600000604 ) ) ;
#17787=EDGE_CURVE ( 'NONE', #2571, #17102, #17161, .T. ) ;
#17800=LINE ( 'NONE', #8052, #15848 ) ;
#17808=CARTESIAN_POINT ( 'NONE',  ( -9.999999999909999104, 19.99999999999999645, -2.399999999999999467 ) ) ;
#17831=LINE ( 'NONE', #1166, #16933 ) ;
#17833=CARTESIAN_POINT ( 'NONE',  ( -10.00000000000000000, -130.0000000000000000, -42.39999999999999858 ) ) ;
#17834=CARTESIAN_POINT ( 'NONE',  ( -10.00000000070000183, -82.23832021890000021, -29.25398675769999812 ) ) ;
#17835=ORIENTED_EDGE ( 'NONE', *, *, #10504, .F. ) ;
#17854=CARTESIAN_POINT ( 'NONE',  ( -9.631980347289379907, 21.69999999997851603, -53.61980015864676119 ) ) ;
#17857=CARTESIAN_POINT ( 'NONE',  ( -26.85555875125346859, -1.316834860305418076, -0.6999999999999992895 ) ) ;
#17859=ORIENTED_EDGE ( 'NONE', *, *, #4208, .F. ) ;
#17860=ADVANCED_FACE ( 'NONE', ( #17014 ), #17471, .T. ) ;
#17864=VERTEX_POINT ( 'NONE', #26929 ) ;
#17865=DIRECTION ( 'NONE',  ( 1.000000000000000000, 0.000000000000000000, 0.000000000000000000 ) ) ;
#17866=DIRECTION ( 'NONE',  ( -1.000000000000000000, 0.000000000000000000, 0.000000000000000000 ) ) ;
#17867=DIRECTION ( 'NONE',  ( 1.553791817432425509E-12, 0.7253743710120286181, -0.6883545756940269156 ) ) ;
#17876=EDGE_CURVE ( 'NONE', #28481, #24422, #12596, .T. ) ;
#17883=EDGE_CURVE ( 'NONE', #26472, #11411, #2898, .T. ) ;
#17884=CARTESIAN_POINT ( 'NONE',  ( 10.88909890409999903, 20.99999999999999645, -56.10000000020000499 ) ) ;
#17899=EDGE_LOOP ( 'NONE', ( #9795, #25897, #10222, #2029, #14484, #15, #25443, #14019, #31114, #16989, #19292, #11500, #7886, #10564, #1238, #28326, #247 ) ) ;
#17900=VERTEX_POINT ( 'NONE', #14666 ) ;
#17904=CARTESIAN_POINT ( 'NONE',  ( -10.69999999999999929, -27.00000000000000000, -28.40000000000000213 ) ) ;
#17905=CARTESIAN_POINT ( 'NONE',  ( 9.000000000029999114, 20.99999999999999645, -45.10000000000000142 ) ) ;
#17906=DIRECTION ( 'NONE',  ( 0.7071067811865476838, -1.595945597898661315E-12, -0.7071067811865473507 ) ) ;
#17909=CARTESIAN_POINT ( 'NONE',  ( 10.69999999997517115, -27.39379052061039843, -31.39999999999999858 ) ) ;
#17921=ORIENTED_EDGE ( 'NONE', *, *, #17330, .F. ) ;
#17923=CARTESIAN_POINT ( 'NONE',  ( 10.00000000020000002, 19.99999999999999645, -2.208382156699995047 ) ) ;
#17924=ORIENTED_EDGE ( 'NONE', *, *, #5994, .F. ) ;
#17931=ORIENTED_EDGE ( 'NONE', *, *, #18352, .T. ) ;
#17954=CARTESIAN_POINT ( 'NONE',  ( -1.243449787579999883E-14, 0.000000000000000000, -0.6999999999999992895 ) ) ;
#17959=ORIENTED_EDGE ( 'NONE', *, *, #11422, .T. ) ;
#17969=ORIENTED_EDGE ( 'NONE', *, *, #29110, .F. ) ;
#17970=ORIENTED_EDGE ( 'NONE', *, *, #18429, .T. ) ;
#17971=ORIENTED_EDGE ( 'NONE', *, *, #8527, .F. ) ;
#17972=AXIS2_PLACEMENT_3D ( 'NONE', #14840, #14526, #7125 ) ;
#17983=CARTESIAN_POINT ( 'NONE',  ( 9.150827312880000619, 19.99999999999999645, -44.09999999970998630 ) ) ;
#17997=DIRECTION ( 'NONE',  ( -1.000000000000000000, 0.000000000000000000, -0.000000000000000000 ) ) ;
#17998=VECTOR ( 'NONE', #2500, 1000.000000000000000 ) ;
#18009=CARTESIAN_POINT ( 'NONE',  ( -10.00045772538970290, 21.69999999997727613, -54.17149754567696363 ) ) ;
#18013=CARTESIAN_POINT ( 'NONE',  ( -10.89131017139999891, -24.73114799890000270, -1.811764705899998606 ) ) ;
#18016=CARTESIAN_POINT ( 'NONE',  ( -8.999999999710000864, 19.99999999959999641, -43.74999999991700150 ) ) ;
#18017=ORIENTED_EDGE ( 'NONE', *, *, #26073, .T. ) ;
#18021=CARTESIAN_POINT ( 'NONE',  ( -10.70170550458792569, 21.69999999997569162, -54.87247492467220411 ) ) ;
#18022=DIRECTION ( 'NONE',  ( -5.551115123049999208E-18, 0.000000000000000000, -1.000000000000000000 ) ) ;
#18025=CARTESIAN_POINT ( 'NONE',  ( 18.24482546714449072, 10.73903380414593478, -1.400000000000001910 ) ) ;
#18031=CARTESIAN_POINT ( 'NONE',  ( 9.999999999959999997, -29.30501631460000311, -26.47986984960000001 ) ) ;
#18040=EDGE_CURVE ( 'NONE', #9370, #26977, #9586, .T. ) ;
#18042=CARTESIAN_POINT ( 'NONE',  ( -17.79876841479999783, 11.52736809289999620, -1.399999999999998579 ) ) ;
#18046=LINE ( 'NONE', #6094, #4714 ) ;
#18047=ORIENTED_EDGE ( 'NONE', *, *, #5761, .T. ) ;
#18056=ORIENTED_EDGE ( 'NONE', *, *, #939, .T. ) ;
#18064=LINE ( 'NONE', #11319, #21639 ) ;
#18067=CARTESIAN_POINT ( 'NONE',  ( 10.69999999997431850, -28.51132621201893258, -31.02125039897099512 ) ) ;
#18068=PLANE ( 'NONE',  #26556 ) ;
#18084=CARTESIAN_POINT ( 'NONE',  ( 10.69999999999999929, -55.00000000000000000, -42.39999999999999858 ) ) ;
#18089=CARTESIAN_POINT ( 'NONE',  ( 9.999999999963435471, -41.43235263099278143, -26.99482620601180471 ) ) ;
#18106=CARTESIAN_POINT ( 'NONE',  ( -10.69999999997181028, -29.62125039897762591, -29.91132621204121733 ) ) ;
#18114=CARTESIAN_POINT ( 'NONE',  ( -10.00166578765888836, 21.00000000000104095, -54.17273359979817826 ) ) ;
#18118=CARTESIAN_POINT ( 'NONE',  ( 10.69999999996051621, -35.47440968381866355, -24.90685721729063928 ) ) ;
#18119=ADVANCED_FACE ( 'NONE', ( #28470 ), #18873, .T. ) ;
#18136=VERTEX_POINT ( 'NONE', #5474 ) ;
#18138=B_SPLINE_CURVE_WITH_KNOTS ( 'NONE', 3,
 ( #4824, #2461, #12053, #15642 ),
 .UNSPECIFIED., .F., .F.,
 ( 4, 4 ),
 ( 0.000000000000000000, 1.000000000000000000 ),
 .UNSPECIFIED. ) ;
#18142=CARTESIAN_POINT ( 'NONE',  ( -12.12499970530000049, 20.99999999999999645, -55.73512393530000253 ) ) ;
#18165=EDGE_CURVE ( 'NONE', #15209, #30015, #16388, .T. ) ;
#18174=CARTESIAN_POINT ( 'NONE',  ( -9.000000000229999131, 20.99999999999999645, -51.10000000000000142 ) ) ;
#18175=CARTESIAN_POINT ( 'NONE',  ( -26.57440914490000239, -3.469982507400000582, -0.6999999999999992895 ) ) ;
#18182=EDGE_LOOP ( 'NONE', ( #2790, #12075, #6873, #15283 ) ) ;
#18184=VECTOR ( 'NONE', #25171, 1000.000000000000000 ) ;
#18193=DIRECTION ( 'NONE',  ( 0.000000000000000000, 2.257157423930000049E-12, 1.000000000000000000 ) ) ;
#18195=DIRECTION ( 'NONE',  ( 0.000000000000000000, 0.000000000000000000, 1.000000000000000000 ) ) ;
#18203=CARTESIAN_POINT ( 'NONE',  ( -9.000000000229999131, 21.70000000000000284, -53.60000000000000142 ) ) ;
#18206=CARTESIAN_POINT ( 'NONE',  ( -14.00000000000000000, 20.99999999996851940, -58.04568740119480452 ) ) ;
#18210=EDGE_CURVE ( 'NONE', #669, #3831, #22415, .T. ) ;
#18214=ORIENTED_EDGE ( 'NONE', *, *, #5615, .F. ) ;
#18217=ADVANCED_FACE ( 'NONE', ( #14773 ), #24375, .T. ) ;
#18222=CARTESIAN_POINT ( 'NONE',  ( -1.243449787579999883E-14, 0.000000000000000000, -0.6999999999999992895 ) ) ;
#18225=FACE_OUTER_BOUND ( 'NONE', #29166, .T. ) ;
#18240=AXIS2_PLACEMENT_3D ( 'NONE', #2580, #22089, #15002 ) ;
#18242=CARTESIAN_POINT ( 'NONE',  ( 10.08101130880000085, 19.99999999999999645, -1.830192468500003944 ) ) ;
#18246=DIRECTION ( 'NONE',  ( -1.000000000000000000, 0.000000000000000000, 0.000000000000000000 ) ) ;
#18251=ORIENTED_EDGE ( 'NONE', *, *, #6748, .T. ) ;
#18253=B_SPLINE_CURVE_WITH_KNOTS ( 'NONE', 3,
 ( #12965, #1019, #25241, #17671 ),
 .UNSPECIFIED., .F., .F.,
 ( 4, 4 ),
 ( 0.000000000000000000, 1.000000000000000000 ),
 .UNSPECIFIED. ) ;
#18260=CARTESIAN_POINT ( 'NONE',  ( -10.89131017139999891, -24.73114799890000270, -1.811764705899998606 ) ) ;
#18273=CARTESIAN_POINT ( 'NONE',  ( -8.999999999722247068, 21.00000000000650147, -51.75449846961598865 ) ) ;
#18279=EDGE_CURVE ( 'NONE', #49, #27161, #1229, .T. ) ;
#18280=CARTESIAN_POINT ( 'NONE',  ( -9.999999999969999109, -24.87872937729999734, -30.52127062079999931 ) ) ;
#18283=CARTESIAN_POINT ( 'NONE',  ( -10.00000000005918288, -28.83786139291737882, -19.12343975056708700 ) ) ;
#18306=ADVANCED_FACE ( 'NONE', ( #10830 ), #29548, .F. ) ;
#18321=ORIENTED_EDGE ( 'NONE', *, *, #25582, .T. ) ;
#18324=CARTESIAN_POINT ( 'NONE',  ( -8.999999999883337765, 20.26179938780245138, -44.10000000000000142 ) ) ;
#18330=CARTESIAN_POINT ( 'NONE',  ( -11.02757632650000019, -24.42656469639999983, -0.8308237180999975546 ) ) ;
#18352=EDGE_CURVE ( 'NONE', #16525, #26528, #29531, .T. ) ;
#18359=CARTESIAN_POINT ( 'NONE',  ( -10.69999999999999929, -24.69736308950000137, -26.47023749829999772 ) ) ;
#18366=CARTESIAN_POINT ( 'NONE',  ( 9.707106781189999367, -55.00000000000000000, -43.10710678118599759 ) ) ;
#18376=DIRECTION ( 'NONE',  ( 0.000000000000000000, -1.000000000000000000, 2.257145581549999994E-12 ) ) ;
#18382=ORIENTED_EDGE ( 'NONE', *, *, #19309, .T. ) ;
#18389=CARTESIAN_POINT ( 'NONE',  ( 0.000000000000000000, -55.00000000000000000, -44.10000000000000142 ) ) ;
#18407=B_SPLINE_CURVE_WITH_KNOTS ( 'NONE', 3,
 ( #20683, #15486, #25566, #4002, #20366, #2275, #23983, #23831, #25725, #21150 ),
 .UNSPECIFIED., .F., .F.,
 ( 4, 2, 2, 2, 4 ),
 ( 0.000000000000000000, 0.2499999999999999445, 0.4999999999999998890, 0.7499999999999997780, 1.000000000000000000 ),
 .UNSPECIFIED. ) ;
#18408=ADVANCED_FACE ( 'NONE', ( #2911 ), #17224, .F. ) ;
#18418=( LENGTH_UNIT ( ) NAMED_UNIT ( * ) SI_UNIT ( .MILLI., .METRE. ) );
#18421=EDGE_LOOP ( 'NONE', ( #13741, #12764, #6963, #12609, #294 ) ) ;
#18429=EDGE_CURVE ( 'NONE', #20670, #7630, #22115, .T. ) ;
#18431=VERTEX_POINT ( 'NONE', #15032 ) ;
#18435=DIRECTION ( 'NONE',  ( 1.000000000000000000, -0.000000000000000000, -2.257150022439999944E-12 ) ) ;
#18436=CARTESIAN_POINT ( 'NONE',  ( -10.49791847189999849, -25.00000000000000000, -3.602081527999998034 ) ) ;
#18439=DIRECTION ( 'NONE',  ( 0.000000000000000000, 0.000000000000000000, -1.000000000000000000 ) ) ;
#18443=CARTESIAN_POINT ( 'NONE',  ( -11.69999999989999928, -24.11120071630000083, -1.399999999999998579 ) ) ;
#18452=EDGE_LOOP ( 'NONE', ( #20620, #17931, #13361, #27571 ) ) ;
#18471=CARTESIAN_POINT ( 'NONE',  ( 11.63809019220000174, -24.14124255329999968, -0.6999999999999992895 ) ) ;
#18472=EDGE_CURVE ( 'NONE', #26129, #27980, #15175, .T. ) ;
#18477=CARTESIAN_POINT ( 'NONE',  ( 21.51557202503504129, 16.01570388398135236, -1.399999999999998579 ) ) ;
#18481=CARTESIAN_POINT ( 'NONE',  ( -9.000000000000000000, -130.0000000000000000, -44.10000000000000142 ) ) ;
#18485=CARTESIAN_POINT ( 'NONE',  ( -10.89131017139999891, -24.73114799960000099, -1.811764705899998606 ) ) ;
#18493=EDGE_CURVE ( 'NONE', #18717, #25785, #22047, .T. ) ;
#18502=LINE ( 'NONE', #18966, #30517 ) ;
#18512=CARTESIAN_POINT ( 'NONE',  ( 10.49791847189999849, -25.00000000000000000, -3.602081527999998034 ) ) ;
#18520=ADVANCED_FACE ( 'NONE', ( #5189 ), #27063, .F. ) ;
#18522=CARTESIAN_POINT ( 'NONE',  ( -17.84839340654884055, 10.55214128775187810, -1.400000000000001910 ) ) ;
#18524=CIRCLE ( 'NONE', #23052, 1.099999999570000497 ) ;
#18530=ORIENTED_EDGE ( 'NONE', *, *, #3269, .F. ) ;
#18535=ORIENTED_EDGE ( 'NONE', *, *, #15121, .F. ) ;
#18550=EDGE_LOOP ( 'NONE', ( #6399, #5341, #6734, #2220 ) ) ;
#18562=DIRECTION ( 'NONE',  ( 0.000000000000000000, 0.000000000000000000, -1.000000000000000000 ) ) ;
#18568=DIRECTION ( 'NONE',  ( 1.000000000000000000, 0.000000000000000000, 0.000000000000000000 ) ) ;
#18570=EDGE_LOOP ( 'NONE', ( #14295, #11069, #14176, #22951 ) ) ;
#18575=( NAMED_UNIT ( * ) SI_UNIT ( $, .STERADIAN. ) SOLID_ANGLE_UNIT ( ) );
#18576=VERTEX_POINT ( 'NONE', #14803 ) ;
#18579=LINE ( 'NONE', #9444, #22605 ) ;
#18580=DIRECTION ( 'NONE',  ( -2.257102469710000208E-12, 0.000000000000000000, 1.000000000000000000 ) ) ;
#18582=B_SPLINE_CURVE_WITH_KNOTS ( 'NONE', 3,
 ( #13867, #21257, #23474, #23160, #14026, #27868 ),
 .UNSPECIFIED., .F., .F.,
 ( 4, 2, 4 ),
 ( 0.000000000000000000, 0.5000000000000000000, 1.000000000000000000 ),
 .UNSPECIFIED. ) ;
#18594=PLANE ( 'NONE',  #29862 ) ;
#18596=LINE ( 'NONE', #2082, #14322 ) ;
#18597=B_SPLINE_CURVE_WITH_KNOTS ( 'NONE', 3,
 ( #28754, #9719, #7362, #19167 ),
 .UNSPECIFIED., .F., .F.,
 ( 4, 4 ),
 ( 0.000000000000000000, 1.000000000000000000 ),
 .UNSPECIFIED. ) ;
#18600=CARTESIAN_POINT ( 'NONE',  ( -1.598721155459999804E-14, 0.000000000000000000, -0.6999999999999992895 ) ) ;
#18608=VERTEX_POINT ( 'NONE', #24864 ) ;
#18609=CARTESIAN_POINT ( 'NONE',  ( -9.000000000000000000, -54.99999999999998579, -42.39999999999999858 ) ) ;
#18621=CARTESIAN_POINT ( 'NONE',  ( -9.999999999969999109, -24.00000000000000000, -28.40000000000000213 ) ) ;
#18628=DIRECTION ( 'NONE',  ( 1.000000000000000000, 0.000000000000000000, 0.000000000000000000 ) ) ;
#18630=EDGE_LOOP ( 'NONE', ( #6991, #14901, #13422, #8616 ) ) ;
#18635=CARTESIAN_POINT ( 'NONE',  ( 11.09640327169999807, -24.58282405819999994, -1.600739409500000265 ) ) ;
#18652=B_SPLINE_CURVE_WITH_KNOTS ( 'NONE', 5,
 ( #23127, #26411, #11924, #4691, #23908, #16954, #9403, #26561, #14610 ),
 .UNSPECIFIED., .F., .F.,
 ( 6, 3, 6 ),
 ( 0.000000000000000000, 0.6978155539409999220, 1.118801870760000039 ),
 .UNSPECIFIED. ) ;
#18655=DIRECTION ( 'NONE',  ( -5.551115123049999208E-18, 0.000000000000000000, -1.000000000000000000 ) ) ;
#18660=FACE_OUTER_BOUND ( 'NONE', #4873, .T. ) ;
#18665=FACE_OUTER_BOUND ( 'NONE', #10302, .T. ) ;
#18668=CIRCLE ( 'NONE', #27206, 1.000000000000000888 ) ;
#18672=CARTESIAN_POINT ( 'NONE',  ( 12.55799324160000019, 21.70000000000000284, -55.95247857500000066 ) ) ;
#18676=PLANE ( 'NONE',  #7257 ) ;
#18687=DIRECTION ( 'NONE',  ( 1.000000000000000000, 4.445489947300000020E-24, -2.257150022439999944E-12 ) ) ;
#18711=CARTESIAN_POINT ( 'NONE',  ( 7.013234437640000065E-10, 20.99999999999999645, -60.10000000000000142 ) ) ;
#18715=LINE ( 'NONE', #6602, #15806 ) ;
#18717=VERTEX_POINT ( 'NONE', #2503 ) ;
#18737=EDGE_CURVE ( 'NONE', #20099, #12344, #25023, .T. ) ;
#18738=CARTESIAN_POINT ( 'NONE',  ( 18.09234735182029041, -19.80227287648861889, -1.399999999999998579 ) ) ;
#18739=CARTESIAN_POINT ( 'NONE',  ( -15.86808677770000209, 10.47263190749999495, -0.7000000003999986564 ) ) ;
#18744=DIRECTION ( 'NONE',  ( 0.000000000000000000, 0.000000000000000000, 1.000000000000000000 ) ) ;
#18784=CARTESIAN_POINT ( 'NONE',  ( -10.69999999999999929, -129.6759735804000115, -38.47487552122000665 ) ) ;
#18787=CARTESIAN_POINT ( 'NONE',  ( -13.15654851664530511, 20.99999999997228528, -56.37844548362021868 ) ) ;
#18794=LINE ( 'NONE', #31073, #13787 ) ;
#18797=AXIS2_PLACEMENT_3D ( 'NONE', #26992, #27148, #17230 ) ;
#18800=LINE ( 'NONE', #30466, #12234 ) ;
#18812=B_SPLINE_CURVE_WITH_KNOTS ( 'NONE', 3,
 ( #21316, #4485, #19264, #30919 ),
 .UNSPECIFIED., .F., .F.,
 ( 4, 4 ),
 ( 0.000000000000000000, 1.000000000000000000 ),
 .UNSPECIFIED. ) ;
#18813=AXIS2_PLACEMENT_3D ( 'NONE', #1700, #18376, #6720 ) ;
#18815=CARTESIAN_POINT ( 'NONE',  ( 9.998463852539998697, 19.99999999999999645, -42.46069674353999801 ) ) ;
#18817=VECTOR ( 'NONE', #9816, 1000.000000000000000 ) ;
#18824=CARTESIAN_POINT ( 'NONE',  ( 10.69999999999999929, -29.06671945340000107, -26.22544931050000017 ) ) ;
#18825=DIRECTION ( 'NONE',  ( 0.000000000000000000, 1.000000000000000000, 0.000000000000000000 ) ) ;
#18828=DIRECTION ( 'NONE',  ( -2.537652630420000242E-15, 0.000000000000000000, 1.000000000000000000 ) ) ;
#18873=PLANE ( 'NONE',  #1671 ) ;
#18876=EDGE_CURVE ( 'NONE', #29870, #11243, #15655, .T. ) ;
#18879=ORIENTED_EDGE ( 'NONE', *, *, #20119, .T. ) ;
#18881=DIRECTION ( 'NONE',  ( 0.000000000000000000, 2.257157423930000049E-12, 1.000000000000000000 ) ) ;
#18895=CARTESIAN_POINT ( 'NONE',  ( 9.999999999939999995, -25.00000000000000000, -16.71944709739999979 ) ) ;
#18898=CARTESIAN_POINT ( 'NONE',  ( 15.51202505004052057, -21.88245214056498611, -1.399999999999998357 ) ) ;
#18910=CARTESIAN_POINT ( 'NONE',  ( -24.04002993240373698, -11.89710236790277520, -1.399999999999998579 ) ) ;
#18919=ADVANCED_FACE ( 'NONE', ( #30164 ), #8597, .F. ) ;
#18922=ORIENTED_EDGE ( 'NONE', *, *, #20540, .T. ) ;
#18923=ORIENTED_EDGE ( 'NONE', *, *, #15135, .T. ) ;
#18926=ORIENTED_EDGE ( 'NONE', *, *, #1972, .T. ) ;
#18935=ORIENTED_EDGE ( 'NONE', *, *, #17643, .F. ) ;
#18947=B_SPLINE_CURVE_WITH_KNOTS ( 'NONE', 3,
 ( #11142, #4369, #18206, #28281 ),
 .UNSPECIFIED., .F., .F.,
 ( 4, 4 ),
 ( 0.000000000000000000, 1.000000000000000000 ),
 .UNSPECIFIED. ) ;
#18949=CARTESIAN_POINT ( 'NONE',  ( -9.999999999979998222, -27.00000000000000000, -31.39999999999999858 ) ) ;
#18950=CARTESIAN_POINT ( 'NONE',  ( 10.69999999998082174, -126.8166236165483554, -33.90282598914290446 ) ) ;
#18962=ORIENTED_EDGE ( 'NONE', *, *, #598, .T. ) ;
#18966=CARTESIAN_POINT ( 'NONE',  ( -4.175165894169885483, -55.00000000000000000, -44.10000000000000142 ) ) ;
#18974=FACE_OUTER_BOUND ( 'NONE', #24764, .T. ) ;
#18975=EDGE_LOOP ( 'NONE', ( #22872, #6616, #17971, #30255 ) ) ;
#18976=LINE ( 'NONE', #28584, #1949 ) ;
#18980=AXIS2_PLACEMENT_3D ( 'NONE', #18389, #11002, #28144 ) ;
#18984=VECTOR ( 'NONE', #10639, 1000.000000000000000 ) ;
#18985=DIRECTION ( 'NONE',  ( -0.000000000000000000, 1.000000000000000000, -2.257145581549999994E-12 ) ) ;
#18986=AXIS2_PLACEMENT_3D ( 'NONE', #12170, #4940, #19417 ) ;
#18993=VERTEX_POINT ( 'NONE', #28120 ) ;
#19002=B_SPLINE_CURVE_WITH_KNOTS ( 'NONE', 3,
 ( #7273, #16863, #29438, #2856, #24257, #5062 ),
 .UNSPECIFIED., .F., .F.,
 ( 4, 2, 4 ),
 ( 0.000000000000000000, 0.5000000000000000000, 1.000000000000000000 ),
 .UNSPECIFIED. ) ;
#19003=AXIS2_PLACEMENT_3D ( 'NONE', #19176, #4547, #4700 ) ;
#19004=DIRECTION ( 'NONE',  ( -1.000000000000000000, 0.000000000000000000, -2.257144471330000330E-12 ) ) ;
#19008=DIRECTION ( 'NONE',  ( -2.537652630420000242E-15, 0.000000000000000000, 1.000000000000000000 ) ) ;
#19016=ORIENTED_EDGE ( 'NONE', *, *, #23525, .F. ) ;
#19024=CARTESIAN_POINT ( 'NONE',  ( -12.47331730070000155, 21.70000000000000284, -55.90289625529999995 ) ) ;
#19031=ADVANCED_FACE ( 'NONE', ( #4975 ), #24174, .F. ) ;
#19032=CARTESIAN_POINT ( 'NONE',  ( 9.999999999949999108, -30.49251257979999963, -21.04205368479999905 ) ) ;
#19039=ORIENTED_EDGE ( 'NONE', *, *, #20020, .F. ) ;
#19054=EDGE_CURVE ( 'NONE', #23803, #20395, #28271, .T. ) ;
#19056=LINE ( 'NONE', #28960, #28194 ) ;
#19058=ORIENTED_EDGE ( 'NONE', *, *, #8269, .T. ) ;
#19066=EDGE_CURVE ( 'NONE', #4970, #20193, #25926, .T. ) ;
#19078=VERTEX_POINT ( 'NONE', #4519 ) ;
#19087=CARTESIAN_POINT ( 'NONE',  ( 9.999999999958301800, -27.75984822500470273, -25.47305230110710994 ) ) ;
#19089=DIRECTION ( 'NONE',  ( 0.000000000000000000, 0.000000000000000000, 1.000000000000000000 ) ) ;
#19091=( LENGTH_UNIT ( ) NAMED_UNIT ( * ) SI_UNIT ( .MILLI., .METRE. ) );
#19093=EDGE_CURVE ( 'NONE', #29138, #20583, #14428, .T. ) ;
#19097=CARTESIAN_POINT ( 'NONE',  ( 11.32877539780000120, -24.28840541759999994, -0.7339858088999950958 ) ) ;
#19100=DIRECTION ( 'NONE',  ( 0.000000000000000000, 1.000000000000000000, 0.000000000000000000 ) ) ;
#19102=ORIENTED_EDGE ( 'NONE', *, *, #6620, .F. ) ;
#19104=CARTESIAN_POINT ( 'NONE',  ( -10.69999999999999929, -130.0000000000000000, -40.31722800480000046 ) ) ;
#19107=PLANE ( 'NONE',  #18986 ) ;
#19109=LINE ( 'NONE', #26046, #16743 ) ;
#19110=CARTESIAN_POINT ( 'NONE',  ( 4.175165894169885483, -119.7166638525666826, -44.10000000000000142 ) ) ;
#19111=ORIENTED_EDGE ( 'NONE', *, *, #30478, .T. ) ;
#19112=CARTESIAN_POINT ( 'NONE',  ( -10.69999999999999929, -24.87868251500000127, -30.52131748510000264 ) ) ;
#19117=ORIENTED_EDGE ( 'NONE', *, *, #13335, .F. ) ;
#19118=DIRECTION ( 'NONE',  ( 0.000000000000000000, 0.000000000000000000, -1.000000000000000000 ) ) ;
#19121=DIRECTION ( 'NONE',  ( -1.000000000000000000, 6.565028073413479156E-24, -2.257144471327815248E-12 ) ) ;
#19130=LINE ( 'NONE', #22545, #26569 ) ;
#19135=CARTESIAN_POINT ( 'NONE',  ( 11.78524365254896011, 20.99999999989818278, -70.02191803005808879 ) ) ;
#19136=ADVANCED_FACE ( 'NONE', ( #21505 ), #16770, .F. ) ;
#19140=CARTESIAN_POINT ( 'NONE',  ( 10.69999999996178985, -27.75961006684773835, -25.47288920101188125 ) ) ;
#19163=ORIENTED_EDGE ( 'NONE', *, *, #6098, .T. ) ;
#19167=CARTESIAN_POINT ( 'NONE',  ( 12.12499559729999810, 20.99999999999999645, -55.73512174120000395 ) ) ;
#19176=CARTESIAN_POINT ( 'NONE',  ( -11.49999999969999998, 20.99999999990000887, -70.09999999999999432 ) ) ;
#19179=CARTESIAN_POINT ( 'NONE',  ( -10.07772970569999949, -25.00000000000000000, -1.850024072400001440 ) ) ;
#19188=CARTESIAN_POINT ( 'NONE',  ( 8.999999999770000869, 21.64982007969998890, -44.65000838630700031 ) ) ;
#19210=LINE ( 'NONE', #23636, #29697 ) ;
#19211=AXIS2_PLACEMENT_3D ( 'NONE', #21156, #2117, #9182 ) ;
#19213=EDGE_CURVE ( 'NONE', #18136, #20876, #11818, .T. ) ;
#19216=CARTESIAN_POINT ( 'NONE',  ( 11.69999999989999928, 19.99999999999999645, -1.399999999299995856 ) ) ;
#19225=DIRECTION ( 'NONE',  ( -1.000000000000000000, 0.000000000000000000, -2.257144471330000330E-12 ) ) ;
#19226=AXIS2_PLACEMENT_3D ( 'NONE', #8106, #15832, #6222 ) ;
#19242=CARTESIAN_POINT ( 'NONE',  ( -10.69999999999999929, -24.87868251500000127, -30.52131748510000264 ) ) ;
#19243=ORIENTED_EDGE ( 'NONE', *, *, #31101, .T. ) ;
#19244=CARTESIAN_POINT ( 'NONE',  ( 10.69999999999999929, -130.0000000000000000, -42.39999999999999858 ) ) ;
#19247=FACE_OUTER_BOUND ( 'NONE', #7620, .T. ) ;
#19260=CARTESIAN_POINT ( 'NONE',  ( -13.99999999969999820, 21.69999999929999390, -67.09999999999999432 ) ) ;
#19264=CARTESIAN_POINT ( 'NONE',  ( 12.63375938795768150, 20.99999999997314148, -55.99857472579974882 ) ) ;
#19267=CARTESIAN_POINT ( 'NONE',  ( -9.999999999979998222, -27.00000000000000000, -31.39999999999999858 ) ) ;
#19272=ORIENTED_EDGE ( 'NONE', *, *, #29945, .T. ) ;
#19292=ORIENTED_EDGE ( 'NONE', *, *, #16313, .T. ) ;
#19294=FACE_OUTER_BOUND ( 'NONE', #3192, .T. ) ;
#19297=DIRECTION ( 'NONE',  ( 0.000000000000000000, 0.000000000000000000, 1.000000000000000000 ) ) ;
#19298=DIRECTION ( 'NONE',  ( -1.000000000000000000, 0.000000000000000000, 0.000000000000000000 ) ) ;
#19308=DIRECTION ( 'NONE',  ( -1.553791817432423893E-12, -0.7253743710120292842, 0.6883545756940262494 ) ) ;
#19309=EDGE_CURVE ( 'NONE', #25785, #1607, #1971, .T. ) ;
#19310=ORIENTED_EDGE ( 'NONE', *, *, #19309, .F. ) ;
#19311=CARTESIAN_POINT ( 'NONE',  ( -15.86808677770000209, 10.47263190749999495, -1.399999999599998990 ) ) ;
#19313=ORIENTED_EDGE ( 'NONE', *, *, #17508, .F. ) ;
#19318=AXIS2_PLACEMENT_3D ( 'NONE', #23692, #16897, #26198 ) ;
#19321=VECTOR ( 'NONE', #16617, 1000.000000000000000 ) ;
#19333=ORIENTED_EDGE ( 'NONE', *, *, #13396, .T. ) ;
#19334=CARTESIAN_POINT ( 'NONE',  ( -9.000000000000000000, 19.99999999999999645, -43.39999999999999858 ) ) ;
#19340=VECTOR ( 'NONE', #3976, 1000.000000000000000 ) ;
#19343=CARTESIAN_POINT ( 'NONE',  ( 11.69999999989999928, 19.99999999999999645, -0.6999999999999992895 ) ) ;
#19352=VECTOR ( 'NONE', #18628, 1000.000000000000000 ) ;
#19391=ORIENTED_EDGE ( 'NONE', *, *, #20119, .F. ) ;
#19402=VERTEX_POINT ( 'NONE', #10865 ) ;
#19417=DIRECTION ( 'NONE',  ( -1.000000000000000000, 4.306888218146944883E-11, 0.000000000000000000 ) ) ;
#19426=ORIENTED_EDGE ( 'NONE', *, *, #19093, .T. ) ;
#19428=FACE_OUTER_BOUND ( 'NONE', #21659, .T. ) ;
#19433=ORIENTED_EDGE ( 'NONE', *, *, #11521, .F. ) ;
#19440=CARTESIAN_POINT ( 'NONE',  ( -16.06710956638348620, 11.80217809800966222, -1.400000000000001910 ) ) ;
#19459=VECTOR ( 'NONE', #23977, 1000.000000000000000 ) ;
#19461=CARTESIAN_POINT ( 'NONE',  ( 10.69999999930000101, -29.12132034360000077, -30.52132034359999935 ) ) ;
#19481=VECTOR ( 'NONE', #2483, 1000.000000000000000 ) ;
#19499=CARTESIAN_POINT ( 'NONE',  ( 10.69999999999945040, -25.27195344073095029, -25.92068947042448457 ) ) ;
#19500=CARTESIAN_POINT ( 'NONE',  ( 10.69999999999999929, -29.12132034360000077, -30.52132034359999935 ) ) ;
#19509=EDGE_LOOP ( 'NONE', ( #441, #8814, #27305, #28727 ) ) ;
#19510=DIRECTION ( 'NONE',  ( -1.000000000000000000, 0.000000000000000000, 0.000000000000000000 ) ) ;
#19526=CARTESIAN_POINT ( 'NONE',  ( 13.12132034340000075, 20.99999999999999645, -69.22132034359999864 ) ) ;
#19535=B_SPLINE_CURVE_WITH_KNOTS ( 'NONE', 3,
 ( #20004, #11343, #23774, #20939, #8813, #25670 ),
 .UNSPECIFIED., .F., .F.,
 ( 4, 2, 4 ),
 ( 0.000000000000000000, 0.5000000000000000000, 1.000000000000000000 ),
 .UNSPECIFIED. ) ;
#19536=PLANE ( 'NONE',  #24351 ) ;
#19537=LINE ( 'NONE', #11979, #29719 ) ;
#19540=CARTESIAN_POINT ( 'NONE',  ( 16.21960138463431278, 10.42209091437901414, -1.400000000000001910 ) ) ;
#19544=VECTOR ( 'NONE', #4968, 1000.000000000000114 ) ;
#19555=CYLINDRICAL_SURFACE ( 'NONE', #17972, 5.000000000000001776 ) ;
#19561=DIRECTION ( 'NONE',  ( 1.595945597898660305E-12, 0.7071067811865475727, 0.7071067811865475727 ) ) ;
#19563=CARTESIAN_POINT ( 'NONE',  ( -13.99999999967382180, 20.99999999990389554, -67.49269908163661569 ) ) ;
#19564=CARTESIAN_POINT ( 'NONE',  ( 10.69999999996386286, -29.23055083351040295, -26.39047791497910112 ) ) ;
#19565=ORIENTED_EDGE ( 'NONE', *, *, #28647, .F. ) ;
#19566=VECTOR ( 'NONE', #11242, 1000.000000000000000 ) ;
#19568=DIRECTION ( 'NONE',  ( 0.000000000000000000, 1.000000000000000000, 0.000000000000000000 ) ) ;
#19571=DIRECTION ( 'NONE',  ( -1.180736691910036071E-13, -0.9986295347540310452, -0.05233595625330160483 ) ) ;
#19573=VECTOR ( 'NONE', #9533, 1000.000000000000114 ) ;
#19575=CARTESIAN_POINT ( 'NONE',  ( -10.69999999999999929, -25.17332254459999774, -30.78523849680000168 ) ) ;
#19582=CARTESIAN_POINT ( 'NONE',  ( 9.999999999925533345, -25.12044511670515590, -9.805662262714768929 ) ) ;
#19583=ADVANCED_FACE ( 'NONE', ( #7376, #16968, #14771 ), #4867, .F. ) ;
#19602=ORIENTED_EDGE ( 'NONE', *, *, #16949, .T. ) ;
#19607=CYLINDRICAL_SURFACE ( 'NONE', #6724, 26.80000000000000071 ) ;
#19618=ORIENTED_EDGE ( 'NONE', *, *, #4950, .T. ) ;
#19630=DIRECTION ( 'NONE',  ( 0.000000000000000000, 0.000000000000000000, 1.000000000000000000 ) ) ;
#19640=EDGE_CURVE ( 'NONE', #11113, #8540, #25742, .T. ) ;
#19647=ADVANCED_FACE ( 'NONE', ( #14320 ), #21702, .T. ) ;
#19649=DIRECTION ( 'NONE',  ( 0.000000000000000000, 0.000000000000000000, 1.000000000000000000 ) ) ;
#19669=ORIENTED_EDGE ( 'NONE', *, *, #16138, .T. ) ;
#19670=CARTESIAN_POINT ( 'NONE',  ( -10.40384843829999895, -24.69832375660000423, -1.291913792900001301 ) ) ;
#19673=CYLINDRICAL_SURFACE ( 'NONE', #6946, 3.000000000000003997 ) ;
#19675=B_SPLINE_CURVE_WITH_KNOTS ( 'NONE', 3,
 ( #15858, #13967, #13488, #23578, #11294, #13650, #25775, #23104, #10827, #16009, #20414, #11136, #18522, #27645, #6088, #25622, #25300, #28124 ),
 .UNSPECIFIED., .F., .F.,
 ( 4, 2, 2, 2, 2, 2, 2, 2, 4 ),
 ( 0.000000000000000000, 0.1250000000000000000, 0.2500000000000000000, 0.3750000000000000000, 0.5000000000000000000, 0.6250000000000000000, 0.7500000000000000000, 0.8750000000000000000, 1.000000000000000000 ),
 .UNSPECIFIED. ) ;
#19690=CARTESIAN_POINT ( 'NONE',  ( 16.07052902885122592, 10.82847174432581028, -1.400000000000001910 ) ) ;
#19695=VECTOR ( 'NONE', #4612, 1000.000000000000114 ) ;
#19699=LINE ( 'NONE', #2705, #8792 ) ;
#19704=VERTEX_POINT ( 'NONE', #22316 ) ;
#19708=ORIENTED_EDGE ( 'NONE', *, *, #4608, .F. ) ;
#19710=ADVANCED_FACE ( 'NONE', ( #1071 ), #24980, .F. ) ;
#19718=PLANE ( 'NONE',  #24096 ) ;
#19720=CARTESIAN_POINT ( 'NONE',  ( 10.69999999999999929, -30.49251257979999963, -21.04205368479999905 ) ) ;
#19721=VERTEX_POINT ( 'NONE', #12870 ) ;
#19726=DIRECTION ( 'NONE',  ( 0.000000000000000000, -2.257145581549999994E-12, -1.000000000000000000 ) ) ;
#19728=CARTESIAN_POINT ( 'NONE',  ( -10.99999999969999998, 20.99999999999999645, -70.09999999999999432 ) ) ;
#19729=CARTESIAN_POINT ( 'NONE',  ( -10.69999999989999928, -45.00000000000000000, -7.274962170800002070 ) ) ;
#19736=LINE ( 'NONE', #27120, #5759 ) ;
#19748=CARTESIAN_POINT ( 'NONE',  ( 10.69999999999999929, -27.00000000000000000, -28.40000000000000213 ) ) ;
#19752=LINE ( 'NONE', #22264, #15433 ) ;
#19756=CARTESIAN_POINT ( 'NONE',  ( -10.69999999999999929, -24.87867968679999819, -26.27867968680000033 ) ) ;
#19757=LINE ( 'NONE', #31097, #20054 ) ;
#19758=VERTEX_POINT ( 'NONE', #27340 ) ;
#19765=CARTESIAN_POINT ( 'NONE',  ( 10.69999999999035722, -129.5232638600235759, -38.12979645447560983 ) ) ;
#19770=CARTESIAN_POINT ( 'NONE',  ( -9.707106781189999367, -55.00000000000000000, -43.10710678118599759 ) ) ;
#19776=AXIS2_PLACEMENT_3D ( 'NONE', #12503, #20061, #870 ) ;
#19778=CARTESIAN_POINT ( 'NONE',  ( 11.04680313989999796, -24.61949705740000027, -1.636966775500001248 ) ) ;
#19782=ORIENTED_EDGE ( 'NONE', *, *, #28090, .F. ) ;
#19783=CARTESIAN_POINT ( 'NONE',  ( 8.999999999799999983, 21.34999999950001026, -70.09999999999999432 ) ) ;
#19792=AXIS2_PLACEMENT_3D ( 'NONE', #15829, #9049, #30300 ) ;
#19794=CARTESIAN_POINT ( 'NONE',  ( 10.69999999996684004, -29.94035316038524641, -27.70911855536421697 ) ) ;
#19796=LINE ( 'NONE', #9724, #21568 ) ;
#19807=CARTESIAN_POINT ( 'NONE',  ( -10.69999999999999929, -122.9701038226999827, -31.65529867039999701 ) ) ;
#19812=VECTOR ( 'NONE', #588, 1000.000000000000000 ) ;
#19813=AXIS2_PLACEMENT_3D ( 'NONE', #22211, #15123, #29437 ) ;
#19830=EDGE_CURVE ( 'NONE', #2860, #21717, #16207, .T. ) ;
#19843=LINE ( 'NONE', #23098, #17310 ) ;
#19850=CARTESIAN_POINT ( 'NONE',  ( 9.999999999967510433, -24.00000000000000355, -28.00651183392525567 ) ) ;
#19856=EDGE_CURVE ( 'NONE', #26528, #16525, #19675, .T. ) ;
#19867=ORIENTED_EDGE ( 'NONE', *, *, #23852, .T. ) ;
#19871=CARTESIAN_POINT ( 'NONE',  ( -10.69999999999999929, -24.95051674469999980, -26.20881489450000146 ) ) ;
#19883=DIRECTION ( 'NONE',  ( 0.000000000000000000, -1.000000000000000000, 2.257145581549999994E-12 ) ) ;
#19885=CARTESIAN_POINT ( 'NONE',  ( 8.999999999770000869, 20.87254207907673731, -44.59478429471910488 ) ) ;
#19888=CARTESIAN_POINT ( 'NONE',  ( 8.999999999770000869, 21.35000000040000145, -51.10000000000000142 ) ) ;
#19889=CARTESIAN_POINT ( 'NONE',  ( -11.62710820939999934, -24.17108566160000294, -1.401657795899999392 ) ) ;
#19900=PLANE ( 'NONE',  #11463 ) ;
#19910=B_SPLINE_CURVE_WITH_KNOTS ( 'NONE', 3,
 ( #10619, #6367, #25729, #6047, #1501, #3530 ),
 .UNSPECIFIED., .F., .F.,
 ( 4, 2, 4 ),
 ( 0.000000000000000000, 0.5000000000000000000, 1.000000000000000000 ),
 .UNSPECIFIED. ) ;
#19928=VERTEX_POINT ( 'NONE', #7346 ) ;
#19929=DIRECTION ( 'NONE',  ( 1.000000000000000000, 0.000000000000000000, 0.000000000000000000 ) ) ;
#19930=CARTESIAN_POINT ( 'NONE',  ( 11.69999999989999928, -2.055600358200002198, -0.6999999999999992895 ) ) ;
#19936=ORIENTED_EDGE ( 'NONE', *, *, #16949, .F. ) ;
#19947=AXIS2_PLACEMENT_3D ( 'NONE', #411, #21958, #4817 ) ;
#19950=CARTESIAN_POINT ( 'NONE',  ( 13.99999999979999821, 21.69999999929999390, -67.09999999999999432 ) ) ;
#19951=VECTOR ( 'NONE', #15173, 1000.000000000000000 ) ;
#19952=CARTESIAN_POINT ( 'NONE',  ( 9.999999999966984632, -29.92191803010020834, -29.18524365260708819 ) ) ;
#19957=FACE_OUTER_BOUND ( 'NONE', #26971, .T. ) ;
#19963=ORIENTED_EDGE ( 'NONE', *, *, #1348, .F. ) ;
#19972=CARTESIAN_POINT ( 'NONE',  ( -11.51411769270000107, -24.20066399839999960, -0.7084723282999999538 ) ) ;
#19974=ADVANCED_FACE ( 'NONE', ( #14592 ), #14279, .F. ) ;
#19978=DIRECTION ( 'NONE',  ( -0.000000000000000000, 1.000000000000000000, -2.257145581549999994E-12 ) ) ;
#19979=CARTESIAN_POINT ( 'NONE',  ( -10.69999999996385398, -38.97187125431320709, -26.38763492401018596 ) ) ;
#19981=ORIENTED_EDGE ( 'NONE', *, *, #17330, .T. ) ;
#19986=EDGE_CURVE ( 'NONE', #27200, #17105, #9550, .T. ) ;
#19989=DIRECTION ( 'NONE',  ( -5.551115123047629543E-18, 6.252214723449840749E-31, -1.000000000000000000 ) ) ;
#19996=VERTEX_POINT ( 'NONE', #4835 ) ;
#19997=CYLINDRICAL_SURFACE ( 'NONE', #11260, 1.099999999999999201 ) ;
#20004=CARTESIAN_POINT ( 'NONE',  ( -10.00000000000000000, -130.0000000000000000, -41.24671599790000442 ) ) ;
#20007=AXIS2_PLACEMENT_3D ( 'NONE', #6076, #27789, #8747 ) ;
#20016=DIRECTION ( 'NONE',  ( -1.000000000000000000, 0.000000000000000000, 0.000000000000000000 ) ) ;
#20020=EDGE_CURVE ( 'NONE', #21103, #24608, #11906, .T. ) ;
#20024=DIRECTION ( 'NONE',  ( 2.257144471330000330E-12, -0.000000000000000000, -1.000000000000000000 ) ) ;
#20033=PLANE ( 'NONE',  #10769 ) ;
#20043=VERTEX_POINT ( 'NONE', #24336 ) ;
#20047=VERTEX_POINT ( 'NONE', #3077 ) ;
#20054=VECTOR ( 'NONE', #17386, 1000.000000000000000 ) ;
#20061=DIRECTION ( 'NONE',  ( -0.5882352941176968164, 0.000000000000000000, -0.8086898285215826654 ) ) ;
#20066=B_SPLINE_CURVE_WITH_KNOTS ( 'NONE', 3,
 ( #11302, #16477, #9866, #16940 ),
 .UNSPECIFIED., .F., .F.,
 ( 4, 4 ),
 ( 0.000000000000000000, 1.000000000000000000 ),
 .UNSPECIFIED. ) ;
#20068=VECTOR ( 'NONE', #14846, 1000.000000000000000 ) ;
#20074=LINE ( 'NONE', #27449, #7985 ) ;
#20075=CYLINDRICAL_SURFACE ( 'NONE', #4651, 1.000000000000000666 ) ;
#20084=CARTESIAN_POINT ( 'NONE',  ( 10.93755790620000035, -24.69832375569999883, -1.748184582200003279 ) ) ;
#20089=EDGE_CURVE ( 'NONE', #15501, #29138, #11109, .T. ) ;
#20093=B_SPLINE_CURVE_WITH_KNOTS ( 'NONE', 3,
 ( #697, #10285, #19885, #15767, #20963, #16083 ),
 .UNSPECIFIED., .F., .F.,
 ( 4, 2, 4 ),
 ( 0.000000000000000000, 0.5000000000000000000, 1.000000000000000000 ),
 .UNSPECIFIED. ) ;
#20094=ORIENTED_EDGE ( 'NONE', *, *, #27097, .F. ) ;
#20098=EDGE_LOOP ( 'NONE', ( #20625, #16290, #2726, #30277 ) ) ;
#20099=VERTEX_POINT ( 'NONE', #1040 ) ;
#20102=CARTESIAN_POINT ( 'NONE',  ( -9.500000000000000000, 20.99999999999999645, -64.10000000019999788 ) ) ;
#20103=CARTESIAN_POINT ( 'NONE',  ( 18.18153821496158074, 11.44785871222162754, -1.400000000000001910 ) ) ;
#20105=DIRECTION ( 'NONE',  ( -0.000000000000000000, 1.000000000000000000, -2.257145581549999994E-12 ) ) ;
#20116=DIRECTION ( 'NONE',  ( -5.551115123049999208E-18, 0.000000000000000000, -1.000000000000000000 ) ) ;
#20119=EDGE_CURVE ( 'NONE', #27091, #5518, #15051, .T. ) ;
#20122=ORIENTED_EDGE ( 'NONE', *, *, #7700, .F. ) ;
#20127=ORIENTED_EDGE ( 'NONE', *, *, #26593, .F. ) ;
#20130=EDGE_LOOP ( 'NONE', ( #9864, #638, #8929, #11346 ) ) ;
#20152=ORIENTED_EDGE ( 'NONE', *, *, #18165, .F. ) ;
#20156=AXIS2_PLACEMENT_3D ( 'NONE', #16898, #16442, #6840 ) ;
#20165=ORIENTED_EDGE ( 'NONE', *, *, #26364, .T. ) ;
#20167=CARTESIAN_POINT ( 'NONE',  ( -10.69999999999999929, -55.00000000000000000, -42.39999999999999858 ) ) ;
#20168=CARTESIAN_POINT ( 'NONE',  ( 10.69999999930000101, -24.87867965640000278, -30.52132034359999935 ) ) ;
#20171=LINE ( 'NONE', #8505, #5498 ) ;
#20177=CARTESIAN_POINT ( 'NONE',  ( 8.999999999770000869, 20.99999999999999645, -64.10000000000000853 ) ) ;
#20181=CARTESIAN_POINT ( 'NONE',  ( 10.69999999996291429, -37.77882377713213913, -25.96954458904216878 ) ) ;
#20184=CARTESIAN_POINT ( 'NONE',  ( 10.94971450390000101, -24.68950648870000109, -1.737779124299995814 ) ) ;
#20185=ORIENTED_EDGE ( 'NONE', *, *, #14778, .F. ) ;
#20193=VERTEX_POINT ( 'NONE', #15975 ) ;
#20197=EDGE_LOOP ( 'NONE', ( #19243, #11879, #13539, #28836 ) ) ;
#20214=CARTESIAN_POINT ( 'NONE',  ( -10.69999999999999929, -27.00000000000000000, -28.40000000000000213 ) ) ;
#20221=CARTESIAN_POINT ( 'NONE',  ( 10.35000000039999968, -130.0000000000000000, -41.24671599790000442 ) ) ;
#20223=VERTEX_POINT ( 'NONE', #21016 ) ;
#20230=CARTESIAN_POINT ( 'NONE',  ( -25.87421760616039279, 7.312998917024513545, -0.6999999999999991784 ) ) ;
#20251=VECTOR ( 'NONE', #27647, 1000.000000000000000 ) ;
#20252=B_SPLINE_CURVE_WITH_KNOTS ( 'NONE', 3,
 ( #30655, #11297, #9081, #28438, #8765, #1853 ),
 .UNSPECIFIED., .F., .F.,
 ( 4, 2, 4 ),
 ( 0.000000000000000000, 0.5000000000000000000, 1.000000000000000000 ),
 .UNSPECIFIED. ) ;
#20259=FACE_BOUND ( 'NONE', #11654, .T. ) ;
#20269=VECTOR ( 'NONE', #12877, 1000.000000000000000 ) ;
#20273=CIRCLE ( 'NONE', #19792, 1.099999999570000497 ) ;
#20297=PLANE ( 'NONE',  #17740 ) ;
#20303=CARTESIAN_POINT ( 'NONE',  ( 10.02699808790000091, 19.99999999999999645, -2.016765154599996279 ) ) ;
#20319=AXIS2_PLACEMENT_3D ( 'NONE', #11068, #23032, #4303 ) ;
#20321=CARTESIAN_POINT ( 'NONE',  ( 11.69999999989999928, 19.99999999999999645, -0.6999999999999992895 ) ) ;
#20329=DIRECTION ( 'NONE',  ( -1.000000000000000000, 0.000000000000000000, 0.000000000000000000 ) ) ;
#20345=ORIENTED_EDGE ( 'NONE', *, *, #3930, .F. ) ;
#20350=ORIENTED_EDGE ( 'NONE', *, *, #18472, .T. ) ;
#20354=ORIENTED_EDGE ( 'NONE', *, *, #27154, .F. ) ;
#20363=CARTESIAN_POINT ( 'NONE',  ( 10.69999999999999929, 19.99999999999999645, -42.39999999999999858 ) ) ;
#20366=CARTESIAN_POINT ( 'NONE',  ( -25.87726812276423516, 7.302694712675908306, -1.399999999999998579 ) ) ;
#20372=ORIENTED_EDGE ( 'NONE', *, *, #939, .F. ) ;
#20379=CARTESIAN_POINT ( 'NONE',  ( -11.16922181809999870, -24.52928868880000124, -1.544021063100003976 ) ) ;
#20383=ADVANCED_FACE ( 'NONE', ( #7313 ), #28403, .F. ) ;
#20388=DIRECTION ( 'NONE',  ( 0.000000000000000000, -2.257145581549999994E-12, -1.000000000000000000 ) ) ;
#20395=VERTEX_POINT ( 'NONE', #10889 ) ;
#20397=ORIENTED_EDGE ( 'NONE', *, *, #5831, .T. ) ;
#20400=EDGE_LOOP ( 'NONE', ( #19669, #24395, #2862, #15059, #13535, #196, #19708, #26043, #23094, #3092, #19981, #20562 ) ) ;
#20407=ORIENTED_EDGE ( 'NONE', *, *, #24315, .F. ) ;
#20414=CARTESIAN_POINT ( 'NONE',  ( -17.59974562539740717, 10.19782190216913875, -1.400000000000001910 ) ) ;
#20425=DIRECTION ( 'NONE',  ( -0.8775825618903722036, -0.4794255386042041156, 0.000000000000000000 ) ) ;
#20430=EDGE_CURVE ( 'NONE', #20047, #17900, #23424, .T. ) ;
#20434=CARTESIAN_POINT ( 'NONE',  ( 9.500000000000000000, 20.99999999999999645, -60.10000000019999788 ) ) ;
#20436=LINE ( 'NONE', #11004, #29013 ) ;
#20441=CARTESIAN_POINT ( 'NONE',  ( -9.999999999979998222, -127.2536115484999897, -34.36329565063000047 ) ) ;
#20442=DIRECTION ( 'NONE',  ( 1.000000000000000000, 6.668066630619518976E-24, -2.257150022442225012E-12 ) ) ;
#20456=ORIENTED_EDGE ( 'NONE', *, *, #5597, .F. ) ;
#20458=CARTESIAN_POINT ( 'NONE',  ( 10.63581336919999920, 19.99999999999999645, -1.053405123100002783 ) ) ;
#20460=AXIS2_PLACEMENT_3D ( 'NONE', #2496, #11930, #12084 ) ;
#20466=VERTEX_POINT ( 'NONE', #18739 ) ;
#20467=( NAMED_UNIT ( * ) PLANE_ANGLE_UNIT ( ) SI_UNIT ( $, .RADIAN. ) );
#20469=DIRECTION ( 'NONE',  ( -0.7071067811870476172, 0.000000000000000000, -0.7071067811860475283 ) ) ;
#20491=FACE_OUTER_BOUND ( 'NONE', #14410, .T. ) ;
#20498=ORIENTED_EDGE ( 'NONE', *, *, #20430, .F. ) ;
#20501=VERTEX_POINT ( 'NONE', #11824 ) ;
#20502=DIRECTION ( 'NONE',  ( -0.7071067811870488384, 0.000000000000000000, -0.7071067811860461960 ) ) ;
#20507=ADVANCED_FACE ( 'NONE', ( #16536 ), #14033, .F. ) ;
#20512=DIRECTION ( 'NONE',  ( 0.000000000000000000, -1.000000000000000000, 2.257145581549999994E-12 ) ) ;
#20514=LINE ( 'NONE', #18142, #4920 ) ;
#20518=DIRECTION ( 'NONE',  ( -1.000000000000000000, 0.000000000000000000, 0.000000000000000000 ) ) ;
#20528=FACE_OUTER_BOUND ( 'NONE', #27925, .T. ) ;
#20531=DIRECTION ( 'NONE',  ( 1.000000000000000000, -0.000000000000000000, -2.257150022439999944E-12 ) ) ;
#20532=PLANE ( 'NONE',  #17703 ) ;
#20533=AXIS2_PLACEMENT_3D ( 'NONE', #110, #21660, #2608 ) ;
#20540=EDGE_CURVE ( 'NONE', #22220, #24506, #19210, .T. ) ;
#20551=ORIENTED_EDGE ( 'NONE', *, *, #2524, .F. ) ;
#20555=CARTESIAN_POINT ( 'NONE',  ( -11.39269908187263169, 20.99999999989999466, -70.09999999996071551 ) ) ;
#20562=ORIENTED_EDGE ( 'NONE', *, *, #27899, .F. ) ;
#20579=EDGE_CURVE ( 'NONE', #5895, #17734, #19056, .T. ) ;
#20583=VERTEX_POINT ( 'NONE', #28652 ) ;
#20590=CARTESIAN_POINT ( 'NONE',  ( -31.69999999989999395, 19.99999999999999645, -0.6999999999999992895 ) ) ;
#20593=DIRECTION ( 'NONE',  ( 0.000000000000000000, 1.000000000000000000, 0.000000000000000000 ) ) ;
#20620=ORIENTED_EDGE ( 'NONE', *, *, #2315, .F. ) ;
#20625=ORIENTED_EDGE ( 'NONE', *, *, #27121, .T. ) ;
#20637=CARTESIAN_POINT ( 'NONE',  ( 13.65677330047603633, -23.08588181436693176, -1.399999999999998801 ) ) ;
#20640=ORIENTED_EDGE ( 'NONE', *, *, #13209, .F. ) ;
#20650=VECTOR ( 'NONE', #26393, 1000.000000000000000 ) ;
#20669=CARTESIAN_POINT ( 'NONE',  ( 10.69999999989999928, 19.99999999999999645, -2.399999999999999467 ) ) ;
#20670=VERTEX_POINT ( 'NONE', #16082 ) ;
#20679=CARTESIAN_POINT ( 'NONE',  ( -9.999999999969999109, -24.87872937729999734, -30.52127062079999931 ) ) ;
#20683=CARTESIAN_POINT ( 'NONE',  ( -26.57440607989999748, -3.469982107200002108, -1.399999999999998579 ) ) ;
#20687=ORIENTED_EDGE ( 'NONE', *, *, #7196, .T. ) ;
#20714=CARTESIAN_POINT ( 'NONE',  ( -11.69999999989999928, -24.11120071670000087, -0.6999999999999992895 ) ) ;
#20720=CARTESIAN_POINT ( 'NONE',  ( -10.69999999999999929, -24.00000000000000000, -28.40000000000000213 ) ) ;
#20723=ORIENTED_EDGE ( 'NONE', *, *, #10118, .F. ) ;
#20750=LINE ( 'NONE', #20434, #401 ) ;
#20756=CARTESIAN_POINT ( 'NONE',  ( 10.69999999999999929, -29.12132034360000077, -30.52132034359999935 ) ) ;
#20794=CARTESIAN_POINT ( 'NONE',  ( -10.35000000009999965, 19.99999999999999645, -42.40000000045999684 ) ) ;
#20807=CARTESIAN_POINT ( 'NONE',  ( 10.00000000070000183, -130.0000000000000000, -41.24671599790000442 ) ) ;
#20812=CARTESIAN_POINT ( 'NONE',  ( -22.97825597456790092, -13.83688083289194992, -1.399999999999998579 ) ) ;
#20827=AXIS2_PLACEMENT_3D ( 'NONE', #12372, #16935, #26542 ) ;
#20828=EDGE_LOOP ( 'NONE', ( #5674, #29668, #10711, #701 ) ) ;
#20838=EDGE_CURVE ( 'NONE', #12344, #29903, #19537, .T. ) ;
#20846=LINE ( 'NONE', #30449, #19352 ) ;
#20858=CARTESIAN_POINT ( 'NONE',  ( 11.06030393429999847, -24.60936423240000082, -1.629296559500004182 ) ) ;
#20863=ORIENTED_EDGE ( 'NONE', *, *, #23502, .F. ) ;
#20873=CARTESIAN_POINT ( 'NONE',  ( 12.12499559729999810, 21.69999999929999390, -55.73512174120000395 ) ) ;
#20876=VERTEX_POINT ( 'NONE', #29736 ) ;
#20896=CARTESIAN_POINT ( 'NONE',  ( 0.000000000000000000, -130.0000000000000000, -43.39999999999999858 ) ) ;
#20904=ORIENTED_EDGE ( 'NONE', *, *, #31079, .F. ) ;
#20906=ORIENTED_EDGE ( 'NONE', *, *, #15047, .T. ) ;
#20935=PLANE ( 'NONE',  #9817 ) ;
#20939=CARTESIAN_POINT ( 'NONE',  ( -10.00000000021934099, -128.8192055956760953, -36.36585972233515918 ) ) ;
#20948=LINE ( 'NONE', #18895, #30052 ) ;
#20949=CARTESIAN_POINT ( 'NONE',  ( -10.00000000030000002, -28.14046567939999832, -25.54455802970000278 ) ) ;
#20963=CARTESIAN_POINT ( 'NONE',  ( 8.999999999770000869, 20.99999999959999997, -44.96700259529604438 ) ) ;
#20967=VERTEX_POINT ( 'NONE', #27679 ) ;
#20977=EDGE_CURVE ( 'NONE', #28677, #15618, #27998, .T. ) ;
#20987=DIRECTION ( 'NONE',  ( -1.000000000000000000, 0.000000000000000000, 0.000000000000000000 ) ) ;
#20993=FACE_OUTER_BOUND ( 'NONE', #20197, .T. ) ;
#21004=CARTESIAN_POINT ( 'NONE',  ( -10.69999999999999929, -129.1531271268999888, -37.03846033197000054 ) ) ;
#21006=VECTOR ( 'NONE', #26101, 1000.000000000000000 ) ;
#21009=CARTESIAN_POINT ( 'NONE',  ( 11.66358246589999936, -24.14124255329999968, -1.399999999999998579 ) ) ;
#21016=CARTESIAN_POINT ( 'NONE',  ( -8.999999999699999975, 21.69999999929999390, -51.10000000000999876 ) ) ;
#21024=FACE_OUTER_BOUND ( 'NONE', #21562, .T. ) ;
#21026=ORIENTED_EDGE ( 'NONE', *, *, #15468, .F. ) ;
#21034=DIRECTION ( 'NONE',  ( -1.000000000000000000, -6.565028073413479156E-24, -2.257144471327815248E-12 ) ) ;
#21035=CARTESIAN_POINT ( 'NONE',  ( 9.867241297310000547, 19.99999999999999645, -42.91081254286000046 ) ) ;
#21043=FACE_OUTER_BOUND ( 'NONE', #9154, .T. ) ;
#21055=CARTESIAN_POINT ( 'NONE',  ( 10.69999999999999929, -24.87867965640000278, -30.52132034359999935 ) ) ;
#21093=ORIENTED_EDGE ( 'NONE', *, *, #12701, .F. ) ;
#21101=ORIENTED_EDGE ( 'NONE', *, *, #23441, .F. ) ;
#21102=CIRCLE ( 'NONE', #25113, 1.099999999570000497 ) ;
#21103=VERTEX_POINT ( 'NONE', #19024 ) ;
#21108=LINE ( 'NONE', #30703, #28033 ) ;
#21111=CARTESIAN_POINT ( 'NONE',  ( 26.43121445407034287, -4.566620399128002994, -1.399999999999998579 ) ) ;
#21113=CARTESIAN_POINT ( 'NONE',  ( -10.99999999969999998, 20.99999999999999645, -58.51619611000000276 ) ) ;
#21118=CARTESIAN_POINT ( 'NONE',  ( -1.110223024630000146E-16, 0.000000000000000000, -44.10000000000000142 ) ) ;
#21120=DIRECTION ( 'NONE',  ( -1.000000000000000000, 0.000000000000000000, 0.000000000000000000 ) ) ;
#21127=CARTESIAN_POINT ( 'NONE',  ( 10.69999999989999928, -25.00000000000000000, -16.71944709739999979 ) ) ;
#21128=ORIENTED_EDGE ( 'NONE', *, *, #13338, .F. ) ;
#21134=ORIENTED_EDGE ( 'NONE', *, *, #10373, .T. ) ;
#21136=PLANE ( 'NONE',  #20319 ) ;
#21142=EDGE_CURVE ( 'NONE', #2860, #1244, #18668, .T. ) ;
#21150=CARTESIAN_POINT ( 'NONE',  ( -17.83928249649999742, 19.99999999999999645, -1.399999999999998579 ) ) ;
#21156=CARTESIAN_POINT ( 'NONE',  ( -9.000000000000000000, 19.99999999999999645, -42.39999999999999858 ) ) ;
#21161=FACE_OUTER_BOUND ( 'NONE', #14597, .T. ) ;
#21166=CARTESIAN_POINT ( 'NONE',  ( -10.69999999999999929, -24.00310551309999951, -28.69094250879999919 ) ) ;
#21209=ORIENTED_EDGE ( 'NONE', *, *, #15354, .T. ) ;
#21212=ORIENTED_EDGE ( 'NONE', *, *, #12614, .T. ) ;
#21221=EDGE_CURVE ( 'NONE', #17368, #30391, #13595, .T. ) ;
#21225=ORIENTED_EDGE ( 'NONE', *, *, #8961, .F. ) ;
#21226=CARTESIAN_POINT ( 'NONE',  ( 13.46518788483360041, 20.99999999997146105, -56.74319753100301256 ) ) ;
#21227=EDGE_CURVE ( 'NONE', #3911, #27980, #27034, .T. ) ;
#21230=CARTESIAN_POINT ( 'NONE',  ( -9.631068057916044367, 21.00000000000229861, -53.61809490181903470 ) ) ;
#21232=VECTOR ( 'NONE', #2391, 1000.000000000000000 ) ;
#21238=B_SPLINE_CURVE_WITH_KNOTS ( 'NONE', 3,
 ( #17093, #30958, #4673, #21514 ),
 .UNSPECIFIED., .F., .F.,
 ( 4, 4 ),
 ( 0.000000000000000000, 1.000000000000000000 ),
 .UNSPECIFIED. ) ;
#21248=ORIENTED_EDGE ( 'NONE', *, *, #2727, .F. ) ;
#21257=CARTESIAN_POINT ( 'NONE',  ( 10.69999999997255991, -29.39962415735867296, -30.24292916419924993 ) ) ;
#21262=CARTESIAN_POINT ( 'NONE',  ( 20.39644572738137285, -17.41965902382794695, -1.399999999999998579 ) ) ;
#21270=DIRECTION ( 'NONE',  ( -1.000000000000000000, 0.000000000000000000, 0.000000000000000000 ) ) ;
#21276=CARTESIAN_POINT ( 'NONE',  ( -10.00000000022208901, -26.89269887560480043, -15.86139282056708133 ) ) ;
#21284=EDGE_LOOP ( 'NONE', ( #14267, #4597, #27505, #2218 ) ) ;
#21305=ORIENTED_EDGE ( 'NONE', *, *, #21872, .T. ) ;
#21314=DIRECTION ( 'NONE',  ( -5.551115123049999208E-18, 0.000000000000000000, -1.000000000000000000 ) ) ;
#21316=CARTESIAN_POINT ( 'NONE',  ( 12.77819780750000156, 20.99999999999999645, -56.09999999999999432 ) ) ;
#21318=AXIS2_PLACEMENT_3D ( 'NONE', #113, #4974, #11597 ) ;
#21320=CARTESIAN_POINT ( 'NONE',  ( -10.00000000066199668, -27.39269908169871925, -31.40000000000157954 ) ) ;
#21325=LINE ( 'NONE', #4806, #28342 ) ;
#21345=CARTESIAN_POINT ( 'NONE',  ( -10.69999999999999929, -24.14402093200000010, -27.39080718840000017 ) ) ;
#21363=DIRECTION ( 'NONE',  ( -1.000000000000000000, 0.000000000000000000, -2.257144471330000330E-12 ) ) ;
#21365=AXIS2_PLACEMENT_3D ( 'NONE', #13483, #18195, #16156 ) ;
#21366=CYLINDRICAL_SURFACE ( 'NONE', #8217, 1.099999999999999201 ) ;
#21367=ORIENTED_EDGE ( 'NONE', *, *, #17166, .F. ) ;
#21369=EDGE_CURVE ( 'NONE', #12344, #29912, #13918, .T. ) ;
#21375=DIRECTION ( 'NONE',  ( 0.000000000000000000, 1.000000000000000000, 0.000000000000000000 ) ) ;
#21395=EDGE_CURVE ( 'NONE', #26472, #19928, #828, .T. ) ;
#21412=EDGE_LOOP ( 'NONE', ( #8526, #27356, #4148, #14975 ) ) ;
#21413=ORIENTED_EDGE ( 'NONE', *, *, #12685, .T. ) ;
#21414=EDGE_CURVE ( 'NONE', #11584, #18993, #2620, .T. ) ;
#21422=LINE ( 'NONE', #9292, #23545 ) ;
#21424=CARTESIAN_POINT ( 'NONE',  ( 10.69999999930000101, -30.00000000000000000, -28.40000000000000213 ) ) ;
#21432=CARTESIAN_POINT ( 'NONE',  ( 0.000000000000000000, 20.99999999999999645, -44.10000000017154065 ) ) ;
#21439=DIRECTION ( 'NONE',  ( 1.000000000000000000, 0.000000000000000000, 0.000000000000000000 ) ) ;
#21445=B_SPLINE_CURVE_WITH_KNOTS ( 'NONE', 3,
 ( #16280, #25898, #1191, #9515, #21320, #19267 ),
 .UNSPECIFIED., .F., .F.,
 ( 4, 2, 4 ),
 ( 0.000000000000000000, 0.5000000000000000000, 1.000000000000000000 ),
 .UNSPECIFIED. ) ;
#21447=EDGE_LOOP ( 'NONE', ( #23834, #30966, #16410, #23352 ) ) ;
#21450=ORIENTED_EDGE ( 'NONE', *, *, #6362, .T. ) ;
#21473=CARTESIAN_POINT ( 'NONE',  ( -10.00000000066199490, -26.60730091830108179, -31.40000000000157954 ) ) ;
#21480=CARTESIAN_POINT ( 'NONE',  ( 9.999999999938754769, -26.89269887572167761, -15.86139282090652891 ) ) ;
#21486=ORIENTED_EDGE ( 'NONE', *, *, #25923, .F. ) ;
#21489=VERTEX_POINT ( 'NONE', #2163 ) ;
#21496=CARTESIAN_POINT ( 'NONE',  ( -10.69999999992358397, -25.00000000000000355, -8.545053439230965608 ) ) ;
#21502=EDGE_CURVE ( 'NONE', #18431, #14341, #28592, .T. ) ;
#21505=FACE_OUTER_BOUND ( 'NONE', #9102, .T. ) ;
#21508=CARTESIAN_POINT ( 'NONE',  ( 8.999999999770000869, 20.13144615300854312, -44.09999999954493433 ) ) ;
#21511=CARTESIAN_POINT ( 'NONE',  ( -12.47331730070000155, 20.99999999999999645, -55.90289625529999995 ) ) ;
#21512=EDGE_CURVE ( 'NONE', #23430, #25954, #22442, .T. ) ;
#21514=CARTESIAN_POINT ( 'NONE',  ( 13.67718073920000066, 20.99999999999999645, -57.16242423349999768 ) ) ;
#21515=CARTESIAN_POINT ( 'NONE',  ( 10.69999999999999929, -120.0000000000000000, -41.24671599705000347 ) ) ;
#21517=AXIS2_PLACEMENT_3D ( 'NONE', #20590, #30188, #8620 ) ;
#21521=EDGE_CURVE ( 'NONE', #17900, #27200, #26353, .T. ) ;
#21542=LINE ( 'NONE', #16962, #29064 ) ;
#21543=AXIS2_PLACEMENT_3D ( 'NONE', #25758, #9366, #23562 ) ;
#21547=AXIS2_PLACEMENT_3D ( 'NONE', #8651, #12763, #22377 ) ;
#21556=CARTESIAN_POINT ( 'NONE',  ( 10.35000000039999968, -43.95328087560000085, -27.24755286599999948 ) ) ;
#21562=EDGE_LOOP ( 'NONE', ( #1784, #14764, #21574, #15142 ) ) ;
#21567=ORIENTED_EDGE ( 'NONE', *, *, #24317, .F. ) ;
#21568=VECTOR ( 'NONE', #22308, 1000.000000000000000 ) ;
#21574=ORIENTED_EDGE ( 'NONE', *, *, #3930, .T. ) ;
#21609=CARTESIAN_POINT ( 'NONE',  ( 9.999999999959413799, -28.79128384721942524, -25.96367195644973336 ) ) ;
#21613=CARTESIAN_POINT ( 'NONE',  ( 0.000000000000000000, 20.99999999999999645, -45.10000000000000142 ) ) ;
#21618=VERTEX_POINT ( 'NONE', #29974 ) ;
#21621=DIRECTION ( 'NONE',  ( 0.000000000000000000, 0.000000000000000000, 1.000000000000000000 ) ) ;
#21626=CARTESIAN_POINT ( 'NONE',  ( 13.12132034340000075, 21.69999999990000106, -69.22132034359999864 ) ) ;
#21633=CARTESIAN_POINT ( 'NONE',  ( -13.92227941755939113, 21.69999999994631423, -67.88484171643710852 ) ) ;
#21635=VERTEX_POINT ( 'NONE', #6058 ) ;
#21639=VECTOR ( 'NONE', #27669, 1000.000000000000000 ) ;
#21648=AXIS2_PLACEMENT_3D ( 'NONE', #23743, #18687, #21375 ) ;
#21654=LINE ( 'NONE', #28577, #1495 ) ;
#21659=EDGE_LOOP ( 'NONE', ( #7089, #30420, #25639, #15695, #7017, #3178 ) ) ;
#21660=DIRECTION ( 'NONE',  ( -9.982533390641031007E-25, -1.000000000000000000, 2.257145581550764975E-12 ) ) ;
#21665=CARTESIAN_POINT ( 'NONE',  ( 10.69999999999999929, -130.0000000000000000, -41.24671599790000442 ) ) ;
#21668=EDGE_CURVE ( 'NONE', #11176, #17105, #21445, .T. ) ;
#21671=VECTOR ( 'NONE', #16932, 1000.000000000000000 ) ;
#21672=CARTESIAN_POINT ( 'NONE',  ( 9.631484144028339855, 21.69999999997851603, -53.61927559727671166 ) ) ;
#21674=DIRECTION ( 'NONE',  ( -1.000000000000000000, -2.587524353642439916E-24, -2.257144471329210308E-12 ) ) ;
#21680=EDGE_CURVE ( 'NONE', #8971, #19758, #15288, .T. ) ;
#21702=CYLINDRICAL_SURFACE ( 'NONE', #1106, 1.700000000000000178 ) ;
#21704=CARTESIAN_POINT ( 'NONE',  ( -10.69999999999999929, -121.9099955515000033, -31.42347851140000259 ) ) ;
#21706=DIRECTION ( 'NONE',  ( 0.000000000000000000, 1.000000000000000000, 0.000000000000000000 ) ) ;
#21707=EDGE_CURVE ( 'NONE', #11113, #5951, #18794, .T. ) ;
#21710=ORIENTED_EDGE ( 'NONE', *, *, #14693, .F. ) ;
#21717=VERTEX_POINT ( 'NONE', #2439 ) ;
#21728=DIRECTION ( 'NONE',  ( 0.000000000000000000, 0.000000000000000000, -1.000000000000000000 ) ) ;
#21730=CARTESIAN_POINT ( 'NONE',  ( 0.000000000000000000, 21.70000000000000284, -45.10000000000000142 ) ) ;
#21734=CARTESIAN_POINT ( 'NONE',  ( 10.69999999930000101, -27.00000000000000000, -25.39999999999999858 ) ) ;
#21735=ADVANCED_FACE ( 'NONE', ( #12028 ), #11719, .F. ) ;
#21745=EDGE_CURVE ( 'NONE', #6537, #409, #25959, .T. ) ;
#21753=ORIENTED_EDGE ( 'NONE', *, *, #9046, .F. ) ;
#21758=ORIENTED_EDGE ( 'NONE', *, *, #7521, .F. ) ;
#21773=DIRECTION ( 'NONE',  ( -1.000000000000000000, 0.000000000000000000, 0.000000000000000000 ) ) ;
#21777=CARTESIAN_POINT ( 'NONE',  ( 12.84292916307208543, 21.69999999994266915, -69.49962415800092685 ) ) ;
#21788=CARTESIAN_POINT ( 'NONE',  ( 9.999999999941215023, -27.47344925854523368, -16.99201750777429965 ) ) ;
#21799=CARTESIAN_POINT ( 'NONE',  ( 10.69999999989999928, -45.00000000000000000, -7.274962170899998526 ) ) ;
#21809=ORIENTED_EDGE ( 'NONE', *, *, #2101, .T. ) ;
#21811=CARTESIAN_POINT ( 'NONE',  ( -9.000000000000000000, 20.99999999999999645, -64.10000000019999788 ) ) ;
#21831=ORIENTED_EDGE ( 'NONE', *, *, #2727, .T. ) ;
#21836=AXIS2_PLACEMENT_3D ( 'NONE', #16441, #7002, #11570 ) ;
#21840=EDGE_CURVE ( 'NONE', #4684, #12935, #19736, .T. ) ;
#21844=EDGE_CURVE ( 'NONE', #14134, #27320, #12635, .T. ) ;
#21868=CARTESIAN_POINT ( 'NONE',  ( -10.69999999999999929, -121.2050733649000023, -31.31359859269999646 ) ) ;
#21872=EDGE_CURVE ( 'NONE', #5618, #20193, #5554, .T. ) ;
#21878=CARTESIAN_POINT ( 'NONE',  ( 10.69999999999999929, -120.5233595624000174, -31.26042064949999855 ) ) ;
#21902=CARTESIAN_POINT ( 'NONE',  ( 17.83928249670000099, 20.00000000010000178, -0.6999999995999997005 ) ) ;
#21925=DIRECTION ( 'NONE',  ( 1.181300906760215537E-13, 0.9986295347541825906, 0.05233595625040957794 ) ) ;
#21931=CARTESIAN_POINT ( 'NONE',  ( 10.69999999992358575, -25.00000000000000711, -8.544674958192336689 ) ) ;
#21940=DIRECTION ( 'NONE',  ( 0.000000000000000000, -1.000000000000000000, 0.000000000000000000 ) ) ;
#21950=CARTESIAN_POINT ( 'NONE',  ( 10.69999999996928963, -24.00000000000000711, -28.79379052057399946 ) ) ;
#21958=DIRECTION ( 'NONE',  ( 0.000000000000000000, 0.000000000000000000, -1.000000000000000000 ) ) ;
#21969=ORIENTED_EDGE ( 'NONE', *, *, #3615, .F. ) ;
#21975=CARTESIAN_POINT ( 'NONE',  ( 10.69999999998643325, -128.7641386039167060, -36.38932005418158866 ) ) ;
#21986=ORIENTED_EDGE ( 'NONE', *, *, #18040, .F. ) ;
#21988=CARTESIAN_POINT ( 'NONE',  ( 10.99289321870000080, -24.65831413369999936, -1.692893218799999877 ) ) ;
#22002=LINE ( 'NONE', #12235, #28896 ) ;
#22003=DIRECTION ( 'NONE',  ( 1.000000000000000000, -0.000000000000000000, -2.257150022439999944E-12 ) ) ;
#22009=B_SPLINE_CURVE_WITH_KNOTS ( 'NONE', 4,
 ( #1762, #11353, #20949, #30553, #23478 ),
 .UNSPECIFIED., .F., .F.,
 ( 5, 5 ),
 ( -1.139969040210000006, 1.139969040210000006 ),
 .UNSPECIFIED. ) ;
#22026=VECTOR ( 'NONE', #58, 1000.000000000000000 ) ;
#22027=CARTESIAN_POINT ( 'NONE',  ( 9.000000000000000000, 19.99999999999999645, -43.39999999999999858 ) ) ;
#22041=CARTESIAN_POINT ( 'NONE',  ( -9.000000000000000000, -130.0000000000000000, -43.75000000037299941 ) ) ;
#22047=LINE ( 'NONE', #3139, #13729 ) ;
#22052=DIRECTION ( 'NONE',  ( -1.000000000000000000, 0.000000000000000000, -2.257144470970000261E-12 ) ) ;
#22063=AXIS2_PLACEMENT_3D ( 'NONE', #9846, #16763, #17227 ) ;
#22065=CARTESIAN_POINT ( 'NONE',  ( 13.12132034340000075, 20.99999999990000887, -69.22132034359999864 ) ) ;
#22068=EDGE_LOOP ( 'NONE', ( #15726, #7694, #8576, #30353, #7231, #21093, #20551, #25881, #10881, #1595, #12140, #4912, #2125, #8430, #22995, #22598, #10493 ) ) ;
#22076=EDGE_CURVE ( 'NONE', #24506, #11396, #26859, .T. ) ;
#22081=CARTESIAN_POINT ( 'NONE',  ( 9.999999999959999997, -24.87868334570000073, -26.27868334529999927 ) ) ;
#22089=DIRECTION ( 'NONE',  ( 3.092054264588954770E-24, -1.000000000000000000, 2.257145581552149937E-12 ) ) ;
#22096=ORIENTED_EDGE ( 'NONE', *, *, #25369, .F. ) ;
#22106=CARTESIAN_POINT ( 'NONE',  ( -10.00000000045850967, -123.0374659603429706, -31.63552742062627487 ) ) ;
#22107=EDGE_LOOP ( 'NONE', ( #5445, #20906, #6314, #15637, #22670 ) ) ;
#22112=DIRECTION ( 'NONE',  ( 0.000000000000000000, 0.000000000000000000, -1.000000000000000000 ) ) ;
#22115=LINE ( 'NONE', #5422, #6197 ) ;
#22126=CARTESIAN_POINT ( 'NONE',  ( 13.12132034340000075, 20.99999999990000887, -69.22132034359999864 ) ) ;
#22137=LINE ( 'NONE', #15360, #4223 ) ;
#22142=ORIENTED_EDGE ( 'NONE', *, *, #10971, .F. ) ;
#22154=ORIENTED_EDGE ( 'NONE', *, *, #28930, .T. ) ;
#22173=ORIENTED_EDGE ( 'NONE', *, *, #7586, .F. ) ;
#22183=CARTESIAN_POINT ( 'NONE',  ( 10.00000000070000183, -120.5233595624000174, -31.26042064949999855 ) ) ;
#22184=DIRECTION ( 'NONE',  ( 0.000000000000000000, 0.000000000000000000, 1.000000000000000000 ) ) ;
#22203=VECTOR ( 'NONE', #18828, 1000.000000000000000 ) ;
#22204=CARTESIAN_POINT ( 'NONE',  ( -10.35000000039999968, 19.99999999999999645, -2.399999999999999467 ) ) ;
#22209=VECTOR ( 'NONE', #21925, 1000.000000000000000 ) ;
#22210=VECTOR ( 'NONE', #6357, 1000.000000000000000 ) ;
#22211=CARTESIAN_POINT ( 'NONE',  ( 0.000000000000000000, 21.70000000000000284, -44.10000000017312516 ) ) ;
#22220=VERTEX_POINT ( 'NONE', #25143 ) ;
#22226=ORIENTED_EDGE ( 'NONE', *, *, #21221, .T. ) ;
#22230=EDGE_CURVE ( 'NONE', #13706, #5024, #13341, .T. ) ;
#22236=B_SPLINE_CURVE_WITH_KNOTS ( 'NONE', 5,
 ( #8874, #19104, #23684, #18784, #21004, #16120, #11404, #4625, #25889 ),
 .UNSPECIFIED., .F., .F.,
 ( 6, 3, 6 ),
 ( 0.000000000000000000, 6.585791987179998586, 10.75845896890000120 ),
 .UNSPECIFIED. ) ;
#22239=LINE ( 'NONE', #230, #18817 ) ;
#22240=DIRECTION ( 'NONE',  ( -0.7071067811865476838, -1.595945597898661315E-12, -0.7071067811865473507 ) ) ;
#22241=CARTESIAN_POINT ( 'NONE',  ( -10.69999999999999929, -24.87868251500000127, -30.52131748510000264 ) ) ;
#22250=VERTEX_POINT ( 'NONE', #15538 ) ;
#22254=EDGE_LOOP ( 'NONE', ( #30489, #10998, #15100, #17026 ) ) ;
#22260=DIRECTION ( 'NONE',  ( -1.000000000000000000, 0.000000000000000000, 0.000000000000000000 ) ) ;
#22264=CARTESIAN_POINT ( 'NONE',  ( -9.999999999559999964, 21.35000000040000145, -64.10000000000000853 ) ) ;
#22280=VECTOR ( 'NONE', #3777, 1000.000000000000000 ) ;
#22283=AXIS2_PLACEMENT_3D ( 'NONE', #13881, #14041, #21120 ) ;
#22292=LINE ( 'NONE', #19930, #4409 ) ;
#22294=ORIENTED_EDGE ( 'NONE', *, *, #16546, .T. ) ;
#22301=CARTESIAN_POINT ( 'NONE',  ( 8.999999999770000869, 21.70000000000000284, -45.10000000000000142 ) ) ;
#22308=DIRECTION ( 'NONE',  ( 0.000000000000000000, 1.000000000000000000, 0.000000000000000000 ) ) ;
#22316=CARTESIAN_POINT ( 'NONE',  ( -10.69999999999999929, -43.95328087560000085, -27.24755286599999948 ) ) ;
#22322=ADVANCED_FACE ( 'NONE', ( #30501 ), #23428, .F. ) ;
#22328=ORIENTED_EDGE ( 'NONE', *, *, #29311, .T. ) ;
#22333=ORIENTED_EDGE ( 'NONE', *, *, #25369, .T. ) ;
#22335=VERTEX_POINT ( 'NONE', #21055 ) ;
#22349=DIRECTION ( 'NONE',  ( 1.595945597898660305E-12, -0.7071067811865475727, 0.7071067811865475727 ) ) ;
#22353=VECTOR ( 'NONE', #27401, 1000.000000000000000 ) ;
#22359=CARTESIAN_POINT ( 'NONE',  ( -9.999999999939999995, -25.00000000000000000, -16.71944709739999979 ) ) ;
#22360=DIRECTION ( 'NONE',  ( -0.000000000000000000, 1.000000000000000000, -2.258510841069999963E-12 ) ) ;
#22372=CARTESIAN_POINT ( 'NONE',  ( 11.39835558780000113, 19.99999999999999645, -0.7167260558000043691 ) ) ;
#22377=DIRECTION ( 'NONE',  ( -1.000000000000000000, 0.000000000000000000, 0.000000000000000000 ) ) ;
#22388=DIRECTION ( 'NONE',  ( 0.000000000000000000, -1.000000000000000000, 0.000000000000000000 ) ) ;
#22392=CARTESIAN_POINT ( 'NONE',  ( 10.34999999979999963, -25.00000000000000000, -2.400000000399998612 ) ) ;
#22401=CARTESIAN_POINT ( 'NONE',  ( -11.69999999989999928, -24.11120071630000083, -1.399999999999998579 ) ) ;
#22402=DIRECTION ( 'NONE',  ( -0.000000000000000000, 1.000000000000000000, -2.255973188440000244E-12 ) ) ;
#22407=DIRECTION ( 'NONE',  ( 0.000000000000000000, -2.257157423930000049E-12, -1.000000000000000000 ) ) ;
#22415=B_SPLINE_CURVE_WITH_KNOTS ( 'NONE', 5,
 ( #29234, #24214, #7224, #10207, #14472, #17432, #28770, #19807, #21704, #7533, #21868, #29393, #7830, #16972, #316 ),
 .UNSPECIFIED., .F., .F.,
 ( 6, 3, 3, 3, 6 ),
 ( 10.75845896890000120, 13.17160131670000034, 18.65982209409999726, 20.85462969119999954, 21.51695459200000116 ),
 .UNSPECIFIED. ) ;
#22424=CARTESIAN_POINT ( 'NONE',  ( 11.50543345310245513, 20.99999999999807798, -55.48449633255769697 ) ) ;
#22442=LINE ( 'NONE', #19770, #28340 ) ;
#22447=EDGE_LOOP ( 'NONE', ( #11617, #17512, #2059, #16942 ) ) ;
#22448=CARTESIAN_POINT ( 'NONE',  ( 11.69999999989999928, -24.11120071670000087, -0.6999999999999992895 ) ) ;
#22449=DIRECTION ( 'NONE',  ( 0.000000000000000000, 0.000000000000000000, -1.000000000000000000 ) ) ;
#22458=CARTESIAN_POINT ( 'NONE',  ( -12.12499970530000049, 21.69999999919999212, -55.73512393530000253 ) ) ;
#22460=CARTESIAN_POINT ( 'NONE',  ( 10.69999999999999929, -120.0000000000000000, -41.24671599705000347 ) ) ;
#22463=CYLINDRICAL_SURFACE ( 'NONE', #26085, 3.000000000000003997 ) ;
#22468=MECHANICAL_DESIGN_GEOMETRIC_PRESENTATION_REPRESENTATION('',(#29487),#8889);
#22471=DIRECTION ( 'NONE',  ( -0.000000000000000000, 1.000000000000000000, -2.257145581549999994E-12 ) ) ;
#22486=CARTESIAN_POINT ( 'NONE',  ( 13.99999999999999822, 21.69999999994720596, -67.49379052020815095 ) ) ;
#22488=ORIENTED_EDGE ( 'NONE', *, *, #13092, .T. ) ;
#22489=ORIENTED_EDGE ( 'NONE', *, *, #15121, .T. ) ;
#22495=B_SPLINE_CURVE_WITH_KNOTS ( 'NONE', 3,
 ( #16626, #122, #5129, #21672, #24182, #14282 ),
 .UNSPECIFIED., .F., .F.,
 ( 4, 2, 4 ),
 ( 0.000000000000000000, 0.5000000000000000000, 1.000000000000000000 ),
 .UNSPECIFIED. ) ;
#22496=CARTESIAN_POINT ( 'NONE',  ( -10.32522729140000095, -24.73114799960000099, -1.399999999999998579 ) ) ;
#22498=DIRECTION ( 'NONE',  ( -1.000000000000000000, -6.565028073413479156E-24, -2.257144471327815248E-12 ) ) ;
#22499=FACE_OUTER_BOUND ( 'NONE', #1796, .T. ) ;
#22507=ADVANCED_FACE ( 'NONE', ( #17094 ), #26694, .T. ) ;
#22516=CARTESIAN_POINT ( 'NONE',  ( -10.00000000070000183, -29.30501631370000482, -26.47986984990000181 ) ) ;
#22542=AXIS2_PLACEMENT_3D ( 'NONE', #15524, #4044, #10818 ) ;
#22545=CARTESIAN_POINT ( 'NONE',  ( -10.00000000000000000, 21.69999999990000106, -70.10000000019999788 ) ) ;
#22550=CARTESIAN_POINT ( 'NONE',  ( 10.00000000000000000, -130.0000000000000000, -42.39999999999999858 ) ) ;
#22553=CARTESIAN_POINT ( 'NONE',  ( -12.47330046629999956, 20.99999999999999645, -55.90292611659999977 ) ) ;
#22576=AXIS2_PLACEMENT_3D ( 'NONE', #3564, #10968, #29843 ) ;
#22579=LINE ( 'NONE', #8547, #7502 ) ;
#22583=PRODUCT_DEFINITION_CONTEXT ( 'detailed design', #29463, 'design' ) ;
#22585=AXIS2_PLACEMENT_3D ( 'NONE', #3999, #1805, #13597 ) ;
#22589=ORIENTED_EDGE ( 'NONE', *, *, #2678, .T. ) ;
#22593=CARTESIAN_POINT ( 'NONE',  ( 9.999999999961779906, -26.27019589019406709, -25.46727582019148173 ) ) ;
#22598=ORIENTED_EDGE ( 'NONE', *, *, #13338, .T. ) ;
#22605=VECTOR ( 'NONE', #12424, 1000.000000000000000 ) ;
#22607=LINE ( 'NONE', #1045, #18984 ) ;
#22614=LINE ( 'NONE', #29988, #5497 ) ;
#22619=CARTESIAN_POINT ( 'NONE',  ( 10.69999999999999929, -30.00000000000000000, -28.40000000000000213 ) ) ;
#22621=CARTESIAN_POINT ( 'NONE',  ( -13.67718144140000014, 20.99999999999999645, -57.16242377749999548 ) ) ;
#22637=ORIENTED_EDGE ( 'NONE', *, *, #26070, .T. ) ;
#22640=ORIENTED_EDGE ( 'NONE', *, *, #11275, .F. ) ;
#22644=VERTEX_POINT ( 'NONE', #11721 ) ;
#22650=CYLINDRICAL_SURFACE ( 'NONE', #15090, 5.000000000000003553 ) ;
#22654=CARTESIAN_POINT ( 'NONE',  ( 10.69999999989999928, -25.00000000000000000, -2.399999999999999467 ) ) ;
#22658=DIRECTION ( 'NONE',  ( -1.000000000000000000, -1.853796481301025284E-24, -2.257144471330669991E-12 ) ) ;
#22663=LINE ( 'NONE', #1109, #1194 ) ;
#22666=VERTEX_POINT ( 'NONE', #26201 ) ;
#22670=ORIENTED_EDGE ( 'NONE', *, *, #5839, .T. ) ;
#22671=DIRECTION ( 'NONE',  ( 0.000000000000000000, -1.000000000000000000, 0.000000000000000000 ) ) ;
#22673=ORIENTED_EDGE ( 'NONE', *, *, #18352, .F. ) ;
#22677=ORIENTED_EDGE ( 'NONE', *, *, #12162, .F. ) ;
#22679=B_SPLINE_CURVE_WITH_KNOTS ( 'NONE', 3,
 ( #8258, #18009, #17854, #12527, #27615, #17401 ),
 .UNSPECIFIED., .F., .F.,
 ( 4, 2, 4 ),
 ( 0.000000000000000000, 0.5000000000000000000, 1.000000000000000000 ),
 .UNSPECIFIED. ) ;
#22683=ORIENTED_EDGE ( 'NONE', *, *, #17508, .T. ) ;
#22719=LINE ( 'NONE', #17214, #29035 ) ;
#22727=ORIENTED_EDGE ( 'NONE', *, *, #2406, .F. ) ;
#22748=CARTESIAN_POINT ( 'NONE',  ( 10.98966923329999901, -24.66097101770000322, -1.689678582800002715 ) ) ;
#22766=ORIENTED_EDGE ( 'NONE', *, *, #25159, .T. ) ;
#22786=ADVANCED_FACE ( 'NONE', ( #30259 ), #29942, .F. ) ;
#22803=FACE_OUTER_BOUND ( 'NONE', #9314, .T. ) ;
#22807=CARTESIAN_POINT ( 'NONE',  ( -10.32522729140000095, -24.79836099970000163, -1.399999999999998579 ) ) ;
#22810=VECTOR ( 'NONE', #27156, 1000.000000000000000 ) ;
#22812=LINE ( 'NONE', #1420, #9266 ) ;
#22824=CARTESIAN_POINT ( 'NONE',  ( 10.49049139470000114, 19.99999999999999645, -1.182260226300003936 ) ) ;
#22825=B_SPLINE_CURVE_WITH_KNOTS ( 'NONE', 5,
 ( #20720, #14108, #23712, #21345, #30942, #30319, #18359, #5114, #19756 ),
 .UNSPECIFIED., .F., .F.,
 ( 6, 3, 6 ),
 ( 0.000000000000000000, 2.404878242390000143, 3.338999440259999840 ),
 .UNSPECIFIED. ) ;
#22831=VERTEX_POINT ( 'NONE', #1476 ) ;
#22834=ORIENTED_EDGE ( 'NONE', *, *, #6151, .T. ) ;
#22842=B_SPLINE_CURVE_WITH_KNOTS ( 'NONE', 3,
 ( #15327, #8072, #24770, #1015 ),
 .UNSPECIFIED., .F., .F.,
 ( 4, 4 ),
 ( 0.000000000000000000, 1.000000000000000000 ),
 .UNSPECIFIED. ) ;
#22852=LINE ( 'NONE', #11200, #10329 ) ;
#22861=B_SPLINE_CURVE_WITH_KNOTS ( 'NONE', 3,
 ( #16733, #28235, #23690, #25737, #28400, #11410, #16586, #26196, #18950, #9512 ),
 .UNSPECIFIED., .F., .F.,
 ( 4, 2, 2, 2, 4 ),
 ( 0.000000000000000000, 0.2500000000000000000, 0.5000000000000000000, 0.7500000000000000000, 1.000000000000000000 ),
 .UNSPECIFIED. ) ;
#22865=AXIS2_PLACEMENT_3D ( 'NONE', #14435, #9703, #9231 ) ;
#22872=ORIENTED_EDGE ( 'NONE', *, *, #24498, .T. ) ;
#22879=VERTEX_POINT ( 'NONE', #26013 ) ;
#22882=FACE_OUTER_BOUND ( 'NONE', #5881, .T. ) ;
#22883=FACE_OUTER_BOUND ( 'NONE', #6520, .T. ) ;
#22886=CARTESIAN_POINT ( 'NONE',  ( -10.00000000045683990, -24.07808196999473438, -29.18524365307840895 ) ) ;
#22887=CARTESIAN_POINT ( 'NONE',  ( 10.06419936220000011, 19.99999999999999645, -43.74658025403999773 ) ) ;
#22901=B_SPLINE_CURVE_WITH_KNOTS ( 'NONE', 3,
 ( #13698, #28012, #6455, #3791, #1592, #28169, #25668, #18089, #11180, #30542 ),
 .UNSPECIFIED., .F., .F.,
 ( 4, 2, 2, 2, 4 ),
 ( 0.000000000000000000, 0.2500000000000000000, 0.5000000000000000000, 0.7500000000000000000, 1.000000000000000000 ),
 .UNSPECIFIED. ) ;
#22905=CARTESIAN_POINT ( 'NONE',  ( -11.30445666259999982, -24.42656469639999983, -1.476955128299997533 ) ) ;
#22906=CARTESIAN_POINT ( 'NONE',  ( 2.910383045670000247E-11, 21.70000000000000284, -60.10000000000000142 ) ) ;
#22917=DIRECTION ( 'NONE',  ( 0.000000000000000000, 1.000000000000000000, 0.000000000000000000 ) ) ;
#22920=VERTEX_POINT ( 'NONE', #28673 ) ;
#22925=EDGE_LOOP ( 'NONE', ( #25992, #12765, #6725, #13902, #2864, #23167, #20152 ) ) ;
#22939=DIRECTION ( 'NONE',  ( 0.7071067811870488384, 0.000000000000000000, 0.7071067811860461960 ) ) ;
#22943=EDGE_CURVE ( 'NONE', #5895, #5911, #9631, .T. ) ;
#22944=CARTESIAN_POINT ( 'NONE',  ( -17.28128630822742196, 12.01496581067445213, -1.400000000000002132 ) ) ;
#22947=CARTESIAN_POINT ( 'NONE',  ( -10.35000000029999967, -25.00000000000000000, -7.274962170099999348 ) ) ;
#22949=ORIENTED_EDGE ( 'NONE', *, *, #27366, .T. ) ;
#22951=ORIENTED_EDGE ( 'NONE', *, *, #26517, .T. ) ;
#22960=CARTESIAN_POINT ( 'NONE',  ( -9.872542079070584009, -130.0000000000000000, -42.90521570519508288 ) ) ;
#22972=EDGE_CURVE ( 'NONE', #3831, #15866, #19699, .T. ) ;
#22981=FACE_OUTER_BOUND ( 'NONE', #1624, .T. ) ;
#22984=CARTESIAN_POINT ( 'NONE',  ( 10.00000000020000002, 19.99999999999999645, -2.400000000399998612 ) ) ;
#22986=AXIS2_PLACEMENT_3D ( 'NONE', #2071, #30864, #14182 ) ;
#22995=ORIENTED_EDGE ( 'NONE', *, *, #7191, .F. ) ;
#23011=CARTESIAN_POINT ( 'NONE',  ( 10.99289321870000080, 19.99999999999999645, -1.692893218799999877 ) ) ;
#23012=AXIS2_PLACEMENT_3D ( 'NONE', #15983, #23701, #4496 ) ;
#23019=CARTESIAN_POINT ( 'NONE',  ( 9.999999999984520827, -128.8192055971804564, -36.36585972525736565 ) ) ;
#23020=B_SPLINE_CURVE_WITH_KNOTS ( 'NONE', 3,
 ( #17291, #14786, #29095, #24225, #482, #10064, #26898, #15093, #2667, #12263 ),
 .UNSPECIFIED., .F., .F.,
 ( 4, 2, 2, 2, 4 ),
 ( 0.000000000000000000, 0.2500000000000000000, 0.5000000000000000000, 0.7500000000000000000, 1.000000000000000000 ),
 .UNSPECIFIED. ) ;
#23032=DIRECTION ( 'NONE',  ( -1.000000000000000000, 0.000000000000000000, 0.000000000000000000 ) ) ;
#23045=ADVANCED_FACE ( 'NONE', ( #7725 ), #8031, .T. ) ;
#23048=LINE ( 'NONE', #5877, #13544 ) ;
#23052=AXIS2_PLACEMENT_3D ( 'NONE', #27788, #18022, #17866 ) ;
#23054=DIRECTION ( 'NONE',  ( -1.000000000000000000, 1.853796481301025284E-24, -2.257144471330669991E-12 ) ) ;
#23065=CARTESIAN_POINT ( 'NONE',  ( -11.14649459219999983, -24.37257237719999736, -0.7852065530999998710 ) ) ;
#23073=LINE ( 'NONE', #14405, #23825 ) ;
#23087=CARTESIAN_POINT ( 'NONE',  ( 9.999999999969999109, -82.23832021929999314, -29.25398675779999991 ) ) ;
#23090=CARTESIAN_POINT ( 'NONE',  ( -10.69999999999999929, -27.00000000000000000, -28.40000000000000213 ) ) ;
#23094=ORIENTED_EDGE ( 'NONE', *, *, #27196, .T. ) ;
#23098=CARTESIAN_POINT ( 'NONE',  ( 10.69999999930000101, -30.49251257979999963, -21.04205368479999905 ) ) ;
#23101=DIRECTION ( 'NONE',  ( 1.635844237846128888E-12, 0.6889064844488322903, 0.7248502298298253876 ) ) ;
#23102=CARTESIAN_POINT ( 'NONE',  ( -10.00000000070000183, -27.00000000000000000, -28.40000000000000213 ) ) ;
#23104=CARTESIAN_POINT ( 'NONE',  ( -17.09439379194196817, 9.921746937126174615, -1.400000000000001910 ) ) ;
#23112=LINE ( 'NONE', #16327, #27325 ) ;
#23118=VERTEX_POINT ( 'NONE', #24884 ) ;
#23122=VERTEX_POINT ( 'NONE', #27390 ) ;
#23123=ORIENTED_EDGE ( 'NONE', *, *, #28126, .T. ) ;
#23127=CARTESIAN_POINT ( 'NONE',  ( 9.000000000000000000, 19.99999999999999645, -43.39999999999999858 ) ) ;
#23136=CARTESIAN_POINT ( 'NONE',  ( 8.999999999770000869, 20.61304188753062050, -44.29887312234927066 ) ) ;
#23145=CARTESIAN_POINT ( 'NONE',  ( -11.78485145404637002, 21.69999999994150031, -70.02209366220616005 ) ) ;
#23148=PLANE ( 'NONE',  #8702 ) ;
#23156=ORIENTED_EDGE ( 'NONE', *, *, #24440, .F. ) ;
#23159=ORIENTED_EDGE ( 'NONE', *, *, #5145, .T. ) ;
#23160=CARTESIAN_POINT ( 'NONE',  ( 10.69999999997017071, -29.92227941849945694, -29.18484171379398617 ) ) ;
#23167=ORIENTED_EDGE ( 'NONE', *, *, #27627, .T. ) ;
#23170=CARTESIAN_POINT ( 'NONE',  ( 10.32522729140000095, -24.73114799960000099, -1.399999999999998579 ) ) ;
#23175=CARTESIAN_POINT ( 'NONE',  ( 9.999999999992681410, -130.0000000001073772, -39.98135229079757380 ) ) ;
#23189=ORIENTED_EDGE ( 'NONE', *, *, #16848, .F. ) ;
#23190=VERTEX_POINT ( 'NONE', #10875 ) ;
#23191=ORIENTED_EDGE ( 'NONE', *, *, #9048, .F. ) ;
#23197=DIRECTION ( 'NONE',  ( 2.257144471330000330E-12, -0.000000000000000000, -1.000000000000000000 ) ) ;
#23206=CARTESIAN_POINT ( 'NONE',  ( -10.00000000020000002, -24.91804464959999876, -26.23931466329999651 ) ) ;
#23210=ORIENTED_EDGE ( 'NONE', *, *, #5915, .F. ) ;
#23211=CARTESIAN_POINT ( 'NONE',  ( 19.41514007621238491, 18.50604284286171364, -1.399999999999998579 ) ) ;
#23216=DIRECTION ( 'NONE',  ( -0.000000000000000000, 0.000000000000000000, 1.000000000000000000 ) ) ;
#23217=CARTESIAN_POINT ( 'NONE',  ( -12.77820031340000106, 20.99999999999999645, -56.10000000020000499 ) ) ;
#23228=ORIENTED_EDGE ( 'NONE', *, *, #11988, .F. ) ;
#23237=CARTESIAN_POINT ( 'NONE',  ( -11.14649459219999983, -24.37257237719999736, -0.7852065530999998710 ) ) ;
#23257=ADVANCED_FACE ( 'NONE', ( #15735 ), #20935, .F. ) ;
#23262=PLANE ( 'NONE',  #7228 ) ;
#23264=CARTESIAN_POINT ( 'NONE',  ( 10.69999999997381757, -25.15707083535441768, -30.79962415710182810 ) ) ;
#23265=ORIENTED_EDGE ( 'NONE', *, *, #25427, .F. ) ;
#23303=EDGE_CURVE ( 'NONE', #24422, #30907, #16116, .T. ) ;
#23306=ORIENTED_EDGE ( 'NONE', *, *, #28250, .T. ) ;
#23317=CARTESIAN_POINT ( 'NONE',  ( 23.03549535077002375, -13.87410949944762351, -1.399999999999998357 ) ) ;
#23336=CARTESIAN_POINT ( 'NONE',  ( 14.76964124820000102, 19.99999999999999645, -0.6999999999999992895 ) ) ;
#23338=EDGE_LOOP ( 'NONE', ( #2116, #23559, #6072, #5567, #249, #27280, #18382, #6486 ) ) ;
#23351=VECTOR ( 'NONE', #24979, 1000.000000000000000 ) ;
#23352=ORIENTED_EDGE ( 'NONE', *, *, #9048, .T. ) ;
#23353=ORIENTED_EDGE ( 'NONE', *, *, #2867, .F. ) ;
#23379=VECTOR ( 'NONE', #10443, 1000.000000000000000 ) ;
#23380=CARTESIAN_POINT ( 'NONE',  ( -8.999999999796672867, 20.52198665876978012, -44.20777309639302644 ) ) ;
#23383=CARTESIAN_POINT ( 'NONE',  ( 10.69999999999999929, -130.0000000000000000, -42.39999999999999858 ) ) ;
#23398=CARTESIAN_POINT ( 'NONE',  ( -10.00000000045316284, -24.07808196999543782, -27.61475634692235559 ) ) ;
#23424=B_SPLINE_CURVE_WITH_KNOTS ( 'NONE', 3,
 ( #15914, #25523, #30081, #18106, #30557, #6471 ),
 .UNSPECIFIED., .F., .F.,
 ( 4, 2, 4 ),
 ( 0.000000000000000000, 0.5000000000000000000, 1.000000000000000000 ),
 .UNSPECIFIED. ) ;
#23425=B_SPLINE_CURVE_WITH_KNOTS ( 'NONE', 3,
 ( #16594, #21950, #4811, #9988, #28408, #4492 ),
 .UNSPECIFIED., .F., .F.,
 ( 4, 2, 4 ),
 ( 0.000000000000000000, 0.5000000000000000000, 1.000000000000000000 ),
 .UNSPECIFIED. ) ;
#23428=PLANE ( 'NONE',  #18813 ) ;
#23430=VERTEX_POINT ( 'NONE', #4049 ) ;
#23441=EDGE_CURVE ( 'NONE', #24111, #24088, #1704, .T. ) ;
#23449=ORIENTED_EDGE ( 'NONE', *, *, #28153, .T. ) ;
#23458=CARTESIAN_POINT ( 'NONE',  ( -10.00000000000000000, 21.70000000000000284, -64.10000000000000853 ) ) ;
#23473=ORIENTED_EDGE ( 'NONE', *, *, #15465, .F. ) ;
#23474=CARTESIAN_POINT ( 'NONE',  ( 10.69999999997181561, -29.62111648953255738, -29.91136270442498102 ) ) ;
#23478=CARTESIAN_POINT ( 'NONE',  ( -10.00000000070000183, -27.00000000000000000, -25.39999999999999858 ) ) ;
#23480=DIRECTION ( 'NONE',  ( -1.000000000000000000, 0.000000000000000000, 0.000000000000000000 ) ) ;
#23493=COLOUR_RGB ( '', 0.31764706, 0.68627451, 0.89019608) ;
#23502=EDGE_CURVE ( 'NONE', #24111, #24506, #30950, .T. ) ;
#23517=LINE ( 'NONE', #6505, #27521 ) ;
#23519=FILL_AREA_STYLE ('',( #26024 ) ) ;
#23520=VECTOR ( 'NONE', #22917, 1000.000000000000000 ) ;
#23525=EDGE_CURVE ( 'NONE', #29098, #18993, #16278, .T. ) ;
#23531=CARTESIAN_POINT ( 'NONE',  ( 23.35460918733123847, 13.32399080374418787, -1.399999999999998801 ) ) ;
#23539=ORIENTED_EDGE ( 'NONE', *, *, #5831, .F. ) ;
#23545=VECTOR ( 'NONE', #26290, 1000.000000000000000 ) ;
#23551=ADVANCED_FACE ( 'NONE', ( #29041 ), #11746, .T. ) ;
#23559=ORIENTED_EDGE ( 'NONE', *, *, #11521, .T. ) ;
#23562=DIRECTION ( 'NONE',  ( 0.7071067811865466846, -1.595945597898659700E-12, -0.7071067811865484609 ) ) ;
#23563=CARTESIAN_POINT ( 'NONE',  ( 10.69999999994010587, -26.89354272454766814, -15.86444061765503122 ) ) ;
#23571=CARTESIAN_POINT ( 'NONE',  ( 10.69999999996289652, -28.79065839761292978, -25.96313344405833234 ) ) ;
#23578=CARTESIAN_POINT ( 'NONE',  ( -16.25551851031397632, 10.05302898035984605, -1.400000000000001688 ) ) ;
#23580=VECTOR ( 'NONE', #26383, 1000.000000000000000 ) ;
#23585=CARTESIAN_POINT ( 'NONE',  ( 9.000000000000000000, -55.00000000000000000, -44.10000000000000142 ) ) ;
#23587=ORIENTED_EDGE ( 'NONE', *, *, #19830, .T. ) ;
#23589=EDGE_LOOP ( 'NONE', ( #14942, #24011, #5076, #15592 ) ) ;
#23600=CYLINDRICAL_SURFACE ( 'NONE', #9406, 26.80000000000000071 ) ;
#23603=ORIENTED_EDGE ( 'NONE', *, *, #24886, .T. ) ;
#23616=CARTESIAN_POINT ( 'NONE',  ( -11.39379051978746915, 21.69999999994131556, -70.10000000020002631 ) ) ;
#23623=CARTESIAN_POINT ( 'NONE',  ( 10.69999999999999929, -24.00000000000000000, -28.40000000000000213 ) ) ;
#23628=VERTEX_POINT ( 'NONE', #14731 ) ;
#23635=CARTESIAN_POINT ( 'NONE',  ( 26.22084555198160771, -5.650681821715154207, -1.399999999999998579 ) ) ;
#23636=CARTESIAN_POINT ( 'NONE',  ( -4.175165894169885483, -50.49316738903675628, -43.39999999999999858 ) ) ;
#23643=DIRECTION ( 'NONE',  ( -1.000000000000000000, 0.000000000000000000, 0.000000000000000000 ) ) ;
#23646=ADVANCED_FACE ( 'NONE', ( #10009 ), #19607, .T. ) ;
#23649=APPLICATION_CONTEXT ( 'automotive_design' ) ;
#23672=CARTESIAN_POINT ( 'NONE',  ( 9.999999999959999997, -36.62914859500000375, -26.86371135770000151 ) ) ;
#23683=CARTESIAN_POINT ( 'NONE',  ( 26.80813537125358081, 0.8641279371233817619, -1.399999999999998579 ) ) ;
#23684=CARTESIAN_POINT ( 'NONE',  ( -10.69999999999999929, -129.8920065082999997, -39.38774058400999678 ) ) ;
#23685=DIRECTION ( 'NONE',  ( -1.000000000000000000, 0.000000000000000000, 0.000000000000000000 ) ) ;
#23686=CARTESIAN_POINT ( 'NONE',  ( 11.02573875750000099, -24.63456739829999975, -1.660048601699999571 ) ) ;
#23690=CARTESIAN_POINT ( 'NONE',  ( 10.69999999997514095, -121.7823864053157195, -31.38636738194435694 ) ) ;
#23692=CARTESIAN_POINT ( 'NONE',  ( 17.16657240410000185, 10.99999999889999458, -0.6999999999999992895 ) ) ;
#23696=CARTESIAN_POINT ( 'NONE',  ( 10.00000000060000005, -25.00000000000000000, -7.274962170899998526 ) ) ;
#23701=DIRECTION ( 'NONE',  ( 0.000000000000000000, 0.000000000000000000, 1.000000000000000000 ) ) ;
#23703=EDGE_LOOP ( 'NONE', ( #17022, #1062 ) ) ;
#23712=CARTESIAN_POINT ( 'NONE',  ( -10.69999999999999929, -24.04799545849999731, -27.72121045900000169 ) ) ;
#23714=CARTESIAN_POINT ( 'NONE',  ( -9.000000000229999131, 21.70000000000000284, -58.10000000000000142 ) ) ;
#23725=AXIS2_PLACEMENT_3D ( 'NONE', #28289, #9090, #25942 ) ;
#23727=CIRCLE ( 'NONE', #11153, 0.9999999999999991118 ) ;
#23728=DIRECTION ( 'NONE',  ( 0.000000000000000000, -1.000000000000000000, 0.000000000000000000 ) ) ;
#23735=FACE_OUTER_BOUND ( 'NONE', #30039, .T. ) ;
#23741=AXIS2_PLACEMENT_3D ( 'NONE', #27188, #29702, #19649 ) ;
#23743=CARTESIAN_POINT ( 'NONE',  ( -10.00000000070000183, -27.00000000000000000, -28.40000000000000213 ) ) ;
#23766=CARTESIAN_POINT ( 'NONE',  ( -10.69999999989999928, -25.00000000000000000, -4.837481085799996805 ) ) ;
#23771=CARTESIAN_POINT ( 'NONE',  ( 10.91239719759999893, 19.99999999999999645, -1.779565482400005560 ) ) ;
#23774=CARTESIAN_POINT ( 'NONE',  ( -10.00000000045946713, -129.7569854617604506, -38.71642352146631794 ) ) ;
#23776=ORIENTED_EDGE ( 'NONE', *, *, #24892, .T. ) ;
#23781=VECTOR ( 'NONE', #18985, 1000.000000000000000 ) ;
#23787=DIRECTION ( 'NONE',  ( 0.000000000000000000, -1.000000000000000000, 0.000000000000000000 ) ) ;
#23798=AXIS2_PLACEMENT_3D ( 'NONE', #30044, #17614, #5818 ) ;
#23800=CARTESIAN_POINT ( 'NONE',  ( -10.99999999969999998, 21.69999999919999212, -70.09999999999999432 ) ) ;
#23802=CARTESIAN_POINT ( 'NONE',  ( -20.44987259205819896, -17.46217831278680421, -1.399999999999998579 ) ) ;
#23803=VERTEX_POINT ( 'NONE', #10328 ) ;
#23804=VECTOR ( 'NONE', #30990, 1000.000000000000000 ) ;
#23806=CARTESIAN_POINT ( 'NONE',  ( 0.000000000000000000, -50.49316738903675628, -63.39999999999999858 ) ) ;
#23814=ORIENTED_EDGE ( 'NONE', *, *, #28875, .T. ) ;
#23824=CYLINDRICAL_SURFACE ( 'NONE', #17424, 3.000000000000003997 ) ;
#23825=VECTOR ( 'NONE', #28863, 1000.000000000000000 ) ;
#23831=CARTESIAN_POINT ( 'NONE',  ( -20.89763770104046259, 16.92004971534728597, -1.399999999999998579 ) ) ;
#23834=ORIENTED_EDGE ( 'NONE', *, *, #21668, .T. ) ;
#23838=CARTESIAN_POINT ( 'NONE',  ( 11.62710820729999917, -24.17108566339999953, -1.401657795999995626 ) ) ;
#23851=CARTESIAN_POINT ( 'NONE',  ( -9.000000000000000000, -130.0000000000000000, -42.39999999999999858 ) ) ;
#23852=EDGE_CURVE ( 'NONE', #19721, #1607, #587, .T. ) ;
#23857=VERTEX_POINT ( 'NONE', #15049 ) ;
#23864=CARTESIAN_POINT ( 'NONE',  ( -10.69999999999999929, -27.00000000000000000, -25.39999999999999858 ) ) ;
#23865=EDGE_CURVE ( 'NONE', #27171, #1470, #9857, .T. ) ;
#23887=EDGE_CURVE ( 'NONE', #29453, #5618, #27452, .T. ) ;
#23889=LINE ( 'NONE', #7189, #13813 ) ;
#23901=VERTEX_POINT ( 'NONE', #29813 ) ;
#23908=CARTESIAN_POINT ( 'NONE',  ( 9.439621097969999042, 19.99999999999999645, -43.30705920210200333 ) ) ;
#23914=VERTEX_POINT ( 'NONE', #11101 ) ;
#23919=CARTESIAN_POINT ( 'NONE',  ( -10.32522729140000095, -25.00000000000000000, -1.399999999999998579 ) ) ;
#23921=CARTESIAN_POINT ( 'NONE',  ( 11.69999999989999928, -2.500000000000002220, -2.399999999999999467 ) ) ;
#23932=DIRECTION ( 'NONE',  ( 1.000000000000000000, 5.998481157687279274E-24, -2.257150022441830001E-12 ) ) ;
#23951=CARTESIAN_POINT ( 'NONE',  ( -8.999999999970000886, 20.99999999999999645, -45.10000000000000142 ) ) ;
#23960=CARTESIAN_POINT ( 'NONE',  ( 17.33810066013692719, 9.903956624692348498, -1.400000000000001910 ) ) ;
#23961=DIRECTION ( 'NONE',  ( -1.000000000000000000, 0.000000000000000000, 0.000000000000000000 ) ) ;
#23965=LINE ( 'NONE', #7573, #4267 ) ;
#23977=DIRECTION ( 'NONE',  ( -1.000000000000000000, 0.000000000000000000, 0.000000000000000000 ) ) ;
#23983=CARTESIAN_POINT ( 'NONE',  ( -23.35903771415276609, 13.31654055986141572, -1.399999999999998357 ) ) ;
#23984=AXIS2_PLACEMENT_3D ( 'NONE', #28719, #22260, #2906 ) ;
#23993=CARTESIAN_POINT ( 'NONE',  ( 4.175165894169885483, -50.49316738903675628, -43.39999999999999858 ) ) ;
#23998=ORIENTED_EDGE ( 'NONE', *, *, #18493, .T. ) ;
#24005=ADVANCED_FACE ( 'NONE', ( #3859 ), #15500, .T. ) ;
#24011=ORIENTED_EDGE ( 'NONE', *, *, #11988, .T. ) ;
#24019=PLANE ( 'NONE',  #22063 ) ;
#24029=AXIS2_PLACEMENT_3D ( 'NONE', #28491, #4424, #26141 ) ;
#24033=LINE ( 'NONE', #7498, #24370 ) ;
#24055=CARTESIAN_POINT ( 'NONE',  ( 17.14121550692227558, 12.10909424797362455, -1.400000000000002132 ) ) ;
#24063=EDGE_CURVE ( 'NONE', #1319, #145, #22861, .T. ) ;
#24067=CARTESIAN_POINT ( 'NONE',  ( -11.69999999989999928, -25.00000000000000000, -2.399999999999999467 ) ) ;
#24070=CARTESIAN_POINT ( 'NONE',  ( 10.69999999999842366, -26.27037943368971540, -25.46729144948177748 ) ) ;
#24072=DIRECTION ( 'NONE',  ( -2.256992747040000044E-12, 0.000000000000000000, -1.000000000000000000 ) ) ;
#24080=CARTESIAN_POINT ( 'NONE',  ( 9.999999999979998222, -27.00000000000000000, -31.39999999999999858 ) ) ;
#24088=VERTEX_POINT ( 'NONE', #19110 ) ;
#24096=AXIS2_PLACEMENT_3D ( 'NONE', #8347, #20016, #22388 ) ;
#24111=VERTEX_POINT ( 'NONE', #13612 ) ;
#24123=CARTESIAN_POINT ( 'NONE',  ( 10.00000000070000183, -27.00000000000000000, -25.39999999999999858 ) ) ;
#24126=ORIENTED_EDGE ( 'NONE', *, *, #7930, .T. ) ;
#24140=DIRECTION ( 'NONE',  ( -0.000000000000000000, 1.000000000000000000, -0.000000000000000000 ) ) ;
#24146=DIRECTION ( 'NONE',  ( 0.000000000000000000, 0.000000000000000000, 1.000000000000000000 ) ) ;
#24174=CYLINDRICAL_SURFACE ( 'NONE', #30741, 20.00000000000000711 ) ;
#24176=CARTESIAN_POINT ( 'NONE',  ( 8.999999999540001738, 19.99999999999999645, -44.09999999970998630 ) ) ;
#24180=DIRECTION ( 'NONE',  ( -1.000000000000000000, 0.000000000000000000, 0.000000000000000000 ) ) ;
#24182=CARTESIAN_POINT ( 'NONE',  ( 9.999984944298805800, 21.69999999997726903, -54.17105275116254148 ) ) ;
#24198=ADVANCED_FACE ( 'NONE', ( #11568 ), #5250, .T. ) ;
#24201=LINE ( 'NONE', #28758, #30539 ) ;
#24205=CARTESIAN_POINT ( 'NONE',  ( 13.15714562406650501, 20.99999999997228528, -56.37888616265984609 ) ) ;
#24207=EDGE_CURVE ( 'NONE', #10804, #5944, #29197, .T. ) ;
#24214=CARTESIAN_POINT ( 'NONE',  ( -10.69999999999999929, -127.0192926649000071, -34.11611703194000000 ) ) ;
#24220=AXIS2_PLACEMENT_3D ( 'NONE', #2653, #24373, #14469 ) ;
#24223=CARTESIAN_POINT ( 'NONE',  ( 9.999999999971848297, -123.0374659623223010, -31.63552742122224259 ) ) ;
#24225=CARTESIAN_POINT ( 'NONE',  ( -10.00000000045272763, -38.97546878308436646, -26.38794647281848427 ) ) ;
#24230=EDGE_LOOP ( 'NONE', ( #2302, #20372, #24393, #29641 ) ) ;
#24251=CARTESIAN_POINT ( 'NONE',  ( -3.510330246760000161, -1.917702155200005976, -44.10000000000000142 ) ) ;
#24257=CARTESIAN_POINT ( 'NONE',  ( 10.69999999999583729, -24.60099947294593292, -26.55635983988242188 ) ) ;
#24262=VERTEX_POINT ( 'NONE', #29160 ) ;
#24264=VERTEX_POINT ( 'NONE', #26500 ) ;
#24266=ORIENTED_EDGE ( 'NONE', *, *, #31101, .F. ) ;
#24277=LINE ( 'NONE', #2725, #29547 ) ;
#24286=DIRECTION ( 'NONE',  ( 1.000000000000000000, 0.000000000000000000, 0.000000000000000000 ) ) ;
#24297=CARTESIAN_POINT ( 'NONE',  ( 9.999999999922765781, -25.00000000003785061, -8.540325879148895183 ) ) ;
#24314=DIRECTION ( 'NONE',  ( 0.000000000000000000, 1.000000000000000000, 0.000000000000000000 ) ) ;
#24315=EDGE_CURVE ( 'NONE', #20583, #26453, #11928, .T. ) ;
#24317=EDGE_CURVE ( 'NONE', #19402, #11684, #27569, .T. ) ;
#24335=DIRECTION ( 'NONE',  ( 0.000000000000000000, 0.000000000000000000, -1.000000000000000000 ) ) ;
#24336=CARTESIAN_POINT ( 'NONE',  ( -17.83928249680000278, 19.99999999999999645, -0.6999999999999992895 ) ) ;
#24337=B_SPLINE_CURVE_WITH_KNOTS ( 'NONE', 3,
 ( #16799, #14760, #24358, #26412, #14456, #17263, #24055, #26870, #5313, #14917, #24512, #12543, #20103, #1371, #8426, #18025, #17570, #27792 ),
 .UNSPECIFIED., .F., .F.,
 ( 4, 2, 2, 2, 2, 2, 2, 2, 4 ),
 ( 0.000000000000000000, 0.1250000000000000000, 0.2500000000000000000, 0.3750000000000000000, 0.5000000000000000000, 0.6250000000000000000, 0.7500000000000000000, 0.8750000000000000000, 1.000000000000000000 ),
 .UNSPECIFIED. ) ;
#24348=VERTEX_POINT ( 'NONE', #25220 ) ;
#24351=AXIS2_PLACEMENT_3D ( 'NONE', #5051, #7106, #17155 ) ;
#24352=ORIENTED_EDGE ( 'NONE', *, *, #24664, .F. ) ;
#24354=ORIENTED_EDGE ( 'NONE', *, *, #16389, .T. ) ;
#24358=CARTESIAN_POINT ( 'NONE',  ( 16.36439430656247040, 11.76631802980117669, -1.400000000000001910 ) ) ;
#24362=LINE ( 'NONE', #29223, #11499 ) ;
#24370=VECTOR ( 'NONE', #21363, 1000.000000000000000 ) ;
#24373=DIRECTION ( 'NONE',  ( 0.000000000000000000, 0.000000000000000000, -1.000000000000000000 ) ) ;
#24375=PLANE ( 'NONE',  #4182 ) ;
#24387=CARTESIAN_POINT ( 'NONE',  ( 9.999999999971805664, -26.21475634739274696, -31.32191803010133668 ) ) ;
#24390=ADVANCED_FACE ( 'NONE', ( #30251 ), #20033, .F. ) ;
#24393=ORIENTED_EDGE ( 'NONE', *, *, #1449, .T. ) ;
#24395=ORIENTED_EDGE ( 'NONE', *, *, #15863, .T. ) ;
#24411=FACE_OUTER_BOUND ( 'NONE', #10806, .T. ) ;
#24422=VERTEX_POINT ( 'NONE', #17808 ) ;
#24424=CARTESIAN_POINT ( 'NONE',  ( 17.16657240410000185, -9.000000001100003644, -1.399999999999998579 ) ) ;
#24429=ORIENTED_EDGE ( 'NONE', *, *, #15918, .F. ) ;
#24435=VERTEX_POINT ( 'NONE', #26004 ) ;
#24439=DIRECTION ( 'NONE',  ( 0.000000000000000000, -1.000000000000000000, 0.000000000000000000 ) ) ;
#24440=EDGE_CURVE ( 'NONE', #28644, #23122, #10290, .T. ) ;
#24443=CARTESIAN_POINT ( 'NONE',  ( -10.69999999989999928, -25.00000000000000000, -7.274962171499997687 ) ) ;
#24455=ORIENTED_EDGE ( 'NONE', *, *, #20579, .T. ) ;
#24462=B_SPLINE_CURVE_WITH_KNOTS ( 'NONE', 3,
 ( #15211, #27326, #5765, #10345, #24659, #12856 ),
 .UNSPECIFIED., .F., .F.,
 ( 4, 2, 4 ),
 ( 0.000000000000000000, 0.5000000000000008882, 1.000000000000000000 ),
 .UNSPECIFIED. ) ;
#24468=CARTESIAN_POINT ( 'NONE',  ( -10.00000000009909407, -126.3827248090510835, -33.44530783418806408 ) ) ;
#24475=CARTESIAN_POINT ( 'NONE',  ( -15.86808677770000209, 10.47263190749999495, -1.399999999599998990 ) ) ;
#24495=EDGE_LOOP ( 'NONE', ( #10602, #18926, #6346, #7571 ) ) ;
#24498=EDGE_CURVE ( 'NONE', #9514, #5024, #17162, .T. ) ;
#24501=ORIENTED_EDGE ( 'NONE', *, *, #5145, .F. ) ;
#24505=DIRECTION ( 'NONE',  ( -0.000000000000000000, 1.000000000000000000, -2.258510841069999963E-12 ) ) ;
#24506=VERTEX_POINT ( 'NONE', #30723 ) ;
#24512=CARTESIAN_POINT ( 'NONE',  ( 17.93289043380325154, 11.80217809782661398, -1.400000000000001910 ) ) ;
#24532=EDGE_CURVE ( 'NONE', #15209, #3166, #9150, .T. ) ;
#24546=ORIENTED_EDGE ( 'NONE', *, *, #6052, .F. ) ;
#24547=CARTESIAN_POINT ( 'NONE',  ( -12.51085694169142926, 20.99999999990085087, -69.72135916458235272 ) ) ;
#24561=AXIS2_PLACEMENT_3D ( 'NONE', #16035, #20442, #11009 ) ;
#24562=DIRECTION ( 'NONE',  ( 0.000000000000000000, 0.000000000000000000, 1.000000000000000000 ) ) ;
#24567=EDGE_CURVE ( 'NONE', #20670, #20967, #12644, .T. ) ;
#24570=CARTESIAN_POINT ( 'NONE',  ( -3.510330247570000228, -1.917702154400000136, -43.40000000037299799 ) ) ;
#24576=ORIENTED_EDGE ( 'NONE', *, *, #18279, .F. ) ;
#24586=DIRECTION ( 'NONE',  ( 0.000000000000000000, -1.000000000000000000, 0.000000000000000000 ) ) ;
#24593=CARTESIAN_POINT ( 'NONE',  ( -10.70000000000073470, -25.58868802739137038, -25.72767439687939728 ) ) ;
#24599=CARTESIAN_POINT ( 'NONE',  ( 10.69999999999999929, -25.00000000000000000, -26.16393202249999916 ) ) ;
#24602=DIRECTION ( 'NONE',  ( -2.966217977826874882E-25, -1.000000000000000000, 2.257145581549900232E-12 ) ) ;
#24608=VERTEX_POINT ( 'NONE', #14513 ) ;
#24616=ORIENTED_EDGE ( 'NONE', *, *, #24982, .F. ) ;
#24642=CARTESIAN_POINT ( 'NONE',  ( -10.69999999999999929, -29.12132034360000077, -30.52132034359999935 ) ) ;
#24654=ORIENTED_EDGE ( 'NONE', *, *, #26517, .F. ) ;
#24655=ORIENTED_EDGE ( 'NONE', *, *, #24317, .T. ) ;
#24659=CARTESIAN_POINT ( 'NONE',  ( 9.999999999978641085, -28.84364016088975546, -30.79900052649311348 ) ) ;
#24664=EDGE_CURVE ( 'NONE', #15209, #18136, #12297, .T. ) ;
#24679=CARTESIAN_POINT ( 'NONE',  ( -9.499999999560001740, 21.70000000000000284, -60.10000000000000142 ) ) ;
#24686=ORIENTED_EDGE ( 'NONE', *, *, #30446, .T. ) ;
#24698=CARTESIAN_POINT ( 'NONE',  ( 10.69999999999999929, -25.00000000000000000, -26.16393202249999916 ) ) ;
#24703=CARTESIAN_POINT ( 'NONE',  ( -10.69999999989999928, -30.49251257979999963, -21.04205368470000082 ) ) ;
#24722=CARTESIAN_POINT ( 'NONE',  ( 11.54917764160000004, 19.99999999999999645, -0.6999999992999966780 ) ) ;
#24728=ORIENTED_EDGE ( 'NONE', *, *, #14280, .T. ) ;
#24730=ORIENTED_EDGE ( 'NONE', *, *, #5915, .T. ) ;
#24732=VECTOR ( 'NONE', #19630, 1000.000000000000000 ) ;
#24733=CIRCLE ( 'NONE', #19211, 0.9999999999999991118 ) ;
#24740=B_SPLINE_CURVE_WITH_KNOTS ( 'NONE', 3,
 ( #5237, #9538, #14265, #19135, #17349, #28581 ),
 .UNSPECIFIED., .F., .F.,
 ( 4, 2, 4 ),
 ( 0.000000000000000000, 0.5000000000000000000, 1.000000000000000000 ),
 .UNSPECIFIED. ) ;
#24754=CARTESIAN_POINT ( 'NONE',  ( -10.69999999999999929, -26.66060153629999974, -31.39999999999999858 ) ) ;
#24764=EDGE_LOOP ( 'NONE', ( #22683, #5642, #3433, #20687 ) ) ;
#24770=CARTESIAN_POINT ( 'NONE',  ( -10.93705068780284684, 21.00000000000141753, -55.10811849999506506 ) ) ;
#24772=ORIENTED_EDGE ( 'NONE', *, *, #6620, .T. ) ;
#24777=CARTESIAN_POINT ( 'NONE',  ( 8.999999999540001738, 19.99999999999999645, -44.09999999970998630 ) ) ;
#24780=CARTESIAN_POINT ( 'NONE',  ( 8.999999999770000869, 21.70000000000000284, -48.10000000000000142 ) ) ;
#24807=EDGE_LOOP ( 'NONE', ( #20094, #2364, #14839, #641 ) ) ;
#24814=PLANE ( 'NONE',  #2501 ) ;
#24815=AXIS2_PLACEMENT_3D ( 'NONE', #12756, #663, #7572 ) ;
#24841=VECTOR ( 'NONE', #18825, 1000.000000000000000 ) ;
#24846=EDGE_CURVE ( 'NONE', #3911, #26986, #18715, .T. ) ;
#24851=ORIENTED_EDGE ( 'NONE', *, *, #2083, .F. ) ;
#24856=CARTESIAN_POINT ( 'NONE',  ( -12.84364016057614855, 20.99999999990135535, -69.49900052649185511 ) ) ;
#24860=CYLINDRICAL_SURFACE ( 'NONE', #5408, 3.000000000000003997 ) ;
#24864=CARTESIAN_POINT ( 'NONE',  ( 10.69999999999999929, -30.49251257979999963, -21.04205368479999905 ) ) ;
#24865=AXIS2_PLACEMENT_3D ( 'NONE', #28629, #5020, #9588 ) ;
#24884=CARTESIAN_POINT ( 'NONE',  ( -9.000000000229999131, 21.70000000000000284, -56.09999999999999432 ) ) ;
#24886=EDGE_CURVE ( 'NONE', #1366, #20223, #28313, .T. ) ;
#24892=EDGE_CURVE ( 'NONE', #25954, #68, #4022, .T. ) ;
#24915=DIRECTION ( 'NONE',  ( 0.000000000000000000, -2.257145581549999994E-12, -1.000000000000000000 ) ) ;
#24933=CARTESIAN_POINT ( 'NONE',  ( 1.110223024630000146E-16, 0.000000000000000000, -43.39999999999999858 ) ) ;
#24935=CARTESIAN_POINT ( 'NONE',  ( -10.00000000050000004, -24.95850565390000142, -26.20104569390000293 ) ) ;
#24944=DIRECTION ( 'NONE',  ( 0.8086898285215826654, 0.000000000000000000, 0.5882352941176968164 ) ) ;
#24946=CARTESIAN_POINT ( 'NONE',  ( -12.57906051704346595, 20.99999999997321964, -55.96254875484549984 ) ) ;
#24952=B_SPLINE_CURVE_WITH_KNOTS ( 'NONE', 3,
 ( #12898, #17909, #3443, #18067, #10544, #20756 ),
 .UNSPECIFIED., .F., .F.,
 ( 4, 2, 4 ),
 ( 0.000000000000000000, 0.5000000000000000000, 1.000000000000000000 ),
 .UNSPECIFIED. ) ;
#24959=CARTESIAN_POINT ( 'NONE',  ( -17.79876841389999598, 11.52736809249999617, -0.7000000003999986564 ) ) ;
#24962=ORIENTED_EDGE ( 'NONE', *, *, #7521, .T. ) ;
#24965=ADVANCED_FACE ( 'NONE', ( #22981 ), #7380, .F. ) ;
#24966=CARTESIAN_POINT ( 'NONE',  ( -11.51892196954422154, 21.69999999997437712, -55.45368347834880041 ) ) ;
#24971=DIRECTION ( 'NONE',  ( 1.595945597898660305E-12, 0.7071067811865475727, -0.7071067811865475727 ) ) ;
#24979=DIRECTION ( 'NONE',  ( 0.000000000000000000, 1.000000000000000000, 9.516197338740001367E-15 ) ) ;
#24980=PLANE ( 'NONE',  #23741 ) ;
#24982=EDGE_CURVE ( 'NONE', #409, #2487, #16659, .T. ) ;
#24992=EDGE_CURVE ( 'NONE', #2860, #13706, #4558, .T. ) ;
#24998=EDGE_CURVE ( 'NONE', #26453, #5171, #9899, .T. ) ;
#25001=VERTEX_POINT ( 'NONE', #9736 ) ;
#25015=AXIS2_PLACEMENT_3D ( 'NONE', #29951, #30271, #20987 ) ;
#25023=B_SPLINE_CURVE_WITH_KNOTS ( 'NONE', 3,
 ( #5156, #14768, #468, #920 ),
 .UNSPECIFIED., .F., .F.,
 ( 4, 4 ),
 ( 0.000000000000000000, 1.000000000000000000 ),
 .UNSPECIFIED. ) ;
#25039=ORIENTED_EDGE ( 'NONE', *, *, #27899, .T. ) ;
#25048=CARTESIAN_POINT ( 'NONE',  ( -2.299991308520000465E-10, 20.99999999990000887, -70.09999999999999432 ) ) ;
#25075=ORIENTED_EDGE ( 'NONE', *, *, #12881, .T. ) ;
#25076=ORIENTED_EDGE ( 'NONE', *, *, #11422, .F. ) ;
#25080=B_SPLINE_CURVE_WITH_KNOTS ( 'NONE', 5,
 ( #20714, #30151, #7696, #19972, #1527, #23237, #8743, #10075, #791, #30313, #19670, #22496 ),
 .UNSPECIFIED., .F., .F.,
 ( 6, 3, 3, 6 ),
 ( -1.429360140840000071, -1.143488112680000057, -0.5717440563379999618, 2.220446049250313081E-16 ),
 .UNSPECIFIED. ) ;
#25083=DIRECTION ( 'NONE',  ( 1.000000000000000000, -0.000000000000000000, -2.257150022439999944E-12 ) ) ;
#25087=CARTESIAN_POINT ( 'NONE',  ( 9.775610180800001103, 19.99999999999999645, -43.93713984030800646 ) ) ;
#25090=ORIENTED_EDGE ( 'NONE', *, *, #6413, .F. ) ;
#25112=CARTESIAN_POINT ( 'NONE',  ( 11.14649462760000098, -24.37257236010000128, -0.7852065437999946607 ) ) ;
#25113=AXIS2_PLACEMENT_3D ( 'NONE', #4348, #18655, #28255 ) ;
#25114=CARTESIAN_POINT ( 'NONE',  ( -10.32522729140000095, -24.73114799960000099, -1.399999999999998579 ) ) ;
#25134=DIRECTION ( 'NONE',  ( 0.000000000000000000, 0.000000000000000000, 1.000000000000000000 ) ) ;
#25143=CARTESIAN_POINT ( 'NONE',  ( -4.175165894169885483, -50.49316738903675628, -43.39999999999999858 ) ) ;
#25147=B_SPLINE_CURVE_WITH_KNOTS ( 'NONE', 5,
 ( #6371, #23686, #20858, #18635, #1818, #4482, #28549, #25734, #11407, #23838, #21009, #13926 ),
 .UNSPECIFIED., .F., .F.,
 ( 6, 3, 3, 6 ),
 ( 0.2292465732300000003, 0.5717440563929999664, 1.143488112780000066, 1.429360140980000082 ),
 .UNSPECIFIED. ) ;
#25159=EDGE_CURVE ( 'NONE', #22644, #15738, #8118, .T. ) ;
#25160=FACE_OUTER_BOUND ( 'NONE', #328, .T. ) ;
#25171=DIRECTION ( 'NONE',  ( 2.257102469710000208E-12, 0.000000000000000000, 1.000000000000000000 ) ) ;
#25172=ADVANCED_FACE ( 'NONE', ( #19957 ), #15085, .F. ) ;
#25176=DIRECTION ( 'NONE',  ( -1.000000000000000000, 0.000000000000000000, 0.000000000000000000 ) ) ;
#25185=ORIENTED_EDGE ( 'NONE', *, *, #23525, .T. ) ;
#25187=DIRECTION ( 'NONE',  ( 1.000000000000000000, 0.000000000000000000, -2.257150022439999944E-12 ) ) ;
#25188=VERTEX_POINT ( 'NONE', #8134 ) ;
#25192=SURFACE_STYLE_FILL_AREA ( #30222 ) ;
#25204=AXIS2_PLACEMENT_3D ( 'NONE', #30494, #1848, #23101 ) ;
#25208=B_SPLINE_CURVE_WITH_KNOTS ( 'NONE', 1,
 ( #26840, #2775 ),
 .UNSPECIFIED., .F., .F.,
 ( 2, 2 ),
 ( -0.7000000000009999335, 0.002002273473630022949 ),
 .UNSPECIFIED. ) ;
#25210=VECTOR ( 'NONE', #24586, 1000.000000000000000 ) ;
#25220=CARTESIAN_POINT ( 'NONE',  ( 13.67718073920000066, 20.99999999999999645, -57.16242423349999768 ) ) ;
#25221=ORIENTED_EDGE ( 'NONE', *, *, #7083, .T. ) ;
#25228=SHAPE_REPRESENTATION ( 'Handle Housing', ( #17722 ), #10330 ) ;
#25232=ORIENTED_EDGE ( 'NONE', *, *, #17499, .F. ) ;
#25234=CARTESIAN_POINT ( 'NONE',  ( 9.999999999919999993, -25.00000000000000000, -4.837481085799996805 ) ) ;
#25241=CARTESIAN_POINT ( 'NONE',  ( -10.69999999999960494, -29.15099216419329053, -26.30554312108708714 ) ) ;
#25261=CARTESIAN_POINT ( 'NONE',  ( -11.48163258379999974, -24.28840542069999842, -1.419991652300001128 ) ) ;
#25280=EDGE_CURVE ( 'NONE', #20223, #23118, #13970, .T. ) ;
#25299=CARTESIAN_POINT ( 'NONE',  ( 9.999999999973411491, -24.37864083538289250, -29.91085694194880773 ) ) ;
#25300=CARTESIAN_POINT ( 'NONE',  ( -17.86780073576266759, 11.40100527483982873, -1.400000000000001910 ) ) ;
#25312=AXIS2_PLACEMENT_3D ( 'NONE', #28007, #16052, #4093 ) ;
#25320=CARTESIAN_POINT ( 'NONE',  ( -10.00000000000000000, -130.0000000000000000, -42.39999999999999858 ) ) ;
#25336=CARTESIAN_POINT ( 'NONE',  ( 4.175165894169885483, -119.7166638525666826, -63.39999999999999858 ) ) ;
#25337=AXIS2_PLACEMENT_3D ( 'NONE', #23806, #13893, #21439 ) ;
#25352=ORIENTED_EDGE ( 'NONE', *, *, #7842, .F. ) ;
#25358=VECTOR ( 'NONE', #30208, 1000.000000000000000 ) ;
#25364=VECTOR ( 'NONE', #24140, 1000.000000000000000 ) ;
#25369=EDGE_CURVE ( 'NONE', #3826, #1366, #23889, .T. ) ;
#25375=VECTOR ( 'NONE', #7210, 1000.000000000000000 ) ;
#25390=ADVANCED_FACE ( 'NONE', ( #4838 ), #14595, .F. ) ;
#25396=CARTESIAN_POINT ( 'NONE',  ( 10.95110162350000138, 19.99999999999999645, -1.734685620000002482 ) ) ;
#25399=CARTESIAN_POINT ( 'NONE',  ( -10.69999999999999929, -120.0000000000000000, -41.24671599700000257 ) ) ;
#25405=EDGE_CURVE ( 'NONE', #1319, #7041, #24033, .T. ) ;
#25413=CARTESIAN_POINT ( 'NONE',  ( -10.00000000070000183, -25.00000000000000000, -26.16393202249999916 ) ) ;
#25417=FACE_OUTER_BOUND ( 'NONE', #18570, .T. ) ;
#25421=DIRECTION ( 'NONE',  ( -1.635844237846128888E-12, 0.6889064844488322903, -0.7248502298298253876 ) ) ;
#25427=EDGE_CURVE ( 'NONE', #21489, #24348, #21238, .T. ) ;
#25443=ORIENTED_EDGE ( 'NONE', *, *, #27977, .T. ) ;
#25469=CARTESIAN_POINT ( 'NONE',  ( -4.175165894169885483, -50.49316738903675628, -63.39999999999999858 ) ) ;
#25476=ORIENTED_EDGE ( 'NONE', *, *, #31079, .T. ) ;
#25480=CARTESIAN_POINT ( 'NONE',  ( -9.999999999539999962, -130.0000000000000000, -42.53299740480396451 ) ) ;
#25488=DIRECTION ( 'NONE',  ( 0.8086898285215826654, 0.000000000000000000, 0.5882352941176968164 ) ) ;
#25491=CARTESIAN_POINT ( 'NONE',  ( -13.88844840186909302, 21.69999999999906137, -57.58021927548519869 ) ) ;
#25492=LINE ( 'NONE', #4086, #15817 ) ;
#25514=PRODUCT_CONTEXT ( 'NONE', #23649, 'mechanical' ) ;
#25517=EDGE_LOOP ( 'NONE', ( #7437, #29750, #24354, #6580 ) ) ;
#25522=CARTESIAN_POINT ( 'NONE',  ( 25.66636617707885648, -7.791308912181349022, -1.399999999999998357 ) ) ;
#25523=CARTESIAN_POINT ( 'NONE',  ( -10.69999999996928963, -30.00000000000001066, -28.79379052075074696 ) ) ;
#25532=CARTESIAN_POINT ( 'NONE',  ( -9.000000000229999131, 20.99999999999999645, -51.10000000000000142 ) ) ;
#25539=CARTESIAN_POINT ( 'NONE',  ( -9.999999999919999993, -25.00000000000000000, -7.274962171499997687 ) ) ;
#25544=AXIS2_PLACEMENT_3D ( 'NONE', #12891, #22498, #13186 ) ;
#25562=CYLINDRICAL_SURFACE ( 'NONE', #22585, 0.9999999999999988898 ) ;
#25566=CARTESIAN_POINT ( 'NONE',  ( -26.87465790466033155, 0.8603305708294651799, -1.399999999999998579 ) ) ;
#25572=CARTESIAN_POINT ( 'NONE',  ( 17.83928249680000278, 19.99999999999999645, -1.399999999299995856 ) ) ;
#25579=CARTESIAN_POINT ( 'NONE',  ( 10.46457122910000059, 21.70000000000000284, -54.63542873130000288 ) ) ;
#25582=EDGE_CURVE ( 'NONE', #30054, #14645, #23965, .T. ) ;
#25597=DIRECTION ( 'NONE',  ( 0.000000000000000000, -1.000000000000000000, 0.000000000000000000 ) ) ;
#25606=CARTESIAN_POINT ( 'NONE',  ( -10.99999999969999998, 20.99999999999999645, -58.51619611000000276 ) ) ;
#25615=EDGE_CURVE ( 'NONE', #1750, #28717, #19002, .T. ) ;
#25616=CARTESIAN_POINT ( 'NONE',  ( -10.69999999989999928, -2.500000000000002220, -2.399999999999999467 ) ) ;
#25622=CARTESIAN_POINT ( 'NONE',  ( -17.91168065875913129, 11.26096619578952129, -1.400000000000001910 ) ) ;
#25626=EDGE_CURVE ( 'NONE', #19996, #28636, #3609, .T. ) ;
#25639=ORIENTED_EDGE ( 'NONE', *, *, #23865, .F. ) ;
#25645=EDGE_CURVE ( 'NONE', #9489, #10599, #4751, .T. ) ;
#25655=CARTESIAN_POINT ( 'NONE',  ( 10.69999999930000101, -127.2537437101000108, -34.36317024011000143 ) ) ;
#25661=AXIS2_PLACEMENT_3D ( 'NONE', #11005, #13514, #27988 ) ;
#25662=FACE_OUTER_BOUND ( 'NONE', #18182, .T. ) ;
#25668=CARTESIAN_POINT ( 'NONE',  ( 9.999999999962065900, -38.97546878332597942, -26.38794647299679497 ) ) ;
#25669=ORIENTED_EDGE ( 'NONE', *, *, #815, .F. ) ;
#25670=CARTESIAN_POINT ( 'NONE',  ( -9.999999999979998222, -127.2536115484999897, -34.36329565063000047 ) ) ;
#25684=CARTESIAN_POINT ( 'NONE',  ( 24.10235451439214316, -11.92514887769131526, -1.399999999999998579 ) ) ;
#25687=ORIENTED_EDGE ( 'NONE', *, *, #26178, .F. ) ;
#25692=FACE_OUTER_BOUND ( 'NONE', #6609, .T. ) ;
#25699=ORIENTED_EDGE ( 'NONE', *, *, #26599, .T. ) ;
#25702=ORIENTED_EDGE ( 'NONE', *, *, #8527, .T. ) ;
#25704=CARTESIAN_POINT ( 'NONE',  ( 10.69999999999999929, -27.00000000000000000, -25.39999999999999858 ) ) ;
#25706=ORIENTED_EDGE ( 'NONE', *, *, #17463, .T. ) ;
#25715=CARTESIAN_POINT ( 'NONE',  ( -17.79876841389999598, -8.472631907500000281, -0.7000000003999986564 ) ) ;
#25725=CARTESIAN_POINT ( 'NONE',  ( -19.46795263067491177, 18.54728466947916132, -1.399999999999998135 ) ) ;
#25729=CARTESIAN_POINT ( 'NONE',  ( -10.69999999996535323, -29.70138143486801141, -27.04887742378237547 ) ) ;
#25730=CYLINDRICAL_SURFACE ( 'NONE', #1215, 3.000000000000003997 ) ;
#25734=CARTESIAN_POINT ( 'NONE',  ( 11.48163258689999999, -24.28840541759999994, -1.419991652300001128 ) ) ;
#25736=CARTESIAN_POINT ( 'NONE',  ( -9.999999999969999109, -24.87872937729999734, -30.52127062079999931 ) ) ;
#25737=CARTESIAN_POINT ( 'NONE',  ( 10.69999999997582485, -123.0138898083720420, -31.69041458428544544 ) ) ;
#25742=CIRCLE ( 'NONE', #24220, 1.100000000390000787 ) ;
#25749=ORIENTED_EDGE ( 'NONE', *, *, #30476, .T. ) ;
#25752=ORIENTED_EDGE ( 'NONE', *, *, #6012, .F. ) ;
#25757=AXIS2_PLACEMENT_3D ( 'NONE', #29622, #19883, #19726 ) ;
#25758=CARTESIAN_POINT ( 'NONE',  ( 10.99999999979999998, 20.99999999999999645, -67.09999999999999432 ) ) ;
#25765=EDGE_CURVE ( 'NONE', #4970, #6914, #27538, .T. ) ;
#25769=DIRECTION ( 'NONE',  ( 0.000000000000000000, -1.000000000000000000, 0.000000000000000000 ) ) ;
#25775=CARTESIAN_POINT ( 'NONE',  ( -16.80807069855958247, 9.890905752026485587, -1.400000000000002132 ) ) ;
#25780=AXIS2_PLACEMENT_3D ( 'NONE', #7454, #10286, #29308 ) ;
#25785=VERTEX_POINT ( 'NONE', #5673 ) ;
#25787=ORIENTED_EDGE ( 'NONE', *, *, #8678, .F. ) ;
#25790=DIRECTION ( 'NONE',  ( 1.635844237846128888E-12, -0.6889064844488322903, 0.7248502298298253876 ) ) ;
#25822=CARTESIAN_POINT ( 'NONE',  ( -10.35000000029999967, -25.00000000000000000, -2.400000000399998612 ) ) ;
#25834=DIRECTION ( 'NONE',  ( 0.000000000000000000, 0.000000000000000000, -1.000000000000000000 ) ) ;
#25837=CARTESIAN_POINT ( 'NONE',  ( 11.69999999989999928, -24.11120071670000087, -1.399999999299995856 ) ) ;
#25841=VECTOR ( 'NONE', #2480, 1000.000000000000000 ) ;
#25842=ORIENTED_EDGE ( 'NONE', *, *, #9216, .T. ) ;
#25847=CARTESIAN_POINT ( 'NONE',  ( 10.69999999930000101, -27.00000000000000000, -31.39999999999999858 ) ) ;
#25853=CARTESIAN_POINT ( 'NONE',  ( -10.00000000016788526, -27.47344925843678709, -16.99201750748492756 ) ) ;
#25854=ADVANCED_FACE ( 'NONE', ( #4560 ), #30688, .F. ) ;
#25871=VECTOR ( 'NONE', #25769, 1000.000000000000000 ) ;
#25881=ORIENTED_EDGE ( 'NONE', *, *, #26593, .T. ) ;
#25882=CARTESIAN_POINT ( 'NONE',  ( 10.32522729140000095, -24.73114799960000099, -1.399999999999998579 ) ) ;
#25888=CARTESIAN_POINT ( 'NONE',  ( 24.35861421954996331, 11.38494958298328008, -1.399999999999998579 ) ) ;
#25889=CARTESIAN_POINT ( 'NONE',  ( -10.69999999999999929, -127.2537393281999982, -34.36317439833000265 ) ) ;
#25897=ORIENTED_EDGE ( 'NONE', *, *, #24992, .F. ) ;
#25898=CARTESIAN_POINT ( 'NONE',  ( -10.00000000010862955, -28.84364015992474606, -30.79900052719611736 ) ) ;
#25922=CARTESIAN_POINT ( 'NONE',  ( 10.69999999996162998, -27.38139074261332695, -25.40000000000000568 ) ) ;
#25923=EDGE_CURVE ( 'NONE', #17734, #10804, #29476, .T. ) ;
#25926=LINE ( 'NONE', #4665, #27711 ) ;
#25934=DIRECTION ( 'NONE',  ( 0.000000000000000000, 2.256505319260000033E-12, 1.000000000000000000 ) ) ;
#25942=DIRECTION ( 'NONE',  ( 0.4911057670060950398, -1.966019939440381643E-12, -0.8710999515631688839 ) ) ;
#25944=ORIENTED_EDGE ( 'NONE', *, *, #17109, .T. ) ;
#25947=PLANE ( 'NONE',  #18980 ) ;
#25954=VERTEX_POINT ( 'NONE', #6913 ) ;
#25959=B_SPLINE_CURVE_WITH_KNOTS ( 'NONE', 5,
 ( #19112, #4488, #2588, #6839, #26355, #14089, #9349, #21166, #14399, #16588, #11874, #7153 ),
 .UNSPECIFIED., .F., .F.,
 ( 6, 3, 3, 6 ),
 ( 3.339306057409999973, 4.810258470149999965, 6.613963845949999865, 6.678484290009999214 ),
 .UNSPECIFIED. ) ;
#25967=ADVANCED_FACE ( 'NONE', ( #30381 ), #8807, .F. ) ;
#25969=ORIENTED_EDGE ( 'NONE', *, *, #28555, .T. ) ;
#25971=CARTESIAN_POINT ( 'NONE',  ( -11.39835558780000113, 19.99999999999999645, -0.7167260558000043691 ) ) ;
#25975=ORIENTED_EDGE ( 'NONE', *, *, #9384, .F. ) ;
#25982=CARTESIAN_POINT ( 'NONE',  ( -9.999999999959999997, -29.06671945329999929, -26.22544931050000017 ) ) ;
#25983=ORIENTED_EDGE ( 'NONE', *, *, #6842, .T. ) ;
#25992=ORIENTED_EDGE ( 'NONE', *, *, #24532, .T. ) ;
#26000=ADVANCED_FACE ( 'NONE', ( #2818 ), #29239, .F. ) ;
#26004=CARTESIAN_POINT ( 'NONE',  ( 10.00000000070000183, -43.95328087560000085, -27.24755286599999948 ) ) ;
#26013=CARTESIAN_POINT ( 'NONE',  ( -10.99289321870000080, -24.65831413349999934, -1.692893218799999877 ) ) ;
#26014=CARTESIAN_POINT ( 'NONE',  ( 12.77819780750000156, 21.69999999929999390, -56.09999999999999432 ) ) ;
#26015=ORIENTED_EDGE ( 'NONE', *, *, #6012, .T. ) ;
#26018=B_SPLINE_CURVE_WITH_KNOTS ( 'NONE', 3,
 ( #2002, #9369, #11740, #1685 ),
 .UNSPECIFIED., .F., .F.,
 ( 4, 4 ),
 ( -0.1743933577400000046, 0.1743933577400000046 ),
 .UNSPECIFIED. ) ;
#26024=FILL_AREA_STYLE_COLOUR ( '', #23493 ) ;
#26032=CARTESIAN_POINT ( 'NONE',  ( 10.58956533789999988, -24.61949705740000027, -1.102843518299999381 ) ) ;
#26037=EDGE_LOOP ( 'NONE', ( #10225, #20456, #29382, #16384, #10313, #23353 ) ) ;
#26043=ORIENTED_EDGE ( 'NONE', *, *, #26364, .F. ) ;
#26044=CARTESIAN_POINT ( 'NONE',  ( -11.69999999989999928, -25.00000000000000000, -0.6999999999999992895 ) ) ;
#26046=CARTESIAN_POINT ( 'NONE',  ( -10.60826873049999897, -25.00000000000000000, -1.605882353199999946 ) ) ;
#26053=CARTESIAN_POINT ( 'NONE',  ( 9.999999999948014917, -29.62149368169943742, -20.12419128126556700 ) ) ;
#26054=DIRECTION ( 'NONE',  ( 1.000000000000000000, 0.000000000000000000, -2.257436476311583018E-12 ) ) ;
#26057=PLANE ( 'NONE',  #23012 ) ;
#26070=EDGE_CURVE ( 'NONE', #20395, #27980, #11819, .T. ) ;
#26071=VECTOR ( 'NONE', #27440, 1000.000000000000114 ) ;
#26073=EDGE_CURVE ( 'NONE', #17864, #24435, #10060, .T. ) ;
#26080=CARTESIAN_POINT ( 'NONE',  ( 8.999999999540001738, 19.99999999999999645, -43.75000000008299850 ) ) ;
#26085=AXIS2_PLACEMENT_3D ( 'NONE', #915, #15374, #24971 ) ;
#26099=ORIENTED_EDGE ( 'NONE', *, *, #24207, .F. ) ;
#26101=DIRECTION ( 'NONE',  ( 0.000000000000000000, 0.000000000000000000, 1.000000000000000000 ) ) ;
#26103=VERTEX_POINT ( 'NONE', #12564 ) ;
#26120=DIRECTION ( 'NONE',  ( 0.000000000000000000, 1.000000000000000000, 0.000000000000000000 ) ) ;
#26121=CARTESIAN_POINT ( 'NONE',  ( 17.16657240420000008, 11.00000000000000355, -0.8000000000000020428 ) ) ;
#26129=VERTEX_POINT ( 'NONE', #26891 ) ;
#26133=VERTEX_POINT ( 'NONE', #19032 ) ;
#26138=VERTEX_POINT ( 'NONE', #7381 ) ;
#26141=DIRECTION ( 'NONE',  ( -1.000000000000000000, 0.000000000000000000, 0.000000000000000000 ) ) ;
#26155=CARTESIAN_POINT ( 'NONE',  ( 17.96875050214646308, 10.23368197051383532, -1.400000000000001910 ) ) ;
#26160=ORIENTED_EDGE ( 'NONE', *, *, #23887, .T. ) ;
#26166=ORIENTED_EDGE ( 'NONE', *, *, #15143, .T. ) ;
#26178=EDGE_CURVE ( 'NONE', #1244, #10748, #3423, .T. ) ;
#26181=CARTESIAN_POINT ( 'NONE',  ( 10.40384844070000092, -24.69832375569999883, -1.291913789700005477 ) ) ;
#26195=CARTESIAN_POINT ( 'NONE',  ( -10.00000000024713209, -25.48914305888663634, -31.02135916506400193 ) ) ;
#26196=CARTESIAN_POINT ( 'NONE',  ( 10.69999999997988382, -126.3403250530292183, -33.48783155437846659 ) ) ;
#26198=DIRECTION ( 'NONE',  ( -1.000000000000000000, 0.000000000000000000, 0.000000000000000000 ) ) ;
#26201=CARTESIAN_POINT ( 'NONE',  ( -10.46446609379999870, 21.70000000000000284, -54.63553390589999736 ) ) ;
#26203=CARTESIAN_POINT ( 'NONE',  ( 9.999999999949999108, -30.49251257979999963, -21.04205368479999905 ) ) ;
#26204=CYLINDRICAL_SURFACE ( 'NONE', #14759, 1.700000000000000178 ) ;
#26207=ORIENTED_EDGE ( 'NONE', *, *, #15135, .F. ) ;
#26211=EDGE_CURVE ( 'NONE', #12999, #23914, #18046, .T. ) ;
#26214=ORIENTED_EDGE ( 'NONE', *, *, #11762, .T. ) ;
#26226=VECTOR ( 'NONE', #7182, 1000.000000000000000 ) ;
#26229=CARTESIAN_POINT ( 'NONE',  ( 8.999999999770000869, 20.70710678120000381, -44.39289321881399530 ) ) ;
#26230=VECTOR ( 'NONE', #19004, 1000.000000000000000 ) ;
#26239=CARTESIAN_POINT ( 'NONE',  ( 10.32522729140000095, -24.73114799960000099, -1.399999999999998579 ) ) ;
#26241=EDGE_LOOP ( 'NONE', ( #344, #25185 ) ) ;
#26245=EDGE_CURVE ( 'NONE', #11243, #22220, #28442, .T. ) ;
#26260=ORIENTED_EDGE ( 'NONE', *, *, #12614, .F. ) ;
#26265=AXIS2_PLACEMENT_3D ( 'NONE', #15007, #21940, #10131 ) ;
#26269=CARTESIAN_POINT ( 'NONE',  ( -17.79876841389999598, -8.472631907500000281, -0.7999999992999995424 ) ) ;
#26272=CARTESIAN_POINT ( 'NONE',  ( 8.999999999770000869, 21.70000000070000112, -44.94917764161499463 ) ) ;
#26273=ORIENTED_EDGE ( 'NONE', *, *, #12266, .T. ) ;
#26276=EDGE_CURVE ( 'NONE', #5374, #27866, #30502, .T. ) ;
#26287=AXIS2_PLACEMENT_3D ( 'NONE', #17320, #26766, #7867 ) ;
#26290=DIRECTION ( 'NONE',  ( -1.000000000000000000, 0.000000000000000000, 3.489272357540000343E-15 ) ) ;
#26296=EDGE_CURVE ( 'NONE', #12935, #15367, #18947, .T. ) ;
#26302=VECTOR ( 'NONE', #19089, 1000.000000000000000 ) ;
#26306=VECTOR ( 'NONE', #19571, 1000.000000000000114 ) ;
#26314=ORIENTED_EDGE ( 'NONE', *, *, #28875, .F. ) ;
#26316=CARTESIAN_POINT ( 'NONE',  ( -1.243449787579999883E-14, 0.000000000000000000, -0.6999999999999992895 ) ) ;
#26327=ADVANCED_FACE ( 'NONE', ( #8606 ), #23262, .F. ) ;
#26334=VECTOR ( 'NONE', #2935, 1000.000000000000114 ) ;
#26342=CARTESIAN_POINT ( 'NONE',  ( 10.69999999999999929, -130.0000000000000000, -22.39999999999999858 ) ) ;
#26344=ORIENTED_EDGE ( 'NONE', *, *, #27977, .F. ) ;
#26353=B_SPLINE_CURVE_WITH_KNOTS ( 'NONE', 3,
 ( #24642, #27000, #3539, #3076, #13135, #888 ),
 .UNSPECIFIED., .F., .F.,
 ( 4, 2, 4 ),
 ( 0.000000000000000000, 0.5000000000000000000, 1.000000000000000000 ),
 .UNSPECIFIED. ) ;
#26355=CARTESIAN_POINT ( 'NONE',  ( -10.69999999999999929, -24.24512542849999974, -29.64315313870000068 ) ) ;
#26358=VECTOR ( 'NONE', #79, 1000.000000000000000 ) ;
#26361=DIRECTION ( 'NONE',  ( -1.000000000000000000, 0.000000000000000000, 0.000000000000000000 ) ) ;
#26364=EDGE_CURVE ( 'NONE', #14172, #25001, #23112, .T. ) ;
#26371=DIRECTION ( 'NONE',  ( -1.000000000000000000, -2.587524353642439916E-24, -2.257144471329210308E-12 ) ) ;
#26378=DIRECTION ( 'NONE',  ( -1.000000000000000000, 0.000000000000000000, 0.000000000000000000 ) ) ;
#26382=EDGE_CURVE ( 'NONE', #22250, #21103, #20066, .T. ) ;
#26383=DIRECTION ( 'NONE',  ( 0.000000000000000000, 0.000000000000000000, -1.000000000000000000 ) ) ;
#26389=CARTESIAN_POINT ( 'NONE',  ( -10.69999999999999929, 19.99999999999999645, -22.39999999999999858 ) ) ;
#26393=DIRECTION ( 'NONE',  ( 1.000000000000000000, -0.000000000000000000, -2.257150022439999944E-12 ) ) ;
#26400=CARTESIAN_POINT ( 'NONE',  ( 9.999999999969999109, -24.00000000000000000, -28.40000000000000213 ) ) ;
#26405=ORIENTED_EDGE ( 'NONE', *, *, #24992, .T. ) ;
#26406=DIRECTION ( 'NONE',  ( -1.000000000000000000, 0.000000000000000000, 0.000000000000000000 ) ) ;
#26411=CARTESIAN_POINT ( 'NONE',  ( 9.097977789939999838, 19.99999999999999645, -43.40000000045500173 ) ) ;
#26412=CARTESIAN_POINT ( 'NONE',  ( 16.58866331865612409, 11.94697101960596974, -1.400000000000001688 ) ) ;
#26436=ORIENTED_EDGE ( 'NONE', *, *, #13585, .F. ) ;
#26437=CARTESIAN_POINT ( 'NONE',  ( 9.999999999969999109, -24.87872937930000106, -30.52127062269999769 ) ) ;
#26442=VERTEX_POINT ( 'NONE', #7352 ) ;
#26453=VERTEX_POINT ( 'NONE', #21988 ) ;
#26454=ADVANCED_FACE ( 'NONE', ( #7648 ), #21366, .F. ) ;
#26472=VERTEX_POINT ( 'NONE', #26400 ) ;
#26484=CARTESIAN_POINT ( 'NONE',  ( 10.69999999999999929, -29.30501631380000305, -26.47986985000000004 ) ) ;
#26495=CARTESIAN_POINT ( 'NONE',  ( 10.99999999979999998, 21.69999999919999212, -70.09999999999999432 ) ) ;
#26500=CARTESIAN_POINT ( 'NONE',  ( -8.999999999710000864, 20.70710678120000381, -44.39289321881399530 ) ) ;
#26501=ORIENTED_EDGE ( 'NONE', *, *, #26724, .F. ) ;
#26503=B_SPLINE_CURVE_WITH_KNOTS ( 'NONE', 3,
 ( #1656, #18324, #23380, #6369 ),
 .UNSPECIFIED., .F., .F.,
 ( 4, 4 ),
 ( 0.000000000000000000, 1.000000000000000000 ),
 .UNSPECIFIED. ) ;
#26508=VECTOR ( 'NONE', #29413, 1000.000000000000000 ) ;
#26512=EDGE_LOOP ( 'NONE', ( #19039, #9285, #7803, #19565 ) ) ;
#26515=ORIENTED_EDGE ( 'NONE', *, *, #25615, .F. ) ;
#26517=EDGE_CURVE ( 'NONE', #21618, #23628, #9707, .T. ) ;
#26518=CYLINDRICAL_SURFACE ( 'NONE', #4881, 20.00000000000000711 ) ;
#26526=AXIS2_PLACEMENT_3D ( 'NONE', #8380, #6657, #23197 ) ;
#26528=VERTEX_POINT ( 'NONE', #19311 ) ;
#26542=DIRECTION ( 'NONE',  ( -1.000000000000000000, 0.000000000000000000, 0.000000000000000000 ) ) ;
#26553=ADVANCED_FACE ( 'NONE', ( #23735 ), #7428, .T. ) ;
#26556=AXIS2_PLACEMENT_3D ( 'NONE', #22807, #4082, #25488 ) ;
#26558=ORIENTED_EDGE ( 'NONE', *, *, #15468, .T. ) ;
#26561=CARTESIAN_POINT ( 'NONE',  ( 9.665310091690001215, 19.99999999999999645, -43.14889995884200147 ) ) ;
#26569=VECTOR ( 'NONE', #26378, 1000.000000000000000 ) ;
#26572=PLANE ( 'NONE',  #28082 ) ;
#26573=EDGE_CURVE ( 'NONE', #16174, #20501, #15199, .T. ) ;
#26592=VECTOR ( 'NONE', #13477, 1000.000000000000000 ) ;
#26593=EDGE_CURVE ( 'NONE', #6267, #30881, #29517, .T. ) ;
#26599=EDGE_CURVE ( 'NONE', #1366, #12957, #22137, .T. ) ;
#26609=DIRECTION ( 'NONE',  ( -0.000000000000000000, 1.000000000000000000, -2.257145581549999994E-12 ) ) ;
#26614=CARTESIAN_POINT ( 'NONE',  ( 16.05747815621842989, 10.97464310281671018, -1.400000000000001910 ) ) ;
#26615=DIRECTION ( 'NONE',  ( -0.000000000000000000, 1.000000000000000000, -2.258510841069999963E-12 ) ) ;
#26617=ORIENTED_EDGE ( 'NONE', *, *, #28930, .F. ) ;
#26618=CARTESIAN_POINT ( 'NONE',  ( 10.00000000070000183, -30.00000000000000000, -28.40000000000000213 ) ) ;
#26625=ADVANCED_FACE ( 'NONE', ( #12679 ), #15505, .T. ) ;
#26628=ORIENTED_EDGE ( 'NONE', *, *, #6321, .T. ) ;
#26633=EDGE_CURVE ( 'NONE', #22666, #20223, #22679, .T. ) ;
#26651=B_SPLINE_CURVE_WITH_KNOTS ( 'NONE', 3,
 ( #25572, #13605, #23211, #1654, #18477, #23531, #25888, #6992, #4166, #30608, #23683, #11710, #30753, #11560 ),
 .UNSPECIFIED., .F., .F.,
 ( 4, 2, 2, 2, 2, 2, 4 ),
 ( 0.000000000000000000, 0.1250000000000001388, 0.2500000000000002776, 0.5000000000000002220, 0.7500000000000001110, 0.8750000000000001110, 1.000000000000000000 ),
 .UNSPECIFIED. ) ;
#26653=CARTESIAN_POINT ( 'NONE',  ( -11.30445666259999982, -24.42656469639999983, -1.476955128299997533 ) ) ;
#26661=DIRECTION ( 'NONE',  ( -1.000000000000000000, 0.000000000000000000, 0.000000000000000000 ) ) ;
#26671=B_SPLINE_CURVE_WITH_KNOTS ( 'NONE', 3,
 ( #13132, #24946, #10939, #23217 ),
 .UNSPECIFIED., .F., .F.,
 ( 4, 4 ),
 ( 0.000000000000000000, 1.000000000000000000 ),
 .UNSPECIFIED. ) ;
#26676=LINE ( 'NONE', #10004, #19544 ) ;
#26683=CARTESIAN_POINT ( 'NONE',  ( 9.999999999963074870, -25.13744799596687685, -26.04099479820597196 ) ) ;
#26684=CARTESIAN_POINT ( 'NONE',  ( 10.69999999999999929, -127.2537437101000108, -34.36317024011000143 ) ) ;
#26687=CARTESIAN_POINT ( 'NONE',  ( -8.999999999970000886, 21.35000000040000145, -60.10000000000000142 ) ) ;
#26694=CYLINDRICAL_SURFACE ( 'NONE', #17308, 10.00000000000001421 ) ;
#26706=LINE ( 'NONE', #14755, #24732 ) ;
#26711=CARTESIAN_POINT ( 'NONE',  ( -11.69999999949999925, 19.99999999999999645, -1.049999999899998926 ) ) ;
#26715=ORIENTED_EDGE ( 'NONE', *, *, #1388, .T. ) ;
#26722=DIRECTION ( 'NONE',  ( -1.000000000000000000, 0.000000000000000000, -2.257436476311583018E-12 ) ) ;
#26724=EDGE_CURVE ( 'NONE', #9370, #18431, #20273, .T. ) ;
#26731=ORIENTED_EDGE ( 'NONE', *, *, #5484, .T. ) ;
#26734=EDGE_CURVE ( 'NONE', #21489, #19996, #18800, .T. ) ;
#26745=ORIENTED_EDGE ( 'NONE', *, *, #633, .F. ) ;
#26766=DIRECTION ( 'NONE',  ( -5.551115123047629543E-18, 6.252214723449840749E-31, -1.000000000000000000 ) ) ;
#26770=CARTESIAN_POINT ( 'NONE',  ( -16.83342759579999637, 11.00000000000000355, -0.8000000000000020428 ) ) ;
#26775=VECTOR ( 'NONE', #13683, 1000.000000000000000 ) ;
#26789=CARTESIAN_POINT ( 'NONE',  ( -13.39900052755271886, 20.99999999990061994, -68.94364015901247456 ) ) ;
#26790=CARTESIAN_POINT ( 'NONE',  ( 10.69999999994264428, -27.47147066701633022, -16.98898364808261618 ) ) ;
#26791=VERTEX_POINT ( 'NONE', #30140 ) ;
#26799=DIRECTION ( 'NONE',  ( 0.000000000000000000, -2.256504834499999987E-12, -1.000000000000000000 ) ) ;
#26801=LINE ( 'NONE', #5245, #30375 ) ;
#26802=EDGE_CURVE ( 'NONE', #28608, #16174, #23073, .T. ) ;
#26805=FACE_OUTER_BOUND ( 'NONE', #30063, .T. ) ;
#26808=ORIENTED_EDGE ( 'NONE', *, *, #11030, .T. ) ;
#26814=ORIENTED_EDGE ( 'NONE', *, *, #24532, .F. ) ;
#26820=DIRECTION ( 'NONE',  ( 1.000000000000000000, 0.000000000000000000, 0.000000000000000000 ) ) ;
#26833=CARTESIAN_POINT ( 'NONE',  ( 11.69999999989999928, -24.11120071670000087, -1.399999999299995856 ) ) ;
#26839=AXIS2_PLACEMENT_3D ( 'NONE', #27927, #6368, #15965 ) ;
#26840=CARTESIAN_POINT ( 'NONE',  ( -11.69999999989999928, -24.11120071630000083, -1.399999999999998579 ) ) ;
#26846=DIRECTION ( 'NONE',  ( -1.000000000000000000, 0.000000000000000000, 0.000000000000000000 ) ) ;
#26849=CYLINDRICAL_SURFACE ( 'NONE', #3717, 20.00000000000000355 ) ;
#26851=ORIENTED_EDGE ( 'NONE', *, *, #30416, .T. ) ;
#26859=CIRCLE ( 'NONE', #9263, 4.175165894169885483 ) ;
#26861=VECTOR ( 'NONE', #30091, 1000.000000000000000 ) ;
#26870=CARTESIAN_POINT ( 'NONE',  ( 17.42753860032010849, 12.07825306288010658, -1.400000000000001910 ) ) ;
#26889=CARTESIAN_POINT ( 'NONE',  ( -10.69999999999813589, -27.37998968024088953, -25.40000000000000213 ) ) ;
#26891=CARTESIAN_POINT ( 'NONE',  ( 9.000000000000000000, 21.70000000000000284, -51.10000000017000588 ) ) ;
#26896=( GEOMETRIC_REPRESENTATION_CONTEXT ( 3 ) GLOBAL_UNCERTAINTY_ASSIGNED_CONTEXT ( ( #26987 ) ) GLOBAL_UNIT_ASSIGNED_CONTEXT ( ( #18418, #20467, #13863 ) ) REPRESENTATION_CONTEXT ( 'NONE', 'WORKASPACE' ) );
#26898=CARTESIAN_POINT ( 'NONE',  ( -10.00000000020261659, -34.37899275726326920, -24.26894200080224095 ) ) ;
#26902=ADVANCED_FACE ( 'NONE', ( #19428 ), #26204, .T. ) ;
#26905=DIRECTION ( 'NONE',  ( 0.000000000000000000, 0.000000000000000000, 1.000000000000000000 ) ) ;
#26909=EDGE_CURVE ( 'NONE', #29211, #5951, #5203, .T. ) ;
#26927=EDGE_CURVE ( 'NONE', #1750, #22335, #23425, .T. ) ;
#26929=CARTESIAN_POINT ( 'NONE',  ( 10.69999999999999929, -43.95328087560000085, -27.24755286599999948 ) ) ;
#26937=DIRECTION ( 'NONE',  ( 0.000000000000000000, -2.257145581549999994E-12, -1.000000000000000000 ) ) ;
#26956=CARTESIAN_POINT ( 'NONE',  ( 10.69999999999999929, -24.92624922430000467, -26.23177045490000125 ) ) ;
#26960=CARTESIAN_POINT ( 'NONE',  ( 10.34999999979999963, 19.99999999999999645, -2.400000000399998612 ) ) ;
#26971=EDGE_LOOP ( 'NONE', ( #17189, #26515, #2522, #28208, #21413, #18251, #1286, #3392, #30852, #7483, #31116, #2026, #24686, #7470, #4916, #11809, #26814 ) ) ;
#26977=VERTEX_POINT ( 'NONE', #25715 ) ;
#26986=VERTEX_POINT ( 'NONE', #8376 ) ;
#26987=UNCERTAINTY_MEASURE_WITH_UNIT (LENGTH_MEASURE( 1.000000000000000082E-05 ), #18418, 'distance_accuracy_value', 'NONE');
#26992=CARTESIAN_POINT ( 'NONE',  ( 10.99999999979999998, 20.99999999999999645, -58.51619795479999908 ) ) ;
#27000=CARTESIAN_POINT ( 'NONE',  ( -10.69999999997381401, -28.84292916499192927, -30.79962415685015742 ) ) ;
#27002=VECTOR ( 'NONE', #10347, 1000.000000000000000 ) ;
#27007=CARTESIAN_POINT ( 'NONE',  ( 11.30445670279999959, -24.42656466549999905, -1.476955110899999646 ) ) ;
#27014=EDGE_CURVE ( 'NONE', #22831, #11286, #13742, .T. ) ;
#27019=DIRECTION ( 'NONE',  ( -0.000000000000000000, 1.000000000000000000, -2.257145581549999994E-12 ) ) ;
#27033=DIRECTION ( 'NONE',  ( 2.257150022439999944E-12, 0.000000000000000000, 1.000000000000000000 ) ) ;
#27034=LINE ( 'NONE', #17579, #23351 ) ;
#27042=ADVANCED_FACE ( 'NONE', ( #13264 ), #14334, .T. ) ;
#27045=ORIENTED_EDGE ( 'NONE', *, *, #23502, .T. ) ;
#27049=FACE_OUTER_BOUND ( 'NONE', #29720, .T. ) ;
#27063=PLANE ( 'NONE',  #14253 ) ;
#27072=CARTESIAN_POINT ( 'NONE',  ( 10.69999999999999929, 19.99999999999999645, -22.39999999999999858 ) ) ;
#27083=CYLINDRICAL_SURFACE ( 'NONE', #24815, 3.000000000000001776 ) ;
#27084=CARTESIAN_POINT ( 'NONE',  ( 13.39900052630364335, 20.99999999989583088, -68.94364016086436209 ) ) ;
#27087=CARTESIAN_POINT ( 'NONE',  ( -9.999999999969999109, -43.95328087550000618, -27.24755286569999768 ) ) ;
#27091=VERTEX_POINT ( 'NONE', #27904 ) ;
#27097=EDGE_CURVE ( 'NONE', #2571, #19758, #4723, .T. ) ;
#27101=LINE ( 'NONE', #25048, #20068 ) ;
#27110=CARTESIAN_POINT ( 'NONE',  ( -14.00000000000000000, 21.70000000000000284, -62.80809805499999499 ) ) ;
#27112=CARTESIAN_POINT ( 'NONE',  ( 10.69999999995908091, -34.38203972397853647, -24.27123760832591515 ) ) ;
#27116=CARTESIAN_POINT ( 'NONE',  ( -11.02573875399999892, -24.63456740089999997, -1.660048605199998528 ) ) ;
#27120=CARTESIAN_POINT ( 'NONE',  ( -13.67718144140000014, 20.99999999999999645, -57.16242377749999548 ) ) ;
#27121=EDGE_CURVE ( 'NONE', #19928, #28095, #29415, .T. ) ;
#27126=EDGE_LOOP ( 'NONE', ( #11126, #22328, #19111, #5492 ) ) ;
#27130=CARTESIAN_POINT ( 'NONE',  ( -17.79876841389999598, -8.472631907500000281, -1.399999999599998990 ) ) ;
#27142=ORIENTED_EDGE ( 'NONE', *, *, #2524, .T. ) ;
#27143=ADVANCED_FACE ( 'NONE', ( #27049 ), #14482, .T. ) ;
#27148=DIRECTION ( 'NONE',  ( 4.901511854548699870E-24, -1.000000000000000000, 2.257145581550420047E-12 ) ) ;
#27154=EDGE_CURVE ( 'NONE', #30881, #9514, #23020, .T. ) ;
#27156=DIRECTION ( 'NONE',  ( 0.000000000000000000, 1.000000000000000000, 0.000000000000000000 ) ) ;
#27161=VERTEX_POINT ( 'NONE', #12568 ) ;
#27162=CIRCLE ( 'NONE', #21648, 2.999999999999999112 ) ;
#27164=CARTESIAN_POINT ( 'NONE',  ( 11.62710820729999917, -24.17108566339999953, -1.401657795999995626 ) ) ;
#27171=VERTEX_POINT ( 'NONE', #935 ) ;
#27188=CARTESIAN_POINT ( 'NONE',  ( -13.99999999969999820, 20.99999999999999645, -63.10000000000000142 ) ) ;
#27190=ADVANCED_FACE ( 'NONE', ( #6099 ), #27354, .F. ) ;
#27191=CARTESIAN_POINT ( 'NONE',  ( -17.00495585196167525, 12.09604337527003892, -1.400000000000001910 ) ) ;
#27193=FACE_OUTER_BOUND ( 'NONE', #329, .T. ) ;
#27196=EDGE_CURVE ( 'NONE', #14172, #7936, #2403, .T. ) ;
#27200=VERTEX_POINT ( 'NONE', #8298 ) ;
#27203=EDGE_LOOP ( 'NONE', ( #14638, #24616, #10904, #13891 ) ) ;
#27204=EDGE_LOOP ( 'NONE', ( #2210, #10744, #19867, #19310 ) ) ;
#27206=AXIS2_PLACEMENT_3D ( 'NONE', #24067, #5471, #12706 ) ;
#27207=EDGE_LOOP ( 'NONE', ( #23776, #11222, #22142, #17406 ) ) ;
#27225=FACE_OUTER_BOUND ( 'NONE', #16409, .T. ) ;
#27233=CARTESIAN_POINT ( 'NONE',  ( 11.25000838620000110, 19.99999999999999645, -0.7501799203000064642 ) ) ;
#27256=ADVANCED_FACE ( 'NONE', ( #3583 ), #5797, .T. ) ;
#27260=AXIS2_PLACEMENT_3D ( 'NONE', #2367, #22449, #9594 ) ;
#27267=CARTESIAN_POINT ( 'NONE',  ( 10.97092067110000002, -24.67424207510000045, -1.714865450400004931 ) ) ;
#27280=ORIENTED_EDGE ( 'NONE', *, *, #13051, .T. ) ;
#27286=CARTESIAN_POINT ( 'NONE',  ( 10.61898076289999970, 19.99999999999999645, -42.96980960428000174 ) ) ;
#27293=CARTESIAN_POINT ( 'NONE',  ( 13.99999999992460076, 21.69999999930106682, -58.04802353003142912 ) ) ;
#27297=CARTESIAN_POINT ( 'NONE',  ( 9.000000000000000000, 21.69999999990000106, -67.10000000019999788 ) ) ;
#27301=DIRECTION ( 'NONE',  ( 0.000000000000000000, -1.000000000000000000, 0.000000000000000000 ) ) ;
#27305=ORIENTED_EDGE ( 'NONE', *, *, #29808, .T. ) ;
#27308=AXIS2_PLACEMENT_3D ( 'NONE', #13170, #20116, #27344 ) ;
#27313=EDGE_LOOP ( 'NONE', ( #3050, #25352, #21969, #2490 ) ) ;
#27316=DIRECTION ( 'NONE',  ( 0.000000000000000000, 2.256504834499999987E-12, 1.000000000000000000 ) ) ;
#27317=CARTESIAN_POINT ( 'NONE',  ( -19.45974949220212480, 18.55460157459818760, -0.6999999999999992895 ) ) ;
#27320=VERTEX_POINT ( 'NONE', #5153 ) ;
#27325=VECTOR ( 'NONE', #25934, 1000.000000000000000 ) ;
#27326=CARTESIAN_POINT ( 'NONE',  ( 9.999999999980001775, -27.39269908193462655, -31.40000000000158664 ) ) ;
#27327=AXIS2_PLACEMENT_3D ( 'NONE', #23851, #2294, #26361 ) ;
#27340=CARTESIAN_POINT ( 'NONE',  ( 18.13191322300000152, 10.47263190709999492, -0.6999999999999992895 ) ) ;
#27342=CARTESIAN_POINT ( 'NONE',  ( 8.999999999770000869, 20.99999999999999645, -45.10000000000000142 ) ) ;
#27344=DIRECTION ( 'NONE',  ( 0.000000000000000000, 1.000000000000000000, 0.000000000000000000 ) ) ;
#27354=CYLINDRICAL_SURFACE ( 'NONE', #1712, 3.999999999999999112 ) ;
#27356=ORIENTED_EDGE ( 'NONE', *, *, #28493, .T. ) ;
#27366=EDGE_CURVE ( 'NONE', #1319, #17864, #7974, .T. ) ;
#27372=VECTOR ( 'NONE', #15690, 1000.000000000000000 ) ;
#27373=CARTESIAN_POINT ( 'NONE',  ( -10.00000000045684523, -29.92191803000534023, -29.18524365307803947 ) ) ;
#27374=CARTESIAN_POINT ( 'NONE',  ( 10.46446609389999871, 20.99999999999999645, -54.63553390589999736 ) ) ;
#27390=CARTESIAN_POINT ( 'NONE',  ( -26.57440914490000239, -3.469982507400000582, -0.6999999999999992895 ) ) ;
#27394=VECTOR ( 'NONE', #14056, 1000.000000000000000 ) ;
#27401=DIRECTION ( 'NONE',  ( -1.000000000000000000, 0.000000000000000000, -2.257144471330000330E-12 ) ) ;
#27433=LINE ( 'NONE', #13268, #7915 ) ;
#27440=DIRECTION ( 'NONE',  ( 0.000000000000000000, 0.9986295347545772749, 0.05233595624287791515 ) ) ;
#27441=EDGE_LOOP ( 'NONE', ( #27685, #18879, #19333, #24654 ) ) ;
#27446=LINE ( 'NONE', #27297, #14783 ) ;
#27449=CARTESIAN_POINT ( 'NONE',  ( -10.60826873110000079, -24.73114799900000094, -1.605882352700004123 ) ) ;
#27452=LINE ( 'NONE', #12837, #13766 ) ;
#27455=CARTESIAN_POINT ( 'NONE',  ( 11.69999999989999928, -25.00000000000000000, -2.399999999999999467 ) ) ;
#27480=AXIS2_PLACEMENT_3D ( 'NONE', #19244, #2417, #16876 ) ;
#27490=CARTESIAN_POINT ( 'NONE',  ( -10.69999999999893703, -28.46561708982691030, -25.75493691888135572 ) ) ;
#27505=ORIENTED_EDGE ( 'NONE', *, *, #12854, .F. ) ;
#27507=CARTESIAN_POINT ( 'NONE',  ( 10.00000000000000000, 21.70000000000000284, -60.10000000000000142 ) ) ;
#27508=CARTESIAN_POINT ( 'NONE',  ( -10.69999999999999929, 19.99999999999999645, -22.39999999999999858 ) ) ;
#27521=VECTOR ( 'NONE', #30590, 1000.000000000000000 ) ;
#27523=DIRECTION ( 'NONE',  ( 0.000000000000000000, 0.000000000000000000, -1.000000000000000000 ) ) ;
#27533=ORIENTED_EDGE ( 'NONE', *, *, #29066, .F. ) ;
#27536=EDGE_CURVE ( 'NONE', #26442, #5618, #1221, .T. ) ;
#27538=LINE ( 'NONE', #817, #3697 ) ;
#27541=CARTESIAN_POINT ( 'NONE',  ( 9.000000000000000000, -130.0000000000000000, -42.39999999999999858 ) ) ;
#27544=ORIENTED_EDGE ( 'NONE', *, *, #16389, .F. ) ;
#27548=SURFACE_SIDE_STYLE ('',( #25192 ) ) ;
#27552=CARTESIAN_POINT ( 'NONE',  ( 10.69999999999999929, 19.99999999999999645, -22.39999999999999858 ) ) ;
#27569=LINE ( 'NONE', #29776, #12795 ) ;
#27571=ORIENTED_EDGE ( 'NONE', *, *, #29945, .F. ) ;
#27580=AXIS2_PLACEMENT_3D ( 'NONE', #3731, #13330, #22939 ) ;
#27603=ORIENTED_EDGE ( 'NONE', *, *, #19093, .F. ) ;
#27606=B_SPLINE_CURVE_WITH_KNOTS ( 'NONE', 3,
 ( #12945, #1305, #5547, #27112, #18118, #20181, #997, #10587, #3646, #8517 ),
 .UNSPECIFIED., .F., .F.,
 ( 4, 2, 2, 2, 4 ),
 ( 0.000000000000000000, 0.2500000000000000000, 0.5000000000000000000, 0.7500000000000000000, 1.000000000000000000 ),
 .UNSPECIFIED. ) ;
#27609=LINE ( 'NONE', #20221, #11723 ) ;
#27615=CARTESIAN_POINT ( 'NONE',  ( -9.000000000000000000, 21.69999999998272244, -51.75635761556686987 ) ) ;
#27627=EDGE_CURVE ( 'NONE', #21618, #30015, #28973, .T. ) ;
#27634=LINE ( 'NONE', #6079, #3973 ) ;
#27644=CARTESIAN_POINT ( 'NONE',  ( 9.999999999971771913, -24.07808197008955631, -29.18524365354899075 ) ) ;
#27645=CARTESIAN_POINT ( 'NONE',  ( -17.92947097108555354, 10.82847174396546741, -1.400000000000001910 ) ) ;
#27647=DIRECTION ( 'NONE',  ( 1.000000000000000000, 0.000000000000000000, 0.000000000000000000 ) ) ;
#27656=ADVANCED_FACE ( 'NONE', ( #18665 ), #9373, .F. ) ;
#27660=B_SPLINE_CURVE_WITH_KNOTS ( 'NONE', 1,
 ( #1611, #23170 ),
 .UNSPECIFIED., .F., .F.,
 ( 2, 2 ),
 ( -0.7000000000009999335, 0.002002273571169999045 ),
 .UNSPECIFIED. ) ;
#27664=FACE_OUTER_BOUND ( 'NONE', #14048, .T. ) ;
#27666=CARTESIAN_POINT ( 'NONE',  ( -9.707106781189999367, -130.0000000000000000, -43.10710678118599759 ) ) ;
#27669=DIRECTION ( 'NONE',  ( 2.256480420250000087E-12, -0.000000000000000000, -1.000000000000000000 ) ) ;
#27672=CARTESIAN_POINT ( 'NONE',  ( -10.00000000057842087, -30.00000000000020606, -28.79269908169879955 ) ) ;
#27679=CARTESIAN_POINT ( 'NONE',  ( -26.57440607989999748, -3.469982107200002108, -1.399999999999998579 ) ) ;
#27685=ORIENTED_EDGE ( 'NONE', *, *, #11367, .F. ) ;
#27697=ORIENTED_EDGE ( 'NONE', *, *, #24207, .T. ) ;
#27699=ORIENTED_EDGE ( 'NONE', *, *, #11880, .T. ) ;
#27703=ORIENTED_EDGE ( 'NONE', *, *, #8777, .T. ) ;
#27711=VECTOR ( 'NONE', #2320, 1000.000000000000000 ) ;
#27735=VECTOR ( 'NONE', #6288, 1000.000000000000000 ) ;
#27738=ORIENTED_EDGE ( 'NONE', *, *, #4885, .F. ) ;
#27750=CARTESIAN_POINT ( 'NONE',  ( 10.67300410500000041, 19.99999999999999645, -42.78321928043000355 ) ) ;
#27761=CYLINDRICAL_SURFACE ( 'NONE', #7152, 3.000000000000000444 ) ;
#27762=PLANE ( 'NONE',  #26839 ) ;
#27767=CARTESIAN_POINT ( 'NONE',  ( -10.40384843829999895, -24.69832375660000423, -1.291913792900001301 ) ) ;
#27777=CARTESIAN_POINT ( 'NONE',  ( -23.35349119075231172, 13.32552209464216553, -0.6999999999999992895 ) ) ;
#27788=CARTESIAN_POINT ( 'NONE',  ( -16.83342759559999635, -9.000000000000001776, -1.399999999999998579 ) ) ;
#27789=DIRECTION ( 'NONE',  ( 0.000000000000000000, 0.000000000000000000, 1.000000000000000000 ) ) ;
#27792=CARTESIAN_POINT ( 'NONE',  ( 18.13191322229999969, 10.47263190749999495, -1.399999999599998990 ) ) ;
#27813=DIRECTION ( 'NONE',  ( -1.000000000000000000, 0.000000000000000000, 0.000000000000000000 ) ) ;
#27819=EDGE_LOOP ( 'NONE', ( #8, #14212, #2401, #21758 ) ) ;
#27833=CARTESIAN_POINT ( 'NONE',  ( -10.69999999999999929, -27.00000000000000000, -25.39999999999999858 ) ) ;
#27843=AXIS2_PLACEMENT_3D ( 'NONE', #26316, #11377, #14366 ) ;
#27845=VECTOR ( 'NONE', #5466, 1000.000000000000000 ) ;
#27850=ADVANCED_FACE ( 'NONE', ( #19294 ), #14583, .T. ) ;
#27858=VERTEX_POINT ( 'NONE', #21811 ) ;
#27861=EDGE_CURVE ( 'NONE', #26129, #26103, #15041, .T. ) ;
#27862=ORIENTED_EDGE ( 'NONE', *, *, #11036, .F. ) ;
#27866=VERTEX_POINT ( 'NONE', #26833 ) ;
#27868=CARTESIAN_POINT ( 'NONE',  ( 10.69999999999999929, -30.00000000000000000, -28.40000000000000213 ) ) ;
#27887=CARTESIAN_POINT ( 'NONE',  ( 9.999999999989825028, -129.7569854622061882, -38.71642352353225647 ) ) ;
#27899=EDGE_CURVE ( 'NONE', #20193, #4001, #27446, .T. ) ;
#27903=EDGE_LOOP ( 'NONE', ( #2177, #22677, #5007, #3552, #2313, #2561 ) ) ;
#27904=CARTESIAN_POINT ( 'NONE',  ( 10.69999999999999929, -29.30501631380000305, -26.47986985000000004 ) ) ;
#27916=CARTESIAN_POINT ( 'NONE',  ( 10.70000000070000112, 19.99999999999999645, -42.59161006100999458 ) ) ;
#27925=EDGE_LOOP ( 'NONE', ( #28907, #15985, #27699, #14690, #30732, #17959 ) ) ;
#27927=CARTESIAN_POINT ( 'NONE',  ( 0.000000000000000000, 20.99999999999999645, -44.10000000017154065 ) ) ;
#27933=CARTESIAN_POINT ( 'NONE',  ( -11.57608395609999974, -24.17108566160000294, -0.7028182529999968953 ) ) ;
#27944=CARTESIAN_POINT ( 'NONE',  ( 10.93831327714496204, 21.69999999997515516, -55.10899305193176900 ) ) ;
#27947=ADVANCED_FACE ( 'NONE', ( #20528 ), #27762, .T. ) ;
#27949=VERTEX_POINT ( 'NONE', #4009 ) ;
#27954=CARTESIAN_POINT ( 'NONE',  ( -12.68067472840826682, 21.69999999999972218, -56.02822601348136544 ) ) ;
#27959=EDGE_LOOP ( 'NONE', ( #28449, #23306 ) ) ;
#27962=DIRECTION ( 'NONE',  ( -0.7071067811870476172, 0.000000000000000000, 0.7071067811860475283 ) ) ;
#27976=LINE ( 'NONE', #23585, #1896 ) ;
#27977=EDGE_CURVE ( 'NONE', #14134, #669, #22236, .T. ) ;
#27980=VERTEX_POINT ( 'NONE', #31065 ) ;
#27988=DIRECTION ( 'NONE',  ( -1.000000000000000000, 0.000000000000000000, 0.000000000000000000 ) ) ;
#27991=CARTESIAN_POINT ( 'NONE',  ( -9.999999999969999109, -29.12127062080000073, -30.52127062269999769 ) ) ;
#27995=CARTESIAN_POINT ( 'NONE',  ( -12.77820031409999935, 21.69999999929999390, -56.09999999999999432 ) ) ;
#27996=EDGE_CURVE ( 'NONE', #9398, #13706, #28545, .T. ) ;
#27998=LINE ( 'NONE', #1421, #13646 ) ;
#28000=DIRECTION ( 'NONE',  ( -0.000000000000000000, -0.000000000000000000, 1.000000000000000000 ) ) ;
#28001=ADVANCED_FACE ( 'NONE', ( #9504 ), #25730, .F. ) ;
#28007=CARTESIAN_POINT ( 'NONE',  ( -10.69999999999999929, -77.50000000000000000, -29.00566191750000300 ) ) ;
#28012=CARTESIAN_POINT ( 'NONE',  ( 9.999999999952072116, -31.36353147791090379, -21.95991608839452880 ) ) ;
#28027=ADVANCED_FACE ( 'NONE', ( #30609 ), #30914, .F. ) ;
#28033=VECTOR ( 'NONE', #25834, 1000.000000000000000 ) ;
#28035=CYLINDRICAL_SURFACE ( 'NONE', #7687, 1.700000000000000178 ) ;
#28041=CARTESIAN_POINT ( 'NONE',  ( -13.65679423271931903, -23.08581637699097655, -1.399999999999998579 ) ) ;
#28042=EDGE_LOOP ( 'NONE', ( #10411, #24126, #14553, #27544, #10342 ) ) ;
#28053=ORIENTED_EDGE ( 'NONE', *, *, #13491, .F. ) ;
#28057=DIRECTION ( 'NONE',  ( -1.553791817432425509E-12, 0.7253743710120286181, -0.6883545756940269156 ) ) ;
#28065=LINE ( 'NONE', #3998, #22210 ) ;
#28074=VERTEX_POINT ( 'NONE', #2734 ) ;
#28075=FACE_OUTER_BOUND ( 'NONE', #4918, .T. ) ;
#28082=AXIS2_PLACEMENT_3D ( 'NONE', #29543, #9730, #27033 ) ;
#28090=EDGE_CURVE ( 'NONE', #7936, #25188, #4952, .T. ) ;
#28092=EDGE_CURVE ( 'NONE', #28151, #19704, #14857, .T. ) ;
#28095=VERTEX_POINT ( 'NONE', #7902 ) ;
#28099=ORIENTED_EDGE ( 'NONE', *, *, #26296, .T. ) ;
#28102=AXIS2_PLACEMENT_3D ( 'NONE', #4276, #23480, #28336 ) ;
#28114=DIRECTION ( 'NONE',  ( 0.000000000000000000, 1.000000000000000000, 0.000000000000000000 ) ) ;
#28120=CARTESIAN_POINT ( 'NONE',  ( 3.510330246760000161, 1.917702155199998870, -44.10000000000000142 ) ) ;
#28124=CARTESIAN_POINT ( 'NONE',  ( -17.79876841479999783, 11.52736809289999620, -1.399999999999998579 ) ) ;
#28126=EDGE_CURVE ( 'NONE', #4970, #12999, #5395, .T. ) ;
#28138=B_SPLINE_CURVE_WITH_KNOTS ( 'NONE', 5,
 ( #13142, #1202, #3870, #17558, #10796, #18013 ),
 .UNSPECIFIED., .F., .F.,
 ( 6, 6 ),
 ( 0.000000000000000000, 1.000000000000000000 ),
 .UNSPECIFIED. ) ;
#28140=FACE_OUTER_BOUND ( 'NONE', #30868, .T. ) ;
#28144=DIRECTION ( 'NONE',  ( -1.000000000000000000, 0.000000000000000000, 0.000000000000000000 ) ) ;
#28147=ADVANCED_FACE ( 'NONE', ( #12330 ), #17506, .T. ) ;
#28151=VERTEX_POINT ( 'NONE', #12167 ) ;
#28153=EDGE_CURVE ( 'NONE', #20047, #3589, #22239, .T. ) ;
#28168=LINE ( 'NONE', #3620, #10707 ) ;
#28169=CARTESIAN_POINT ( 'NONE',  ( 9.999999999961115549, -37.77593666300375475, -25.96758248523643786 ) ) ;
#28172=ORIENTED_EDGE ( 'NONE', *, *, #25765, .F. ) ;
#28182=CARTESIAN_POINT ( 'NONE',  ( 25.32376197130138706, -8.841464498151523799, -1.399999999999998357 ) ) ;
#28184=DIRECTION ( 'NONE',  ( -0.8923938138917432150, 1.018860921557045171E-12, 0.4512574441798702374 ) ) ;
#28194=VECTOR ( 'NONE', #7402, 1000.000000000000000 ) ;
#28197=CARTESIAN_POINT ( 'NONE',  ( -10.00000000000468603, -29.62149368164926955, -20.12419128111021749 ) ) ;
#28208=ORIENTED_EDGE ( 'NONE', *, *, #8710, .T. ) ;
#28235=CARTESIAN_POINT ( 'NONE',  ( 10.69999999997493134, -121.1571612431100817, -31.29363678846695862 ) ) ;
#28250=EDGE_CURVE ( 'NONE', #5951, #29211, #3748, .T. ) ;
#28255=DIRECTION ( 'NONE',  ( -1.000000000000000000, 0.000000000000000000, 0.000000000000000000 ) ) ;
#28257=CYLINDRICAL_SURFACE ( 'NONE', #16062, 3.000000000000003997 ) ;
#28258=CARTESIAN_POINT ( 'NONE',  ( 9.734589334720000764, 19.99999999999999645, -43.07962306035999944 ) ) ;
#28266=ADVANCED_FACE ( 'NONE', ( #25692 ), #18594, .T. ) ;
#28268=DIRECTION ( 'NONE',  ( 0.000000000000000000, 1.000000000000000000, 0.000000000000000000 ) ) ;
#28271=LINE ( 'NONE', #26080, #22203 ) ;
#28281=CARTESIAN_POINT ( 'NONE',  ( -13.99999999969999820, 20.99999999999999645, -58.51619611000000276 ) ) ;
#28283=ADVANCED_FACE ( 'NONE', ( #11672 ), #28035, .T. ) ;
#28288=ORIENTED_EDGE ( 'NONE', *, *, #24440, .T. ) ;
#28289=CARTESIAN_POINT ( 'NONE',  ( -10.99999999969999998, 20.99999999999999645, -58.51619611000000276 ) ) ;
#28294=LINE ( 'NONE', #8784, #21006 ) ;
#28313=LINE ( 'NONE', #16051, #25358 ) ;
#28326=ORIENTED_EDGE ( 'NONE', *, *, #4372, .T. ) ;
#28336=DIRECTION ( 'NONE',  ( 0.000000000000000000, -1.000000000000000000, 0.000000000000000000 ) ) ;
#28340=VECTOR ( 'NONE', #15050, 1000.000000000000000 ) ;
#28342=VECTOR ( 'NONE', #2444, 1000.000000000000000 ) ;
#28373=ORIENTED_EDGE ( 'NONE', *, *, #14412, .T. ) ;
#28375=CARTESIAN_POINT ( 'NONE',  ( 10.00000000020000002, 19.99999999999999645, -2.400000000399998612 ) ) ;
#28377=ADVANCED_FACE ( 'NONE', ( #24411 ), #19536, .T. ) ;
#28395=VECTOR ( 'NONE', #929, 1000.000000000000000 ) ;
#28400=CARTESIAN_POINT ( 'NONE',  ( 10.69999999997629914, -123.6108562392817731, -31.89970902356391136 ) ) ;
#28401=ORIENTED_EDGE ( 'NONE', *, *, #26245, .T. ) ;
#28403=CYLINDRICAL_SURFACE ( 'NONE', #20156, 0.9999999999999988898 ) ;
#28408=CARTESIAN_POINT ( 'NONE',  ( 10.69999999997255991, -24.59987423426687059, -30.24240556170614269 ) ) ;
#28412=CARTESIAN_POINT ( 'NONE',  ( -9.999999999959999997, -24.87868334570000073, -26.27868334529999927 ) ) ;
#28414=ORIENTED_EDGE ( 'NONE', *, *, #21395, .T. ) ;
#28428=LINE ( 'NONE', #4359, #19321 ) ;
#28437=EDGE_CURVE ( 'NONE', #13159, #20501, #3450, .T. ) ;
#28438=CARTESIAN_POINT ( 'NONE',  ( 9.631068058028711576, 20.99999999999431211, -53.61809490185450500 ) ) ;
#28442=LINE ( 'NONE', #25469, #5199 ) ;
#28444=EDGE_CURVE ( 'NONE', #30538, #14782, #14811, .T. ) ;
#28447=ORIENTED_EDGE ( 'NONE', *, *, #13209, .T. ) ;
#28449=ORIENTED_EDGE ( 'NONE', *, *, #26909, .T. ) ;
#28454=LINE ( 'NONE', #6586, #4784 ) ;
#28464=CARTESIAN_POINT ( 'NONE',  ( -10.14136574519999989, -25.00000000000000000, -1.689351118899999671 ) ) ;
#28470=FACE_OUTER_BOUND ( 'NONE', #22107, .T. ) ;
#28475=CARTESIAN_POINT ( 'NONE',  ( -10.02699808790000091, 19.99999999999999645, -2.016765154599996279 ) ) ;
#28481=VERTEX_POINT ( 'NONE', #8163 ) ;
#28491=CARTESIAN_POINT ( 'NONE',  ( -1.243449787579999883E-14, 0.000000000000000000, -0.6999999999999992895 ) ) ;
#28493=EDGE_CURVE ( 'NONE', #5911, #26442, #22812, .T. ) ;
#28495=FACE_OUTER_BOUND ( 'NONE', #5559, .T. ) ;
#28500=PLANE ( 'NONE',  #12284 ) ;
#28510=CARTESIAN_POINT ( 'NONE',  ( -24.50943110104372380, -10.89728548205058623, -1.399999999999998579 ) ) ;
#28531=B_SPLINE_CURVE_WITH_KNOTS ( 'NONE', 3,
 ( #30556, #21111, #23635, #25522, #28182, #25684, #23317, #6624, #21262, #1765, #18738, #11046, #18898, #20637, #16224, #25837 ),
 .UNSPECIFIED., .F., .F.,
 ( 4, 2, 2, 2, 2, 2, 2, 4 ),
 ( 0.000000000000000000, 0.1249999999999999445, 0.2499999999999998890, 0.4999999999999997780, 0.6249999999999997780, 0.7499999999999996669, 0.8749999999999997780, 1.000000000000000000 ),
 .UNSPECIFIED. ) ;
#28545=LINE ( 'NONE', #6993, #12287 ) ;
#28546=LINE ( 'NONE', #1503, #7763 ) ;
#28549=CARTESIAN_POINT ( 'NONE',  ( 11.37440860439999923, -24.37257236010000128, -1.450121496399996213 ) ) ;
#28555=EDGE_CURVE ( 'NONE', #29870, #3695, #25492, .T. ) ;
#28574=ORIENTED_EDGE ( 'NONE', *, *, #17527, .F. ) ;
#28577=CARTESIAN_POINT ( 'NONE',  ( -13.12132034329999897, 20.99999999999999645, -69.22132034359999864 ) ) ;
#28581=CARTESIAN_POINT ( 'NONE',  ( 10.99999999979999998, 20.99999999990000887, -70.09999999999999432 ) ) ;
#28582=LINE ( 'NONE', #2154, #28595 ) ;
#28584=CARTESIAN_POINT ( 'NONE',  ( 9.500000000000000000, 21.70000000000000284, -64.10000000019999788 ) ) ;
#28592=LINE ( 'NONE', #7799, #19812 ) ;
#28595=VECTOR ( 'NONE', #6704, 1000.000000000000000 ) ;
#28596=DIRECTION ( 'NONE',  ( -1.000000000000000000, 0.000000000000000000, -2.257144471330000330E-12 ) ) ;
#28608=VERTEX_POINT ( 'NONE', #15889 ) ;
#28627=DIRECTION ( 'NONE',  ( 0.000000000000000000, 0.000000000000000000, -1.000000000000000000 ) ) ;
#28629=CARTESIAN_POINT ( 'NONE',  ( -13.99999999969999820, 20.99999999999999645, -51.10000000000000142 ) ) ;
#28633=CARTESIAN_POINT ( 'NONE',  ( -10.24010329480000081, 19.99999999999999645, -1.477379946600000604 ) ) ;
#28635=FACE_OUTER_BOUND ( 'NONE', #24807, .T. ) ;
#28636=VERTEX_POINT ( 'NONE', #22126 ) ;
#28644=VERTEX_POINT ( 'NONE', #8563 ) ;
#28647=EDGE_CURVE ( 'NONE', #24608, #26791, #26671, .T. ) ;
#28652=CARTESIAN_POINT ( 'NONE',  ( 10.89131017139999891, -24.73114799890000270, -1.811764705899998606 ) ) ;
#28657=VECTOR ( 'NONE', #7250, 1000.000000000000000 ) ;
#28658=PLANE ( 'NONE',  #12175 ) ;
#28673=CARTESIAN_POINT ( 'NONE',  ( -10.00000000070000183, -25.00000000000000000, -26.16393202249999916 ) ) ;
#28677=VERTEX_POINT ( 'NONE', #25579 ) ;
#28681=EDGE_CURVE ( 'NONE', #15176, #2437, #27609, .T. ) ;
#28685=FACE_OUTER_BOUND ( 'NONE', #22925, .T. ) ;
#28691=ADVANCED_FACE ( 'NONE', ( #1188 ), #10052, .F. ) ;
#28714=DIRECTION ( 'NONE',  ( 1.595945597898660305E-12, -0.7071067811865475727, -0.7071067811865475727 ) ) ;
#28717=VERTEX_POINT ( 'NONE', #13928 ) ;
#28719=CARTESIAN_POINT ( 'NONE',  ( 2.910560681360000016E-11, 19.99999999999999645, -45.10000000000000142 ) ) ;
#28723=DIRECTION ( 'NONE',  ( 0.000000000000000000, 1.000000000000000000, 0.000000000000000000 ) ) ;
#28724=CARTESIAN_POINT ( 'NONE',  ( -10.70000000000117168, -25.27195344040325864, -25.92068947064144524 ) ) ;
#28727=ORIENTED_EDGE ( 'NONE', *, *, #20977, .F. ) ;
#28737=VECTOR ( 'NONE', #600, 1000.000000000000000 ) ;
#28738=CARTESIAN_POINT ( 'NONE',  ( 7.797918471980000099, 19.99999999999999645, -43.60208152801600079 ) ) ;
#28747=ORIENTED_EDGE ( 'NONE', *, *, #1679, .T. ) ;
#28748=EDGE_CURVE ( 'NONE', #11411, #18136, #3042, .T. ) ;
#28751=EDGE_CURVE ( 'NONE', #27161, #29903, #18812, .T. ) ;
#28752=EDGE_LOOP ( 'NONE', ( #21209, #20640, #2518, #30226 ) ) ;
#28754=CARTESIAN_POINT ( 'NONE',  ( 12.55799324160000019, 20.99999999999999645, -55.95247857500000066 ) ) ;
#28758=CARTESIAN_POINT ( 'NONE',  ( -10.69999999930000101, -27.00000000000000000, -25.39999999999999858 ) ) ;
#28770=CARTESIAN_POINT ( 'NONE',  ( -10.69999999999999929, -123.9932870109000049, -32.02938626120000265 ) ) ;
#28804=EDGE_CURVE ( 'NONE', #17105, #17588, #9390, .T. ) ;
#28810=ORIENTED_EDGE ( 'NONE', *, *, #19986, .T. ) ;
#28822=DIRECTION ( 'NONE',  ( -1.000000000000000000, 0.000000000000000000, 0.000000000000000000 ) ) ;
#28823=AXIS2_PLACEMENT_3D ( 'NONE', #18609, #13415, #20502 ) ;
#28836=ORIENTED_EDGE ( 'NONE', *, *, #5558, .T. ) ;
#28852=ORIENTED_EDGE ( 'NONE', *, *, #11146, .F. ) ;
#28863=DIRECTION ( 'NONE',  ( 0.000000000000000000, 1.000000000000000000, 0.000000000000000000 ) ) ;
#28875=EDGE_CURVE ( 'NONE', #1244, #27171, #19109, .T. ) ;
#28892=DIRECTION ( 'NONE',  ( -1.000000000000000000, 0.000000000000000000, 0.000000000000000000 ) ) ;
#28896=VECTOR ( 'NONE', #7516, 1000.000000000000000 ) ;
#28907=ORIENTED_EDGE ( 'NONE', *, *, #18279, .T. ) ;
#28913=ORIENTED_EDGE ( 'NONE', *, *, #23303, .F. ) ;
#28930=EDGE_CURVE ( 'NONE', #20670, #22879, #30073, .T. ) ;
#28932=DIRECTION ( 'NONE',  ( 0.000000000000000000, 1.000000000000000000, 0.000000000000000000 ) ) ;
#28940=CARTESIAN_POINT ( 'NONE',  ( 8.999999999770000869, 21.70000000000000284, -45.10000000000000142 ) ) ;
#28948=EDGE_LOOP ( 'NONE', ( #21450, #26160, #3163, #26273, #6824, #27697, #15206, #19936, #6299, #4764, #11845, #15665 ) ) ;
#28949=ORIENTED_EDGE ( 'NONE', *, *, #21707, .T. ) ;
#28951=ORIENTED_EDGE ( 'NONE', *, *, #12886, .F. ) ;
#28956=CARTESIAN_POINT ( 'NONE',  ( 10.00000000070000183, -30.00000000000000000, -28.40000000000000213 ) ) ;
#28960=CARTESIAN_POINT ( 'NONE',  ( -10.99999999969999998, 20.99999999999999645, -70.09999999999999432 ) ) ;
#28963=ORIENTED_EDGE ( 'NONE', *, *, #28748, .T. ) ;
#28973=B_SPLINE_CURVE_WITH_KNOTS ( 'NONE', 3,
 ( #18824, #23571, #31100, #19140, #25922, #6555 ),
 .UNSPECIFIED., .F., .F.,
 ( 4, 2, 4 ),
 ( 0.000000000000000000, 0.5000000000000000000, 1.000000000000000000 ),
 .UNSPECIFIED. ) ;
#28982=CARTESIAN_POINT ( 'NONE',  ( 13.67718073920000066, 21.70000000000000284, -57.16242423349999768 ) ) ;
#28985=ORIENTED_EDGE ( 'NONE', *, *, #14412, .F. ) ;
#28987=CARTESIAN_POINT ( 'NONE',  ( -10.88910015670000142, 21.70000000000000284, -56.10000000020000499 ) ) ;
#28992=DIRECTION ( 'NONE',  ( 1.000000000000000000, -6.668066630619518976E-24, -2.257150022442225012E-12 ) ) ;
#28993=CARTESIAN_POINT ( 'NONE',  ( 10.69999999989999928, -25.00000000000000000, -7.274962170899998526 ) ) ;
#28995=DIRECTION ( 'NONE',  ( 0.000000000000000000, -1.000000000000000000, 0.000000000000000000 ) ) ;
#29008=LINE ( 'NONE', #2886, #10204 ) ;
#29013=VECTOR ( 'NONE', #20593, 1000.000000000000000 ) ;
#29021=ORIENTED_EDGE ( 'NONE', *, *, #26296, .F. ) ;
#29022=CARTESIAN_POINT ( 'NONE',  ( -11.08586295458008486, 19.99999999999999645, -1.599967101673252401 ) ) ;
#29035=VECTOR ( 'NONE', #26820, 1000.000000000000000 ) ;
#29038=CARTESIAN_POINT ( 'NONE',  ( 10.00000000070000183, 19.99999999999999645, -42.39999999999999858 ) ) ;
#29041=FACE_OUTER_BOUND ( 'NONE', #18630, .T. ) ;
#29045=AXIS2_PLACEMENT_3D ( 'NONE', #19729, #9507, #16729 ) ;
#29064=VECTOR ( 'NONE', #7520, 1000.000000000000000 ) ;
#29066=EDGE_CURVE ( 'NONE', #27949, #10599, #4758, .T. ) ;
#29092=EDGE_LOOP ( 'NONE', ( #4531, #11387, #20354, #20127, #22488, #4323, #28373 ) ) ;
#29094=ORIENTED_EDGE ( 'NONE', *, *, #6339, .F. ) ;
#29095=CARTESIAN_POINT ( 'NONE',  ( -10.00000000057676530, -41.43235263067919760, -26.99482620585297710 ) ) ;
#29098=VERTEX_POINT ( 'NONE', #24251 ) ;
#29101=VERTEX_POINT ( 'NONE', #24570 ) ;
#29109=CIRCLE ( 'NONE', #16039, 1.100000000390000787 ) ;
#29110=EDGE_CURVE ( 'NONE', #5828, #25188, #357, .T. ) ;
#29135=EDGE_LOOP ( 'NONE', ( #6106, #6360, #30475, #11665 ) ) ;
#29138=VERTEX_POINT ( 'NONE', #29432 ) ;
#29144=CARTESIAN_POINT ( 'NONE',  ( -13.67718144140000014, 21.70000000000000284, -57.16242377749999548 ) ) ;
#29147=CARTESIAN_POINT ( 'NONE',  ( 10.69999999992642614, -25.11956699865401532, -9.802329118429168986 ) ) ;
#29154=CARTESIAN_POINT ( 'NONE',  ( -10.69999999930000101, -29.06671945329999929, -26.22544931050000017 ) ) ;
#29157=FACE_OUTER_BOUND ( 'NONE', #16631, .T. ) ;
#29158=DIRECTION ( 'NONE',  ( 0.000000000000000000, 1.000000000000000000, 0.000000000000000000 ) ) ;
#29159=CARTESIAN_POINT ( 'NONE',  ( -11.19633371010000111, -24.50869457490000158, -1.530575679400000944 ) ) ;
#29160=CARTESIAN_POINT ( 'NONE',  ( -12.12499970569999874, 20.99999999999999645, -55.73512393480000071 ) ) ;
#29166=EDGE_LOOP ( 'NONE', ( #15337, #14372, #25687, #23814 ) ) ;
#29170=CARTESIAN_POINT ( 'NONE',  ( -11.56700259526638419, 19.99999999999999645, -1.400000000399997946 ) ) ;
#29178=CARTESIAN_POINT ( 'NONE',  ( -15.72433334783165293, 11.02535689765575455, -1.400000000000001910 ) ) ;
#29187=DIRECTION ( 'NONE',  ( -0.9915824307782121760, 0.1294769592320275942, 0.000000000000000000 ) ) ;
#29191=B_SPLINE_CURVE_WITH_KNOTS ( 'NONE', 3,
 ( #9806, #26789, #5233, #2568, #19563, #3026 ),
 .UNSPECIFIED., .F., .F.,
 ( 4, 2, 4 ),
 ( 0.000000000000000000, 0.5000000000000000000, 1.000000000000000000 ),
 .UNSPECIFIED. ) ;
#29197=B_SPLINE_CURVE_WITH_KNOTS ( 'NONE', 3,
 ( #14703, #14397, #2586, #21633, #5092, #10133 ),
 .UNSPECIFIED., .F., .F.,
 ( 4, 2, 4 ),
 ( 0.000000000000000000, 0.5000000000000000000, 1.000000000000000000 ),
 .UNSPECIFIED. ) ;
#29203=DIRECTION ( 'NONE',  ( 1.000000000000000000, 0.000000000000000000, 0.000000000000000000 ) ) ;
#29204=LINE ( 'NONE', #10027, #19481 ) ;
#29211=VERTEX_POINT ( 'NONE', #17620 ) ;
#29216=ADVANCED_FACE ( 'NONE', ( #1425 ), #20297, .T. ) ;
#29220=CARTESIAN_POINT ( 'NONE',  ( 10.69999999996467288, -29.52967710426907288, -26.74956343519520274 ) ) ;
#29223=CARTESIAN_POINT ( 'NONE',  ( 13.99999999979999821, 20.99999999999999645, -67.09999999999999432 ) ) ;
#29234=CARTESIAN_POINT ( 'NONE',  ( -10.69999999999999929, -127.2537393281999982, -34.36317439833000265 ) ) ;
#29235=CARTESIAN_POINT ( 'NONE',  ( 10.69999999999999929, -27.00000000000000000, -31.39999999999999858 ) ) ;
#29239=PLANE ( 'NONE',  #11744 ) ;
#29241=B_SPLINE_CURVE_WITH_KNOTS ( 'NONE', 3,
 ( #2022, #23264, #6419, #16478, #30808, #16017 ),
 .UNSPECIFIED., .F., .F.,
 ( 4, 2, 4 ),
 ( 0.000000000000000000, 0.5000000000000008882, 1.000000000000000000 ),
 .UNSPECIFIED. ) ;
#29249=ORIENTED_EDGE ( 'NONE', *, *, #15208, .T. ) ;
#29264=ORIENTED_EDGE ( 'NONE', *, *, #9638, .F. ) ;
#29280=FACE_OUTER_BOUND ( 'NONE', #14501, .T. ) ;
#29293=CARTESIAN_POINT ( 'NONE',  ( 10.00000000070000183, -130.0000000000000000, -41.24671599790000442 ) ) ;
#29308=DIRECTION ( 'NONE',  ( 1.000000000000000000, 0.000000000000000000, 0.000000000000000000 ) ) ;
#29311=EDGE_CURVE ( 'NONE', #3166, #11286, #22663, .T. ) ;
#29327=B_SPLINE_CURVE_WITH_KNOTS ( 'NONE', 5,
 ( #3488, #30087, #26956, #1138, #993, #24599 ),
 .UNSPECIFIED., .F., .F.,
 ( 6, 6 ),
 ( 3.365645383459999973, 3.604193613869999702 ),
 .UNSPECIFIED. ) ;
#29331=FACE_OUTER_BOUND ( 'NONE', #11402, .T. ) ;
#29334=DIRECTION ( 'NONE',  ( -0.000000000000000000, 1.000000000000000000, -2.258510841069999963E-12 ) ) ;
#29360=CARTESIAN_POINT ( 'NONE',  ( 11.66358246589999936, -24.14124255329999968, -1.399999999999998579 ) ) ;
#29362=VECTOR ( 'NONE', #19225, 1000.000000000000000 ) ;
#29379=AXIS2_PLACEMENT_3D ( 'NONE', #6856, #16457, #16306 ) ;
#29382=ORIENTED_EDGE ( 'NONE', *, *, #21142, .T. ) ;
#29389=CARTESIAN_POINT ( 'NONE',  ( 9.999999999969375608, -29.39900052789773000, -30.24364015896112434 ) ) ;
#29393=CARTESIAN_POINT ( 'NONE',  ( -10.69999999999999929, -120.8032508028999956, -31.27837281569999917 ) ) ;
#29412=DIRECTION ( 'NONE',  ( 0.000000000000000000, -1.000000000000000000, 0.000000000000000000 ) ) ;
#29413=DIRECTION ( 'NONE',  ( -2.257127817980000114E-12, 0.000000000000000000, -1.000000000000000000 ) ) ;
#29415=B_SPLINE_CURVE_WITH_KNOTS ( 'NONE', 3,
 ( #26437, #2822, #7387, #24387, #635, #24080 ),
 .UNSPECIFIED., .F., .F.,
 ( 4, 2, 4 ),
 ( 0.000000000000000000, 0.5000000000000000000, 1.000000000000000000 ),
 .UNSPECIFIED. ) ;
#29419=DIRECTION ( 'NONE',  ( 1.000000000000000000, 6.668066630619518976E-24, -2.257150022442225012E-12 ) ) ;
#29432=CARTESIAN_POINT ( 'NONE',  ( 10.89131017049999883, -25.00000000000000000, -1.811764705999995062 ) ) ;
#29437=DIRECTION ( 'NONE',  ( 0.000000000000000000, -2.257145581549999994E-12, -1.000000000000000000 ) ) ;
#29438=CARTESIAN_POINT ( 'NONE',  ( 10.69999999999822826, -24.07808197001402917, -27.61475634682798841 ) ) ;
#29440=ADVANCED_FACE ( 'NONE', ( #25662 ), #4091, .F. ) ;
#29441=DIRECTION ( 'NONE',  ( 0.000000000000000000, -1.000000000000000000, 2.257145581549999994E-12 ) ) ;
#29446=ORIENTED_EDGE ( 'NONE', *, *, #26211, .F. ) ;
#29453=VERTEX_POINT ( 'NONE', #23458 ) ;
#29458=CARTESIAN_POINT ( 'NONE',  ( -10.69999999999999929, -26.63513617180875670, -25.40000000000000213 ) ) ;
#29463=APPLICATION_CONTEXT ( 'automotive_design' ) ;
#29464=DIRECTION ( 'NONE',  ( -1.000000000000000000, 0.000000000000000000, -2.257144471330000330E-12 ) ) ;
#29469=DIRECTION ( 'NONE',  ( 1.000000000000000000, 1.167320209990000089E-13, -2.253435535809999718E-12 ) ) ;
#29470=CARTESIAN_POINT ( 'NONE',  ( -11.48163258379999974, -24.28840542069999842, -1.419991652300001128 ) ) ;
#29476=B_SPLINE_CURVE_WITH_KNOTS ( 'NONE', 3,
 ( #9425, #23616, #23145, #16359, #14011, #30841 ),
 .UNSPECIFIED., .F., .F.,
 ( 4, 2, 4 ),
 ( 0.000000000000000000, 0.5000000000000000000, 1.000000000000000000 ),
 .UNSPECIFIED. ) ;
#29487=STYLED_ITEM ( 'NONE', ( #9331 ), #10459 ) ;
#29513=VECTOR ( 'NONE', #4354, 1000.000000000000000 ) ;
#29517=LINE ( 'NONE', #5903, #26334 ) ;
#29519=CARTESIAN_POINT ( 'NONE',  ( -20.90359613196108057, 16.91137956061550085, -0.6999999999999992895 ) ) ;
#29523=VERTEX_POINT ( 'NONE', #19500 ) ;
#29527=FACE_OUTER_BOUND ( 'NONE', #1398, .T. ) ;
#29531=B_SPLINE_CURVE_WITH_KNOTS ( 'NONE', 3,
 ( #18042, #10517, #3575, #13169, #22944, #27191, #30009, #5629, #15229, #926, #19440, #721, #17074, #2764, #29178, #12357, #10312, #24475 ),
 .UNSPECIFIED., .F., .F.,
 ( 4, 2, 2, 2, 2, 2, 2, 2, 4 ),
 ( 0.000000000000000000, 0.1250000000000000000, 0.2500000000000000000, 0.3750000000000000000, 0.5000000000000000000, 0.6250000000000000000, 0.7500000000000000000, 0.8750000000000000000, 1.000000000000000000 ),
 .UNSPECIFIED. ) ;
#29537=CARTESIAN_POINT ( 'NONE',  ( -2.299991308520000465E-10, 20.99999999999999645, -64.10000000000000853 ) ) ;
#29543=CARTESIAN_POINT ( 'NONE',  ( -10.00000000000000000, 19.99999999999999645, -42.39999999999999858 ) ) ;
#29547=VECTOR ( 'NONE', #12322, 1000.000000000000000 ) ;
#29548=PLANE ( 'NONE',  #10710 ) ;
#29553=VECTOR ( 'NONE', #26905, 1000.000000000000000 ) ;
#29563=EDGE_LOOP ( 'NONE', ( #6134, #17835, #5317, #27703 ) ) ;
#29567=LINE ( 'NONE', #23087, #13041 ) ;
#29570=LINE ( 'NONE', #27508, #26508 ) ;
#29588=B_SPLINE_CURVE_WITH_KNOTS ( 'NONE', 5,
 ( #20363, #27916, #27750, #27286, #6036, #6196, #22887, #25087, #29956, #13275, #17983, #24777 ),
 .UNSPECIFIED., .F., .F.,
 ( 6, 3, 3, 6 ),
 ( 0.000000000000000000, 1.359200785760000141, 2.718430693529999775, 3.788335907300000027 ),
 .UNSPECIFIED. ) ;
#29598=DIRECTION ( 'NONE',  ( -1.000000000000000000, 0.000000000000000000, 0.000000000000000000 ) ) ;
#29610=VERTEX_POINT ( 'NONE', #29235 ) ;
#29622=CARTESIAN_POINT ( 'NONE',  ( 0.000000000000000000, 21.70000000000000284, -44.10000000017312516 ) ) ;
#29624=LINE ( 'NONE', #6011, #26861 ) ;
#29626=ADVANCED_FACE ( 'NONE', ( #20259, #30010, #27193 ), #10364, .T. ) ;
#29634=B_SPLINE_CURVE_WITH_KNOTS ( 'NONE', 3,
 ( #5265, #24468, #2902, #22106, #13592, #11079 ),
 .UNSPECIFIED., .F., .F.,
 ( 4, 2, 4 ),
 ( 0.000000000000000000, 0.4999999999999975575, 1.000000000000000000 ),
 .UNSPECIFIED. ) ;
#29636=CLOSED_SHELL ( 'NONE', ( #26454, #30344, #20507, #41, #17860, #14861, #29626, #6224, #11695, #26902, #14069, #10829, #18520, #17260, #28691, #15755, #26327, #16731, #19031, #15028, #2551, #16330, #18919, #31076, #613, #29216, #30653, #30281, #27850, #11397, #12196, #10461, #13280, #6272, #26000, #28027, #18306, #15916, #4283, #323, #19710, #12476, #12198, #18217, #16098, #2438, #24965, #28147, #15949, #3700, #10469, #10792, #15805, #12581, #28001, #11216, #4334, #25967, #27042, #27256, #19136, #9788, #28377, #27656, #5220, #22786, #6102, #16513, #30248, #24390, #22322, #28266, #24005, #23045, #29841, #27947, #24198, #676, #1957, #9433, #14311, #9618, #26625, #5281, #7901, #27190, #8130, #7905, #23551, #9057, #28283, #3249, #25854, #10263, #10861, #27143, #29996, #10228, #10321, #4780, #16941, #20383, #23257, #12341, #10567, #7920, #12941, #727, #13076, #15245, #9228, #11582, #14911, #22507, #11130, #4862, #7632, #21735, #2020, #19974, #25172, #13151, #13736, #6681, #15598, #18408, #19647, #18119, #17136, #10299, #29440, #1271, #5561, #26553, #19583, #3638, #4822, #8027, #23646, #30183, #25390, #17518, #17282 ) ) ;
#29641=ORIENTED_EDGE ( 'NONE', *, *, #12979, .T. ) ;
#29656=B_SPLINE_CURVE_WITH_KNOTS ( 'NONE', 3,
 ( #7370, #21226, #24205, #13997 ),
 .UNSPECIFIED., .F., .F.,
 ( 4, 4 ),
 ( 0.000000000000000000, 1.000000000000000000 ),
 .UNSPECIFIED. ) ;
#29668=ORIENTED_EDGE ( 'NONE', *, *, #6169, .T. ) ;
#29675=CARTESIAN_POINT ( 'NONE',  ( 11.37440860439999923, -24.37257236010000128, -1.450121496399996213 ) ) ;
#29685=ORIENTED_EDGE ( 'NONE', *, *, #26573, .F. ) ;
#29687=CARTESIAN_POINT ( 'NONE',  ( -10.46446609379999870, 21.70000000000000284, -54.63553390589999736 ) ) ;
#29697=VECTOR ( 'NONE', #23787, 1000.000000000000000 ) ;
#29702=DIRECTION ( 'NONE',  ( 1.000000000000000000, 0.000000000000000000, -0.000000000000000000 ) ) ;
#29706=DIRECTION ( 'NONE',  ( -1.000000000000000000, 0.000000000000000000, -2.257144471330000330E-12 ) ) ;
#29710=ORIENTED_EDGE ( 'NONE', *, *, #21840, .F. ) ;
#29713=ORIENTED_EDGE ( 'NONE', *, *, #12886, .T. ) ;
#29719=VECTOR ( 'NONE', #14965, 1000.000000000000000 ) ;
#29720=EDGE_LOOP ( 'NONE', ( #27862, #1428, #15523, #24266, #6494 ) ) ;
#29724=CARTESIAN_POINT ( 'NONE',  ( -13.12132034329999897, 21.69999999990000106, -69.22132034359999864 ) ) ;
#29736=CARTESIAN_POINT ( 'NONE',  ( 10.00000000070000183, -27.00000000000000000, -25.39999999999999858 ) ) ;
#29738=CYLINDRICAL_SURFACE ( 'NONE', #16814, 26.80000000000000071 ) ;
#29750=ORIENTED_EDGE ( 'NONE', *, *, #11351, .F. ) ;
#29756=LINE ( 'NONE', #12612, #2108 ) ;
#29757=CARTESIAN_POINT ( 'NONE',  ( -3.510330247560000227, -1.917702154400000136, -44.00000000037249492 ) ) ;
#29776=CARTESIAN_POINT ( 'NONE',  ( 9.999999999770000869, 21.35000000040000145, -60.10000000000000142 ) ) ;
#29782=EDGE_LOOP ( 'NONE', ( #17969, #15282, #3017, #17921 ) ) ;
#29792=FACE_OUTER_BOUND ( 'NONE', #17899, .T. ) ;
#29808=EDGE_CURVE ( 'NONE', #26986, #15618, #20252, .T. ) ;
#29812=CARTESIAN_POINT ( 'NONE',  ( -10.79767709090000061, -24.52928868880000124, -0.9448358073000027169 ) ) ;
#29813=CARTESIAN_POINT ( 'NONE',  ( -9.999999999559999964, 21.70000000000000284, -60.10000000000000142 ) ) ;
#29814=ORIENTED_EDGE ( 'NONE', *, *, #16373, .F. ) ;
#29822=DIRECTION ( 'NONE',  ( -0.000000000000000000, 1.000000000000000000, -2.257145581549999994E-12 ) ) ;
#29841=ADVANCED_FACE ( 'NONE', ( #6564 ), #18676, .T. ) ;
#29843=DIRECTION ( 'NONE',  ( -1.595945597898660305E-12, 0.7071067811865475727, 0.7071067811865475727 ) ) ;
#29862=AXIS2_PLACEMENT_3D ( 'NONE', #21432, #11518, #2080 ) ;
#29864=ORIENTED_EDGE ( 'NONE', *, *, #12253, .F. ) ;
#29870=VERTEX_POINT ( 'NONE', #6870 ) ;
#29877=DIRECTION ( 'NONE',  ( 0.000000000000000000, -2.257145581549999994E-12, -1.000000000000000000 ) ) ;
#29887=EDGE_CURVE ( 'NONE', #26129, #28677, #22495, .T. ) ;
#29898=CARTESIAN_POINT ( 'NONE',  ( 9.499999999770000869, 21.70000000000000284, -64.10000000000000853 ) ) ;
#29903=VERTEX_POINT ( 'NONE', #2622 ) ;
#29906=ORIENTED_EDGE ( 'NONE', *, *, #24846, .T. ) ;
#29912=VERTEX_POINT ( 'NONE', #7348 ) ;
#29922=ORIENTED_EDGE ( 'NONE', *, *, #26073, .F. ) ;
#29928=DIRECTION ( 'NONE',  ( -5.551115123049999208E-18, 0.000000000000000000, -1.000000000000000000 ) ) ;
#29942=CYLINDRICAL_SURFACE ( 'NONE', #28823, 0.9999999999999988898 ) ;
#29945=EDGE_CURVE ( 'NONE', #8872, #20466, #6729, .T. ) ;
#29951=CARTESIAN_POINT ( 'NONE',  ( -16.83342759559999635, -9.000000000000001776, -0.6999999999999992895 ) ) ;
#29956=CARTESIAN_POINT ( 'NONE',  ( 9.450015891510000543, 19.99999999999999645, -44.04981409108790302 ) ) ;
#29970=CARTESIAN_POINT ( 'NONE',  ( -10.98966923020000053, -24.66097101990000340, -1.689678586199998334 ) ) ;
#29973=EDGE_CURVE ( 'NONE', #29523, #17368, #30957, .T. ) ;
#29974=CARTESIAN_POINT ( 'NONE',  ( 10.69999999999999929, -29.06671945340000107, -26.22544931050000017 ) ) ;
#29988=CARTESIAN_POINT ( 'NONE',  ( -9.500000000000000000, 20.99999999999999645, -60.10000000019999788 ) ) ;
#29996=ADVANCED_FACE ( 'NONE', ( #17242 ), #26849, .F. ) ;
#30005=CARTESIAN_POINT ( 'NONE',  ( 10.00000000070000183, -30.00000000000000000, -28.40000000000000213 ) ) ;
#30009=CARTESIAN_POINT ( 'NONE',  ( -16.85878449349630870, 12.10909424796742329, -1.400000000000002132 ) ) ;
#30010=FACE_BOUND ( 'NONE', #17628, .T. ) ;
#30015=VERTEX_POINT ( 'NONE', #25704 ) ;
#30028=EDGE_LOOP ( 'NONE', ( #26628, #24730, #10265, #14603 ) ) ;
#30039=EDGE_LOOP ( 'NONE', ( #24501, #15549, #3784, #8866, #21026 ) ) ;
#30044=CARTESIAN_POINT ( 'NONE',  ( 9.000000000000000000, -130.0000000000000000, -42.39999999999999858 ) ) ;
#30052=VECTOR ( 'NONE', #18580, 1000.000000000000000 ) ;
#30054=VERTEX_POINT ( 'NONE', #16862 ) ;
#30063=EDGE_LOOP ( 'NONE', ( #27045, #5332, #30729, #21101 ) ) ;
#30067=AXIS2_PLACEMENT_3D ( 'NONE', #21113, #4579, #28184 ) ;
#30073=B_SPLINE_CURVE_WITH_KNOTS ( 'NONE', 5,
 ( #22401, #848, #19889, #2585, #29470, #7455, #26653, #29159, #7309, #7906, #27116, #5091 ),
 .UNSPECIFIED., .F., .F.,
 ( 6, 3, 3, 6 ),
 ( -1.429360140840000071, -1.143488112685019376, -0.5717440563530578057, -0.2292465842890714089 ),
 .UNSPECIFIED. ) ;
#30075=CARTESIAN_POINT ( 'NONE',  ( -10.69999999999999929, -24.87867968679999819, -26.27867968680000033 ) ) ;
#30081=CARTESIAN_POINT ( 'NONE',  ( -10.69999999997017248, -29.92209366267258019, -29.18485145335326436 ) ) ;
#30087=CARTESIAN_POINT ( 'NONE',  ( 10.69999999999999929, -24.90230198360000102, -26.25506235030000113 ) ) ;
#30091=DIRECTION ( 'NONE',  ( 1.000000000000000000, -0.000000000000000000, -2.257150022439999944E-12 ) ) ;
#30095=CARTESIAN_POINT ( 'NONE',  ( 10.92933985129999996, -24.70409753159999866, -1.761594278200002917 ) ) ;
#30099=ORIENTED_EDGE ( 'NONE', *, *, #17883, .T. ) ;
#30103=VECTOR ( 'NONE', #28892, 1000.000000000000000 ) ;
#30109=CARTESIAN_POINT ( 'NONE',  ( 18.13191322229999969, 10.47263190749999495, -0.7999999992999995424 ) ) ;
#30132=CARTESIAN_POINT ( 'NONE',  ( -10.32522729140000095, -24.73114799960000099, -1.399999999999998579 ) ) ;
#30134=EDGE_LOOP ( 'NONE', ( #13060, #22154, #4732, #13412, #6652 ) ) ;
#30140=CARTESIAN_POINT ( 'NONE',  ( -12.77820031340000106, 20.99999999999999645, -56.10000000020000499 ) ) ;
#30151=CARTESIAN_POINT ( 'NONE',  ( -11.63809019400000011, -24.14124255240000139, -0.6999999999999992895 ) ) ;
#30164=FACE_OUTER_BOUND ( 'NONE', #860, .T. ) ;
#30175=CARTESIAN_POINT ( 'NONE',  ( -10.49791847189999849, 19.99999999999999645, -3.602081527999998034 ) ) ;
#30183=ADVANCED_FACE ( 'NONE', ( #9627 ), #11839, .F. ) ;
#30188=DIRECTION ( 'NONE',  ( 0.000000000000000000, 1.000000000000000000, 0.000000000000000000 ) ) ;
#30191=AXIS2_PLACEMENT_3D ( 'NONE', #9611, #21728, #9764 ) ;
#30194=FACE_OUTER_BOUND ( 'NONE', #13069, .T. ) ;
#30200=EDGE_CURVE ( 'NONE', #12805, #9943, #7229, .T. ) ;
#30208=DIRECTION ( 'NONE',  ( 0.000000000000000000, 1.000000000000000000, 0.000000000000000000 ) ) ;
#30214=VERTEX_POINT ( 'NONE', #11989 ) ;
#30216=CARTESIAN_POINT ( 'NONE',  ( -10.00000000000000000, 19.99999999999999645, -42.39999999999999858 ) ) ;
#30222=FILL_AREA_STYLE ('',( #6460 ) ) ;
#30226=ORIENTED_EDGE ( 'NONE', *, *, #5119, .T. ) ;
#30248=ADVANCED_FACE ( 'NONE', ( #17327 ), #197, .F. ) ;
#30251=FACE_OUTER_BOUND ( 'NONE', #3127, .T. ) ;
#30255=ORIENTED_EDGE ( 'NONE', *, *, #5615, .T. ) ;
#30259=FACE_OUTER_BOUND ( 'NONE', #27207, .T. ) ;
#30266=ORIENTED_EDGE ( 'NONE', *, *, #3084, .F. ) ;
#30267=DIRECTION ( 'NONE',  ( 0.000000000000000000, 0.000000000000000000, 1.000000000000000000 ) ) ;
#30271=DIRECTION ( 'NONE',  ( -5.551115123049999208E-18, 0.000000000000000000, -1.000000000000000000 ) ) ;
#30277=ORIENTED_EDGE ( 'NONE', *, *, #6584, .T. ) ;
#30281=ADVANCED_FACE ( 'NONE', ( #29280 ), #27083, .T. ) ;
#30289=LINE ( 'NONE', #10937, #3984 ) ;
#30300=DIRECTION ( 'NONE',  ( -1.000000000000000000, 0.000000000000000000, 0.000000000000000000 ) ) ;
#30312=ORIENTED_EDGE ( 'NONE', *, *, #5119, .F. ) ;
#30313=CARTESIAN_POINT ( 'NONE',  ( -10.49243769149999927, -24.66097101990000340, -1.192453596599994725 ) ) ;
#30315=CARTESIAN_POINT ( 'NONE',  ( -7.797918471980000099, 19.99999999999999645, -43.60208152801600079 ) ) ;
#30318=DIRECTION ( 'NONE',  ( 1.595945597898660305E-12, 0.7071067811865475727, 0.7071067811865475727 ) ) ;
#30319=CARTESIAN_POINT ( 'NONE',  ( -10.69999999999999929, -24.61475988249999958, -26.57332276320000020 ) ) ;
#30333=CARTESIAN_POINT ( 'NONE',  ( 12.41983200457754322, 21.70000000000019469, -55.86851685976566273 ) ) ;
#30339=DIRECTION ( 'NONE',  ( 0.000000000000000000, -1.000000000000000000, 0.000000000000000000 ) ) ;
#30344=ADVANCED_FACE ( 'NONE', ( #12445 ), #19997, .F. ) ;
#30351=VECTOR ( 'NONE', #30267, 1000.000000000000000 ) ;
#30353=ORIENTED_EDGE ( 'NONE', *, *, #28804, .F. ) ;
#30366=AXIS2_PLACEMENT_3D ( 'NONE', #12481, #393, #4800 ) ;
#30375=VECTOR ( 'NONE', #2884, 1000.000000000000000 ) ;
#30381=FACE_OUTER_BOUND ( 'NONE', #8472, .T. ) ;
#30382=ORIENTED_EDGE ( 'NONE', *, *, #2867, .T. ) ;
#30391=VERTEX_POINT ( 'NONE', #26618 ) ;
#30402=VECTOR ( 'NONE', #1423, 1000.000000000000000 ) ;
#30404=DIRECTION ( 'NONE',  ( 1.000000000000000000, -0.000000000000000000, -3.489272357540000343E-15 ) ) ;
#30416=EDGE_CURVE ( 'NONE', #15903, #21635, #4744, .T. ) ;
#30419=CARTESIAN_POINT ( 'NONE',  ( -26.22090100435761784, -5.650641260081752826, -1.399999999999999023 ) ) ;
#30420=ORIENTED_EDGE ( 'NONE', *, *, #7023, .T. ) ;
#30438=CIRCLE ( 'NONE', #1272, 1.099999999570000497 ) ;
#30446=EDGE_CURVE ( 'NONE', #14782, #20501, #6135, .T. ) ;
#30449=CARTESIAN_POINT ( 'NONE',  ( 14.76964124820000102, 19.99999999999999645, -1.399999999999998579 ) ) ;
#30461=EDGE_LOOP ( 'NONE', ( #30546, #3631, #5216, #9750 ) ) ;
#30466=CARTESIAN_POINT ( 'NONE',  ( 14.00000000000000000, 20.99999999999999645, -62.80809897700000022 ) ) ;
#30475=ORIENTED_EDGE ( 'NONE', *, *, #7893, .T. ) ;
#30476=EDGE_CURVE ( 'NONE', #5911, #27858, #21325, .T. ) ;
#30478=EDGE_CURVE ( 'NONE', #11286, #26133, #30605, .T. ) ;
#30480=CARTESIAN_POINT ( 'NONE',  ( 10.60826873110000079, -25.00000000000000000, -1.605882352700004123 ) ) ;
#30489=ORIENTED_EDGE ( 'NONE', *, *, #8678, .T. ) ;
#30494=CARTESIAN_POINT ( 'NONE',  ( -10.69999999999999929, -27.00000000000000000, -28.40000000000000213 ) ) ;
#30501=FACE_OUTER_BOUND ( 'NONE', #27903, .T. ) ;
#30502=LINE ( 'NONE', #13973, #9738 ) ;
#30514=CARTESIAN_POINT ( 'NONE',  ( -10.69999999999999929, -24.00000000000000000, -28.40000000000000213 ) ) ;
#30517=VECTOR ( 'NONE', #25597, 1000.000000000000000 ) ;
#30535=EDGE_CURVE ( 'NONE', #14788, #27320, #9739, .T. ) ;
#30538=VERTEX_POINT ( 'NONE', #12033 ) ;
#30539=VECTOR ( 'NONE', #22003, 1000.000000000000000 ) ;
#30541=CARTESIAN_POINT ( 'NONE',  ( -10.88910015670000142, 20.99999999999999645, -56.10000000020000499 ) ) ;
#30542=CARTESIAN_POINT ( 'NONE',  ( 10.00000000070000183, -43.95328087560000085, -27.24755286599999948 ) ) ;
#30545=ORIENTED_EDGE ( 'NONE', *, *, #815, .T. ) ;
#30546=ORIENTED_EDGE ( 'NONE', *, *, #20838, .F. ) ;
#30552=CARTESIAN_POINT ( 'NONE',  ( 10.69999999999999929, -130.0000000000000000, -41.24671599790000442 ) ) ;
#30553=CARTESIAN_POINT ( 'NONE',  ( -10.00000000050000004, -27.56998452010000022, -25.39999999999999858 ) ) ;
#30555=AXIS2_PLACEMENT_3D ( 'NONE', #3052, #14876, #17524 ) ;
#30556=CARTESIAN_POINT ( 'NONE',  ( 26.57440914490000239, -3.469982507400000582, -1.399999999999998579 ) ) ;
#30557=CARTESIAN_POINT ( 'NONE',  ( -10.69999999997255991, -29.40012576568826574, -30.24240556185885254 ) ) ;
#30585=ORIENTED_EDGE ( 'NONE', *, *, #21872, .F. ) ;
#30586=ORIENTED_EDGE ( 'NONE', *, *, #18429, .F. ) ;
#30587=ORIENTED_EDGE ( 'NONE', *, *, #20089, .F. ) ;
#30590=DIRECTION ( 'NONE',  ( 1.000000000000000000, 0.000000000000000000, 0.000000000000000000 ) ) ;
#30601=VECTOR ( 'NONE', #650, 1000.000000000000000 ) ;
#30605=B_SPLINE_CURVE_WITH_KNOTS ( 'NONE', 3,
 ( #23696, #24297, #19582, #14709, #17058, #21480, #21788, #16739, #26053, #26203 ),
 .UNSPECIFIED., .F., .F.,
 ( 4, 2, 2, 2, 4 ),
 ( 0.000000000000000000, 0.2499999999999996669, 0.4999999999999993339, 0.7499999999999996669, 1.000000000000000000 ),
 .UNSPECIFIED. ) ;
#30608=CARTESIAN_POINT ( 'NONE',  ( 26.75124393581684146, 1.948321199505564705, -1.399999999999998801 ) ) ;
#30609=FACE_OUTER_BOUND ( 'NONE', #13285, .T. ) ;
#30636=DIRECTION ( 'NONE',  ( 0.000000000000000000, 0.000000000000000000, -1.000000000000000000 ) ) ;
#30641=LINE ( 'NONE', #23714, #11522 ) ;
#30653=ADVANCED_FACE ( 'NONE', ( #15781 ), #21136, .T. ) ;
#30655=CARTESIAN_POINT ( 'NONE',  ( 8.999999999770000869, 20.99999999999999645, -51.10000000000000142 ) ) ;
#30688=CYLINDRICAL_SURFACE ( 'NONE', #15265, 0.9999999999999988898 ) ;
#30693=ORIENTED_EDGE ( 'NONE', *, *, #20838, .T. ) ;
#30703=CARTESIAN_POINT ( 'NONE',  ( 11.69999999989999928, 19.99999999999999645, -1.049999999600002898 ) ) ;
#30723=CARTESIAN_POINT ( 'NONE',  ( -4.175165894169885483, -119.7166638525666826, -43.39999999999999858 ) ) ;
#30729=ORIENTED_EDGE ( 'NONE', *, *, #6321, .F. ) ;
#30732=ORIENTED_EDGE ( 'NONE', *, *, #29808, .F. ) ;
#30741=AXIS2_PLACEMENT_3D ( 'NONE', #2613, #30794, #12060 ) ;
#30753=CARTESIAN_POINT ( 'NONE',  ( 26.71519619425450642, -2.391783224228639870, -1.399999999999998579 ) ) ;
#30782=CARTESIAN_POINT ( 'NONE',  ( 9.963156062430000404, 19.99999999999999645, -42.69473902060000370 ) ) ;
#30794=DIRECTION ( 'NONE',  ( 1.000000000000000000, 5.998481157687279274E-24, -2.257150022441830001E-12 ) ) ;
#30802=DIRECTION ( 'NONE',  ( 0.000000000000000000, -2.257145581549999994E-12, -1.000000000000000000 ) ) ;
#30807=EDGE_CURVE ( 'NONE', #9747, #20099, #10687, .T. ) ;
#30808=CARTESIAN_POINT ( 'NONE',  ( 10.69999999997516760, -26.60546859447386581, -31.39999999999999147 ) ) ;
#30812=LINE ( 'NONE', #15590, #26230 ) ;
#30828=EDGE_CURVE ( 'NONE', #8540, #11113, #10775, .T. ) ;
#30841=CARTESIAN_POINT ( 'NONE',  ( -13.12132034329999897, 21.69999999990000106, -69.22132034359999864 ) ) ;
#30845=CARTESIAN_POINT ( 'NONE',  ( -9.000000000229999131, 21.70000000000000284, -48.10000000000000142 ) ) ;
#30852=ORIENTED_EDGE ( 'NONE', *, *, #27366, .F. ) ;
#30864=DIRECTION ( 'NONE',  ( -1.000000000000000000, 6.565028073413479156E-24, -2.257144471327815248E-12 ) ) ;
#30867=CARTESIAN_POINT ( 'NONE',  ( -8.999999999710000864, 20.70710678120000381, -44.39289321881399530 ) ) ;
#30868=EDGE_LOOP ( 'NONE', ( #10215, #21710, #21134, #22294 ) ) ;
#30880=CARTESIAN_POINT ( 'NONE',  ( -16.39980503796714828, -21.22523991776962404, -1.399999999999998579 ) ) ;
#30881=VERTEX_POINT ( 'NONE', #27087 ) ;
#30884=ORIENTED_EDGE ( 'NONE', *, *, #2441, .F. ) ;
#30892=ORIENTED_EDGE ( 'NONE', *, *, #9046, .T. ) ;
#30907=VERTEX_POINT ( 'NONE', #17174 ) ;
#30914=PLANE ( 'NONE',  #16285 ) ;
#30917=DIRECTION ( 'NONE',  ( 0.000000000000000000, 1.000000000000000000, 0.000000000000000000 ) ) ;
#30919=CARTESIAN_POINT ( 'NONE',  ( 12.55799324160000019, 20.99999999999999645, -55.95247857500000066 ) ) ;
#30942=CARTESIAN_POINT ( 'NONE',  ( -10.69999999999999929, -24.34033515279999804, -26.95726941919999931 ) ) ;
#30943=LINE ( 'NONE', #16459, #8919 ) ;
#30950=LINE ( 'NONE', #9544, #5712 ) ;
#30953=CYLINDRICAL_SURFACE ( 'NONE', #150, 1.099999999999999201 ) ;
#30957=LINE ( 'NONE', #19461, #8745 ) ;
#30958=CARTESIAN_POINT ( 'NONE',  ( 14.00000000000000000, 20.99999999996851940, -58.04643232978019540 ) ) ;
#30962=DIRECTION ( 'NONE',  ( -0.8775825618903718706, 0.4794255386042047262, 0.000000000000000000 ) ) ;
#30963=ORIENTED_EDGE ( 'NONE', *, *, #11762, .F. ) ;
#30966=ORIENTED_EDGE ( 'NONE', *, *, #19986, .F. ) ;
#30968=CARTESIAN_POINT ( 'NONE',  ( -9.999999999969999109, -24.00000000000000000, -28.40000000000000213 ) ) ;
#30990=DIRECTION ( 'NONE',  ( 0.000000000000000000, 0.000000000000000000, 1.000000000000000000 ) ) ;
#30996=CARTESIAN_POINT ( 'NONE',  ( -10.00000000020000002, 19.99999999999999645, -2.208382156699995047 ) ) ;
#31039=EDGE_CURVE ( 'NONE', #26791, #12957, #3944, .T. ) ;
#31044=ORIENTED_EDGE ( 'NONE', *, *, #21221, .F. ) ;
#31051=CARTESIAN_POINT ( 'NONE',  ( -10.69999999999999929, -27.00000000000000000, -28.40000000000000213 ) ) ;
#31054=LINE ( 'NONE', #23672, #19695 ) ;
#31058=ORIENTED_EDGE ( 'NONE', *, *, #21840, .T. ) ;
#31059=LINE ( 'NONE', #6825, #14008 ) ;
#31061=FACE_OUTER_BOUND ( 'NONE', #29135, .T. ) ;
#31065=CARTESIAN_POINT ( 'NONE',  ( 8.999999999770000869, 21.70000000000000284, -45.10000000000000142 ) ) ;
#31072=EDGE_LOOP ( 'NONE', ( #23189, #12535, #9068, #27533 ) ) ;
#31073=CARTESIAN_POINT ( 'NONE',  ( 18.13191322229999969, -9.527368092500001495, -0.7999999992999995424 ) ) ;
#31076=ADVANCED_FACE ( 'NONE', ( #8333 ), #23148, .T. ) ;
#31079=EDGE_CURVE ( 'NONE', #22666, #11888, #28168, .T. ) ;
#31088=AXIS2_PLACEMENT_3D ( 'NONE', #1133, #13079, #8351 ) ;
#31093=CARTESIAN_POINT ( 'NONE',  ( -10.69999999999999929, -25.00000000000000000, -26.16393202249999916 ) ) ;
#31097=CARTESIAN_POINT ( 'NONE',  ( 9.500000000000000000, 21.70000000000000284, -60.10000000019999788 ) ) ;
#31100=CARTESIAN_POINT ( 'NONE',  ( 10.69999999996243290, -28.46594883620507588, -25.75514764082761587 ) ) ;
#31101=EDGE_CURVE ( 'NONE', #4546, #28608, #193, .T. ) ;
#31106=CARTESIAN_POINT ( 'NONE',  ( 16.20123158649999695, 11.52736809289999620, -1.399999999999998579 ) ) ;
#31109=VECTOR ( 'NONE', #7368, 1000.000000000000000 ) ;
#31114=ORIENTED_EDGE ( 'NONE', *, *, #2366, .T. ) ;
#31116=ORIENTED_EDGE ( 'NONE', *, *, #14521, .T. ) ;
ENDSEC;
END-ISO-10303-21;
